ISO-10303-21;
HEADER;
FILE_DESCRIPTION (('STEP AP214'),
    '1' );
FILE_NAME ('hex bolt gradeab_iso_ISO 4014 - M10 x 100 x 26-S.step',
    '2026-10-09T14:04:53',
    ( '' ),
    ( '' ),
    'SwSTEP 2.0',
    'SolidWorks 2021',
    '' );
FILE_SCHEMA (( 'AUTOMOTIVE_DESIGN' ));
ENDSEC;

DATA;
#33=EDGE_CURVE ( 'NONE', #89169, #22959, #61888, .T. ) ;
#45=ORIENTED_EDGE ( 'NONE', *, *, #78057, .F. ) ;
#59=CARTESIAN_POINT ( 'NONE',  ( 0.000000000000000000, 0.000000000000000000, 8.000000000000000000 ) ) ;
#67=EDGE_CURVE ( 'NONE', #4657, #43097, #41719, .T. ) ;
#70=EDGE_LOOP ( 'NONE', ( #14398, #103627, #81786, #35183, #67385, #53899 ) ) ;
#92=DIRECTION ( 'NONE',  ( 0.000000000000000000, -1.000000000000000000, 0.000000000000000000 ) ) ;
#114=( LENGTH_UNIT ( ) NAMED_UNIT ( * ) SI_UNIT ( .MILLI., .METRE. ) );
#135=EDGE_CURVE ( 'NONE', #78511, #45219, #29192, .T. ) ;
#172=CARTESIAN_POINT ( 'NONE',  ( 84.15356149169568312, 5.000000000000023093, 6.123233995736781074E-16 ) ) ;
#180=DIRECTION ( 'NONE',  ( 0.000000000000000000, 0.000000000000000000, 1.000000000000000000 ) ) ;
#198=CARTESIAN_POINT ( 'NONE',  ( 0.4988340113754564098, 3.871605243940360097, 7.999999999999996447 ) ) ;
#208=VECTOR ( 'NONE', #3737, 1000.000000000000000 ) ;
#227=ORIENTED_EDGE ( 'NONE', *, *, #17235, .T. ) ;
#231=VERTEX_POINT ( 'NONE', #96649 ) ;
#238=CIRCLE ( 'NONE', #77810, 0.4000000000000001887 ) ;
#294=ADVANCED_FACE ( 'NONE', ( #51802 ), #85848, .T. ) ;
#321=CARTESIAN_POINT ( 'NONE',  ( 98.59800593614012598, -5.000000000000020428, 0.000000000000000000 ) ) ;
#361=EDGE_LOOP ( 'NONE', ( #69773, #97426, #67085, #73591, #21283 ) ) ;
#370=DIRECTION ( 'NONE',  ( 0.000000000000000000, -1.000000000000000000, 0.000000000000000000 ) ) ;
#394=DIRECTION ( 'NONE',  ( 0.000000000000000000, 0.5000000000000009992, 0.8660254037844380415 ) ) ;
#402=CARTESIAN_POINT ( 'NONE',  ( 102.0666666666666629, 1.023464760207051730E-14, 0.000000000000000000 ) ) ;
#404=EDGE_CURVE ( 'NONE', #3901, #1310, #12401, .T. ) ;
#425=ORIENTED_EDGE ( 'NONE', *, *, #39572, .T. ) ;
#426=EDGE_CURVE ( 'NONE', #9363, #29639, #83534, .T. ) ;
#491=AXIS2_PLACEMENT_3D ( 'NONE', #31691, #89386, #30635 ) ;
#511=EDGE_CURVE ( 'NONE', #39124, #34646, #11877, .T. ) ;
#535=CARTESIAN_POINT ( 'NONE',  ( 102.0666666666666629, 4.172000000000019249, 0.000000000000000000 ) ) ;
#570=ORIENTED_EDGE ( 'NONE', *, *, #97685, .F. ) ;
#592=EDGE_CURVE ( 'NONE', #102339, #9659, #46179, .T. ) ;
#607=CARTESIAN_POINT ( 'NONE',  ( 0.000000000000000000, -6.928203230275511437, -3.999999999999997335 ) ) ;
#611=ORIENTED_EDGE ( 'NONE', *, *, #54631, .T. ) ;
#621=CARTESIAN_POINT ( 'NONE',  ( 87.62222222222222001, 4.172000000000019249, 0.000000000000000000 ) ) ;
#650=VECTOR ( 'NONE', #38589, 999.9999999999998863 ) ;
#669=ADVANCED_FACE ( 'NONE', ( #964 ), #72098, .T. ) ;
#721=ORIENTED_EDGE ( 'NONE', *, *, #58191, .T. ) ;
#780=DIRECTION ( 'NONE',  ( 0.5735764363510554853, 0.8191520442889852482, 0.000000000000000000 ) ) ;
#799=CIRCLE ( 'NONE', #38817, 5.000000000000010658 ) ;
#837=ORIENTED_EDGE ( 'NONE', *, *, #76816, .T. ) ;
#881=CIRCLE ( 'NONE', #32044, 5.000000000000010658 ) ;
#889=DIRECTION ( 'NONE',  ( 0.000000000000000000, -1.000000000000000000, 0.000000000000000000 ) ) ;
#921=FACE_OUTER_BOUND ( 'NONE', #71190, .T. ) ;
#924=ORIENTED_EDGE ( 'NONE', *, *, #39644, .F. ) ;
#948=CIRCLE ( 'NONE', #42338, 5.000000000000010658 ) ;
#961=DIRECTION ( 'NONE',  ( 0.000000000000000000, -1.000000000000000000, 0.000000000000000000 ) ) ;
#964=FACE_OUTER_BOUND ( 'NONE', #43504, .T. ) ;
#971=EDGE_LOOP ( 'NONE', ( #12898, #106488, #53796, #12965, #34148 ) ) ;
#1040=DIRECTION ( 'NONE',  ( -1.000000000000000000, -1.224606353822377258E-16, -0.000000000000000000 ) ) ;
#1092=EDGE_LOOP ( 'NONE', ( #12741, #98908, #96303, #87577, #9713 ) ) ;
#1101=CARTESIAN_POINT ( 'NONE',  ( 6.800000000000000711, 0.000000000000000000, -5.400000000000001243 ) ) ;
#1112=AXIS2_PLACEMENT_3D ( 'NONE', #11999, #77816, #58981 ) ;
#1119=CIRCLE ( 'NONE', #87324, 5.000000000000010658 ) ;
#1150=DIRECTION ( 'NONE',  ( 0.000000000000000000, -1.000000000000000000, 0.000000000000000000 ) ) ;
#1171=DIRECTION ( 'NONE',  ( -1.000000000000000000, -0.000000000000000000, -0.000000000000000000 ) ) ;
#1210=EDGE_CURVE ( 'NONE', #77725, #102376, #18713, .T. ) ;
#1218=EDGE_CURVE ( 'NONE', #87052, #73679, #22173, .T. ) ;
#1297=ORIENTED_EDGE ( 'NONE', *, *, #96152, .T. ) ;
#1310=VERTEX_POINT ( 'NONE', #61264 ) ;
#1328=DIRECTION ( 'NONE',  ( 0.000000000000000000, -1.000000000000000000, 0.000000000000000000 ) ) ;
#1372=CARTESIAN_POINT ( 'NONE',  ( -8.252218488625017898E-15, -6.732211846623387785, 4.339467034331188522 ) ) ;
#1422=AXIS2_PLACEMENT_3D ( 'NONE', #95336, #54307, #87253 ) ;
#1435=CARTESIAN_POINT ( 'NONE',  ( 101.4868948250290259, 1.016364837396684119E-14, 0.000000000000000000 ) ) ;
#1481=DIRECTION ( 'NONE',  ( 0.000000000000000000, 1.000000000000000000, 0.000000000000000000 ) ) ;
#1516=LINE ( 'NONE', #59261, #27205 ) ;
#1521=DIRECTION ( 'NONE',  ( -0.000000000000000000, 0.000000000000000000, -1.000000000000000000 ) ) ;
#1527=VERTEX_POINT ( 'NONE', #32493 ) ;
#1545=AXIS2_PLACEMENT_3D ( 'NONE', #26592, #28178, #18475 ) ;
#1553=ORIENTED_EDGE ( 'NONE', *, *, #58689, .T. ) ;
#1566=VERTEX_POINT ( 'NONE', #33544 ) ;
#1615=AXIS2_PLACEMENT_3D ( 'NONE', #32685, #33207, #100568 ) ;
#1645=CARTESIAN_POINT ( 'NONE',  ( 100.0424503805845831, 1.016364837396684119E-14, 0.000000000000000000 ) ) ;
#1697=DIRECTION ( 'NONE',  ( 0.000000000000000000, -1.000000000000000000, 0.000000000000000000 ) ) ;
#1700=CONICAL_SURFACE ( 'NONE', #53145, 5.000000000000010658, 0.9599310885968697082 ) ;
#1705=EDGE_CURVE ( 'NONE', #20613, #71082, #8712, .T. ) ;
#1707=EDGE_LOOP ( 'NONE', ( #12150, #104339, #21184, #103283, #98378 ) ) ;
#1731=CARTESIAN_POINT ( 'NONE',  ( 99.17777777777777715, 1.023464760207051730E-14, 0.000000000000000000 ) ) ;
#1767=FACE_OUTER_BOUND ( 'NONE', #16568, .T. ) ;
#1861=CIRCLE ( 'NONE', #29497, 5.000000000000010658 ) ;
#1868=CARTESIAN_POINT ( 'NONE',  ( 85.31310517497098544, 6.123233995736568081E-16, -5.000000000000011546 ) ) ;
#1881=TOROIDAL_SURFACE ( 'NONE', #63896, 5.400000000000001243, 0.4000000000000000222 ) ;
#1923=FACE_OUTER_BOUND ( 'NONE', #40395, .T. ) ;
#1927=DIRECTION ( 'NONE',  ( -0.5735764363510459374, -0.8191520442889919096, 0.000000000000000000 ) ) ;
#1934=VECTOR ( 'NONE', #1927, 1000.000000000000000 ) ;
#1953=DIRECTION ( 'NONE',  ( -1.000000000000000000, -1.224606353822377258E-16, -0.000000000000000000 ) ) ;
#1982=ORIENTED_EDGE ( 'NONE', *, *, #24892, .F. ) ;
#2020=FACE_OUTER_BOUND ( 'NONE', #77003, .T. ) ;
#2021=FACE_OUTER_BOUND ( 'NONE', #98289, .T. ) ;
#2050=ORIENTED_EDGE ( 'NONE', *, *, #6380, .F. ) ;
#2081=ORIENTED_EDGE ( 'NONE', *, *, #17235, .F. ) ;
#2102=EDGE_CURVE ( 'NONE', #102684, #1527, #89200, .T. ) ;
#2140=CIRCLE ( 'NONE', #65830, 5.000000000000010658 ) ;
#2170=CARTESIAN_POINT ( 'NONE',  ( 0.000000000000000000, 6.123233995736767268E-16, -5.000000000000000888 ) ) ;
#2182=DIRECTION ( 'NONE',  ( 0.000000000000000000, -1.000000000000000000, 0.000000000000000000 ) ) ;
#2200=CARTESIAN_POINT ( 'NONE',  ( 89.06666666666666288, -4.171999999999998820, 0.000000000000000000 ) ) ;
#2202=CARTESIAN_POINT ( 'NONE',  ( 102.6464385083043283, 1.030564683017419500E-14, 0.000000000000000000 ) ) ;
#2258=SURFACE_SIDE_STYLE ('',( #34149 ) ) ;
#2264=EDGE_CURVE ( 'NONE', #37220, #48016, #101302, .T. ) ;
#2287=VECTOR ( 'NONE', #3635, 1000.000000000000000 ) ;
#2317=ORIENTED_EDGE ( 'NONE', *, *, #6369, .T. ) ;
#2335=FACE_OUTER_BOUND ( 'NONE', #100459, .T. ) ;
#2365=EDGE_CURVE ( 'NONE', #24844, #100880, #18174, .T. ) ;
#2414=CARTESIAN_POINT ( 'NONE',  ( 81.84444444444444855, 1.023464760207051730E-14, 0.000000000000000000 ) ) ;
#2492=AXIS2_PLACEMENT_3D ( 'NONE', #100963, #1171, #51344 ) ;
#2497=AXIS2_PLACEMENT_3D ( 'NONE', #44193, #77081, #43125 ) ;
#2517=DIRECTION ( 'NONE',  ( -1.000000000000000000, -1.224606353822377258E-16, -0.000000000000000000 ) ) ;
#2519=AXIS2_PLACEMENT_3D ( 'NONE', #7380, #73712, #49436 ) ;
#2540=EDGE_LOOP ( 'NONE', ( #72395, #48934, #97791, #99475, #11796, #101917 ) ) ;
#2544=LINE ( 'NONE', #17682, #16266 ) ;
#2642=EDGE_CURVE ( 'NONE', #54959, #35138, #62880, .T. ) ;
#2683=AXIS2_PLACEMENT_3D ( 'NONE', #101203, #1953, #77463 ) ;
#2722=CARTESIAN_POINT ( 'NONE',  ( 0.08224679563971407092, 7.710515798486365036, 2.644994884459111351 ) ) ;
#2766=CARTESIAN_POINT ( 'NONE',  ( 91.95555555555554861, 1.023464760207051730E-14, 0.000000000000000000 ) ) ;
#2768=DIRECTION ( 'NONE',  ( -1.000000000000000000, -1.224606353822377258E-16, -0.000000000000000000 ) ) ;
#2820=ORIENTED_EDGE ( 'NONE', *, *, #74300, .F. ) ;
#2894=ORIENTED_EDGE ( 'NONE', *, *, #51724, .F. ) ;
#2924=CARTESIAN_POINT ( 'NONE',  ( 88.20199406385988539, -2.002967142162725287E-29, 5.000000000000011546 ) ) ;
#2927=ADVANCED_FACE ( 'NONE', ( #13638 ), #105319, .F. ) ;
#2928=ORIENTED_EDGE ( 'NONE', *, *, #73513, .F. ) ;
#2944=VERTEX_POINT ( 'NONE', #54614 ) ;
#2989=VECTOR ( 'NONE', #10092, 1000.000000000000000 ) ;
#3027=VERTEX_POINT ( 'NONE', #5040 ) ;
#3086=AXIS2_PLACEMENT_3D ( 'NONE', #26285, #59146, #92560 ) ;
#3096=DIRECTION ( 'NONE',  ( -1.000000000000000000, -0.000000000000000000, -0.000000000000000000 ) ) ;
#3134=EDGE_CURVE ( 'NONE', #60462, #54541, #14912, .T. ) ;
#3135=DIRECTION ( 'NONE',  ( -1.000000000000000000, -1.224606353822377258E-16, -0.000000000000000000 ) ) ;
#3143=DIRECTION ( 'NONE',  ( 0.000000000000000000, -1.000000000000000000, 0.000000000000000000 ) ) ;
#3149=FACE_OUTER_BOUND ( 'NONE', #71581, .T. ) ;
#3202=EDGE_CURVE ( 'NONE', #48016, #62320, #98709, .T. ) ;
#3208=VECTOR ( 'NONE', #49503, 1000.000000000000000 ) ;
#3212=EDGE_CURVE ( 'NONE', #90932, #42388, #39046, .T. ) ;
#3239=DIRECTION ( 'NONE',  ( 0.000000000000000000, 0.000000000000000000, 1.000000000000000000 ) ) ;
#3243=ADVANCED_FACE ( 'NONE', ( #51852 ), #97601, .T. ) ;
#3244=CARTESIAN_POINT ( 'NONE',  ( 101.2019940638598854, -5.000000000000000888, 6.123233995736779101E-16 ) ) ;
#3264=DIRECTION ( 'NONE',  ( -1.000000000000000000, -1.224606353822377258E-16, -0.000000000000000000 ) ) ;
#3284=ORIENTED_EDGE ( 'NONE', *, *, #105138, .F. ) ;
#3341=EDGE_CURVE ( 'NONE', #52131, #63286, #42708, .T. ) ;
#3388=AXIS2_PLACEMENT_3D ( 'NONE', #84982, #84452, #58027 ) ;
#3401=VERTEX_POINT ( 'NONE', #31723 ) ;
#3422=AXIS2_PLACEMENT_3D ( 'NONE', #41883, #10053, #57522 ) ;
#3436=DIRECTION ( 'NONE',  ( 0.000000000000000000, -1.000000000000000000, 0.000000000000000000 ) ) ;
#3439=FACE_OUTER_BOUND ( 'NONE', #106693, .T. ) ;
#3462=CARTESIAN_POINT ( 'NONE',  ( 98.31310517497099966, 1.030564683017419500E-14, 0.000000000000000000 ) ) ;
#3526=EDGE_LOOP ( 'NONE', ( #73658, #49880, #3793, #83430, #80989 ) ) ;
#3571=DIRECTION ( 'NONE',  ( 0.000000000000000000, 1.000000000000000000, 0.000000000000000000 ) ) ;
#3607=DIRECTION ( 'NONE',  ( 0.000000000000000000, -1.000000000000000000, 0.000000000000000000 ) ) ;
#3634=EDGE_CURVE ( 'NONE', #58039, #38733, #99365, .T. ) ;
#3635=DIRECTION ( 'NONE',  ( 0.5735764363510557073, -0.8191520442889850262, 1.003171929053516612E-16 ) ) ;
#3660=DIRECTION ( 'NONE',  ( 0.000000000000000000, -1.000000000000000000, 0.000000000000000000 ) ) ;
#3712=ORIENTED_EDGE ( 'NONE', *, *, #88764, .F. ) ;
#3734=ORIENTED_EDGE ( 'NONE', *, *, #83507, .F. ) ;
#3737=DIRECTION ( 'NONE',  ( -1.000000000000000000, -0.000000000000000000, -0.000000000000000000 ) ) ;
#3749=ORIENTED_EDGE ( 'NONE', *, *, #105871, .F. ) ;
#3788=FACE_OUTER_BOUND ( 'NONE', #87584, .T. ) ;
#3792=DIRECTION ( 'NONE',  ( 0.000000000000000000, -1.000000000000000000, 0.000000000000000000 ) ) ;
#3793=ORIENTED_EDGE ( 'NONE', *, *, #85701, .T. ) ;
#3851=VECTOR ( 'NONE', #53716, 1000.000000000000000 ) ;
#3874=VECTOR ( 'NONE', #73356, 1000.000000000000000 ) ;
#3899=DIRECTION ( 'NONE',  ( 0.000000000000000000, -1.000000000000000000, 0.000000000000000000 ) ) ;
#3901=VERTEX_POINT ( 'NONE', #4311 ) ;
#3918=ORIENTED_EDGE ( 'NONE', *, *, #93636, .T. ) ;
#3956=ORIENTED_EDGE ( 'NONE', *, *, #7199, .F. ) ;
#3994=CARTESIAN_POINT ( 'NONE',  ( 105.5353273971932140, 5.000000000000020428, 0.000000000000000000 ) ) ;
#4036=DIRECTION ( 'NONE',  ( -1.000000000000000000, -1.224606353822377258E-16, -0.000000000000000000 ) ) ;
#4076=EDGE_CURVE ( 'NONE', #95902, #48016, #103017, .T. ) ;
#4145=DIRECTION ( 'NONE',  ( 0.000000000000000000, -1.000000000000000000, 0.000000000000000000 ) ) ;
#4187=CARTESIAN_POINT ( 'NONE',  ( 0.000000000000000000, 0.000000000000000000, 5.000000000000000888 ) ) ;
#4212=ORIENTED_EDGE ( 'NONE', *, *, #48194, .F. ) ;
#4222=DIRECTION ( 'NONE',  ( 0.000000000000000000, -1.000000000000000000, 0.000000000000000000 ) ) ;
#4234=VERTEX_POINT ( 'NONE', #33928 ) ;
#4294=CARTESIAN_POINT ( 'NONE',  ( 87.04245038058458306, -2.002967142162725287E-29, 5.000000000000011546 ) ) ;
#4311=CARTESIAN_POINT ( 'NONE',  ( 91.37578371391791165, -2.002967142162725287E-29, 5.000000000000011546 ) ) ;
#4313=ORIENTED_EDGE ( 'NONE', *, *, #49773, .T. ) ;
#4374=DIRECTION ( 'NONE',  ( -1.000000000000000000, -1.224606353822377258E-16, -0.000000000000000000 ) ) ;
#4400=CONICAL_SURFACE ( 'NONE', #106005, 4.172000000000009479, 0.9599310885968813656 ) ;
#4493=CARTESIAN_POINT ( 'NONE',  ( 0.000000000000000000, 6.928203230275505220, 4.000000000000006217 ) ) ;
#4499=EDGE_LOOP ( 'NONE', ( #52468, #26034, #25246, #97272, #36737, #95599 ) ) ;
#4508=VERTEX_POINT ( 'NONE', #78592 ) ;
#4512=DIRECTION ( 'NONE',  ( 0.000000000000000000, 0.000000000000000000, 1.000000000000000000 ) ) ;
#4530=ORIENTED_EDGE ( 'NONE', *, *, #27446, .T. ) ;
#4539=VECTOR ( 'NONE', #47731, 1000.000000000000000 ) ;
#4552=EDGE_CURVE ( 'NONE', #54541, #65774, #78072, .T. ) ;
#4559=ORIENTED_EDGE ( 'NONE', *, *, #4076, .F. ) ;
#4590=EDGE_CURVE ( 'NONE', #10855, #92963, #1119, .T. ) ;
#4620=AXIS2_PLACEMENT_3D ( 'NONE', #35109, #52851, #59368 ) ;
#4634=EDGE_CURVE ( 'NONE', #36922, #17355, #81761, .T. ) ;
#4657=VERTEX_POINT ( 'NONE', #7882 ) ;
#4721=FACE_OUTER_BOUND ( 'NONE', #15881, .T. ) ;
#4761=ORIENTED_EDGE ( 'NONE', *, *, #19686, .T. ) ;
#4798=ORIENTED_EDGE ( 'NONE', *, *, #90647, .F. ) ;
#4811=VECTOR ( 'NONE', #95693, 999.9999999999998863 ) ;
#4821=VECTOR ( 'NONE', #103032, 1000.000000000000000 ) ;
#4889=CARTESIAN_POINT ( 'NONE',  ( 86.75754961941542831, 1.030564683017419500E-14, 0.000000000000000000 ) ) ;
#4961=CARTESIAN_POINT ( 'NONE',  ( 5.799999999999999822, 6.928203230275505220, 4.000000000000007105 ) ) ;
#4962=ORIENTED_EDGE ( 'NONE', *, *, #104465, .T. ) ;
#5012=CARTESIAN_POINT ( 'NONE',  ( 0.000000000000000000, 0.000000000000000000, 0.000000000000000000 ) ) ;
#5040=CARTESIAN_POINT ( 'NONE',  ( 99.75754961941544252, -5.000000000000000888, 6.123233995736779101E-16 ) ) ;
#5045=EDGE_LOOP ( 'NONE', ( #83539, #59778, #53353, #38426, #49318 ) ) ;
#5169=EDGE_CURVE ( 'NONE', #63754, #64539, #14768, .T. ) ;
#5172=CARTESIAN_POINT ( 'NONE',  ( 80.40000000000000568, 1.023464760207051730E-14, 0.000000000000000000 ) ) ;
#5202=ORIENTED_EDGE ( 'NONE', *, *, #48044, .F. ) ;
#5212=AXIS2_PLACEMENT_3D ( 'NONE', #12655, #13718, #80043 ) ;
#5226=EDGE_CURVE ( 'NONE', #54541, #6367, #37223, .T. ) ;
#5234=DIRECTION ( 'NONE',  ( -1.000000000000000000, -0.000000000000000000, -0.000000000000000000 ) ) ;
#5284=CARTESIAN_POINT ( 'NONE',  ( 81.26467260280679739, 1.016364837396684119E-14, 0.000000000000000000 ) ) ;
#5285=EDGE_CURVE ( 'NONE', #69907, #74576, #12534, .T. ) ;
#5337=EDGE_CURVE ( 'NONE', #16556, #11414, #73431, .T. ) ;
#5339=ORIENTED_EDGE ( 'NONE', *, *, #14456, .T. ) ;
#5366=DIRECTION ( 'NONE',  ( -1.000000000000000000, -1.224606353822377258E-16, -0.000000000000000000 ) ) ;
#5385=ORIENTED_EDGE ( 'NONE', *, *, #29003, .F. ) ;
#5386=ORIENTED_EDGE ( 'NONE', *, *, #75544, .T. ) ;
#5404=ORIENTED_EDGE ( 'NONE', *, *, #78889, .T. ) ;
#5422=DIRECTION ( 'NONE',  ( 1.000000000000000000, 1.224606353822377258E-16, 0.000000000000000000 ) ) ;
#5449=CARTESIAN_POINT ( 'NONE',  ( 91.95555555555554861, -4.171999999999998820, 5.616230220889773285E-16 ) ) ;
#5465=DIRECTION ( 'NONE',  ( -1.000000000000000000, -0.000000000000000000, -0.000000000000000000 ) ) ;
#5486=LINE ( 'NONE', #61626, #36046 ) ;
#5535=EDGE_CURVE ( 'NONE', #76580, #64598, #102716, .T. ) ;
#5546=VERTEX_POINT ( 'NONE', #95543 ) ;
#5612=DIRECTION ( 'NONE',  ( 0.000000000000000000, -1.000000000000000000, 0.000000000000000000 ) ) ;
#5624=DIRECTION ( 'NONE',  ( 0.000000000000000000, -1.000000000000000000, 0.000000000000000000 ) ) ;
#5628=AXIS2_PLACEMENT_3D ( 'NONE', #94228, #93697, #44082 ) ;
#5684=CARTESIAN_POINT ( 'NONE',  ( 89.64643850830432825, 5.000000000000021316, 0.000000000000000000 ) ) ;
#5696=DIRECTION ( 'NONE',  ( 0.000000000000000000, -1.000000000000000000, 0.000000000000000000 ) ) ;
#5735=EDGE_CURVE ( 'NONE', #13365, #65096, #6511, .T. ) ;
#5803=CARTESIAN_POINT ( 'NONE',  ( 89.64643850830432825, 1.030564683017419500E-14, 0.000000000000000000 ) ) ;
#5804=CARTESIAN_POINT ( 'NONE',  ( 0.4973051450610682656, -3.866309095671417673, -8.000000000000001776 ) ) ;
#5810=AXIS2_PLACEMENT_3D ( 'NONE', #81964, #40996, #97103 ) ;
#5836=CARTESIAN_POINT ( 'NONE',  ( 102.0666666666666629, 1.023464760207051730E-14, 0.000000000000000000 ) ) ;
#5844=EDGE_LOOP ( 'NONE', ( #27007, #45834, #60404, #73727, #86197, #31275 ) ) ;
#5911=AXIS2_PLACEMENT_3D ( 'NONE', #38852, #41887, #96552 ) ;
#5960=FACE_OUTER_BOUND ( 'NONE', #96945, .T. ) ;
#6102=VERTEX_POINT ( 'NONE', #17690 ) ;
#6139=DIRECTION ( 'NONE',  ( -1.000000000000000000, -1.224606353822377258E-16, -0.000000000000000000 ) ) ;
#6143=VECTOR ( 'NONE', #26634, 1000.000000000000000 ) ;
#6154=DIRECTION ( 'NONE',  ( -1.000000000000000000, -1.224606353822377258E-16, -0.000000000000000000 ) ) ;
#6181=EDGE_CURVE ( 'NONE', #15530, #17909, #67827, .T. ) ;
#6196=EDGE_LOOP ( 'NONE', ( #92985, #66074, #93610, #77410, #27761 ) ) ;
#6224=LINE ( 'NONE', #14315, #106123 ) ;
#6252=DIRECTION ( 'NONE',  ( -1.000000000000000000, -0.000000000000000000, -0.000000000000000000 ) ) ;
#6282=ORIENTED_EDGE ( 'NONE', *, *, #59716, .F. ) ;
#6347=DIRECTION ( 'NONE',  ( -1.000000000000000000, -0.000000000000000000, -0.000000000000000000 ) ) ;
#6360=CIRCLE ( 'NONE', #88995, 5.000000000000011546 ) ;
#6367=VERTEX_POINT ( 'NONE', #54258 ) ;
#6369=EDGE_CURVE ( 'NONE', #15045, #10855, #82618, .T. ) ;
#6380=EDGE_CURVE ( 'NONE', #1527, #105973, #25846, .T. ) ;
#6415=EDGE_CURVE ( 'NONE', #43584, #46987, #40216, .T. ) ;
#6457=EDGE_CURVE ( 'NONE', #76468, #104209, #90363, .T. ) ;
#6511=LINE ( 'NONE', #32424, #44125 ) ;
#6541=EDGE_CURVE ( 'NONE', #39221, #82852, #36946, .T. ) ;
#6561=ORIENTED_EDGE ( 'NONE', *, *, #81919, .T. ) ;
#6570=AXIS2_PLACEMENT_3D ( 'NONE', #93961, #20111, #44888 ) ;
#6637=ORIENTED_EDGE ( 'NONE', *, *, #48835, .F. ) ;
#6657=CIRCLE ( 'NONE', #61829, 5.000000000000011546 ) ;
#6667=DIRECTION ( 'NONE',  ( 0.000000000000000000, -1.000000000000000000, 0.000000000000000000 ) ) ;
#6669=VERTEX_POINT ( 'NONE', #1868 ) ;
#6695=DIRECTION ( 'NONE',  ( -0.000000000000000000, 1.000000000000000000, 1.877893248421449282E-16 ) ) ;
#6713=DIRECTION ( 'NONE',  ( -1.000000000000000000, -1.224606353822377258E-16, -0.000000000000000000 ) ) ;
#6740=AXIS2_PLACEMENT_3D ( 'NONE', #13022, #85899, #3899 ) ;
#6747=DIRECTION ( 'NONE',  ( -1.000000000000000000, -0.000000000000000000, -0.000000000000000000 ) ) ;
#6748=ORIENTED_EDGE ( 'NONE', *, *, #1705, .T. ) ;
#6751=ORIENTED_EDGE ( 'NONE', *, *, #18659, .T. ) ;
#6758=AXIS2_PLACEMENT_3D ( 'NONE', #98048, #6909, #16602 ) ;
#6759=DIRECTION ( 'NONE',  ( 1.000000000000000000, 1.224606353822377258E-16, 0.000000000000000000 ) ) ;
#6761=VERTEX_POINT ( 'NONE', #43418 ) ;
#6779=CIRCLE ( 'NONE', #48111, 5.000000000000011546 ) ;
#6795=DIRECTION ( 'NONE',  ( 0.000000000000000000, -1.000000000000000000, 0.000000000000000000 ) ) ;
#6830=ORIENTED_EDGE ( 'NONE', *, *, #100436, .T. ) ;
#6890=CONICAL_SURFACE ( 'NONE', #5212, 4.172000000000009479, 0.9599310885968813656 ) ;
#6909=DIRECTION ( 'NONE',  ( -1.000000000000000000, -0.000000000000000000, -0.000000000000000000 ) ) ;
#7038=CARTESIAN_POINT ( 'NONE',  ( 105.5353273971932140, 1.030564683017419500E-14, 0.000000000000000000 ) ) ;
#7085=AXIS2_PLACEMENT_3D ( 'NONE', #82101, #56759, #31993 ) ;
#7098=CARTESIAN_POINT ( 'NONE',  ( 0.3167204509598381956, 8.479269695850865318, -1.313474075707212974 ) ) ;
#7106=CARTESIAN_POINT ( 'NONE',  ( 83.28888888888889142, -4.171999999999998820, 5.616230220889773285E-16 ) ) ;
#7199=EDGE_CURVE ( 'NONE', #4657, #54111, #64949, .T. ) ;
#7207=ADVANCED_FACE ( 'NONE', ( #2020 ), #34968, .T. ) ;
#7213=EDGE_CURVE ( 'NONE', #64079, #21657, #9046, .T. ) ;
#7219=DIRECTION ( 'NONE',  ( -1.000000000000000000, -0.000000000000000000, -0.000000000000000000 ) ) ;
#7223=DIRECTION ( 'NONE',  ( -1.000000000000000000, -1.224606353822377258E-16, -0.000000000000000000 ) ) ;
#7241=CARTESIAN_POINT ( 'NONE',  ( 0.000000000000000000, 0.000000000000000000, 0.000000000000000000 ) ) ;
#7250=ORIENTED_EDGE ( 'NONE', *, *, #6181, .T. ) ;
#7267=CIRCLE ( 'NONE', #29728, 5.000000000000011546 ) ;
#7268=ORIENTED_EDGE ( 'NONE', *, *, #105739, .T. ) ;
#7283=ORIENTED_EDGE ( 'NONE', *, *, #96603, .F. ) ;
#7337=ADVANCED_BREP_SHAPE_REPRESENTATION ( '', ( #90947, #10728 ), #79871 ) ;
#7353=DIRECTION ( 'NONE',  ( -1.000000000000000000, -0.000000000000000000, -0.000000000000000000 ) ) ;
#7368=CARTESIAN_POINT ( 'NONE',  ( 85.59800593614014019, -2.002967142162725287E-29, 5.000000000000011546 ) ) ;
#7379=AXIS2_PLACEMENT_3D ( 'NONE', #26405, #93223, #10165 ) ;
#7380=CARTESIAN_POINT ( 'NONE',  ( 98.59800593614012598, 1.016364837396684119E-14, 0.000000000000000000 ) ) ;
#7402=ORIENTED_EDGE ( 'NONE', *, *, #105076, .F. ) ;
#7456=DIRECTION ( 'NONE',  ( 0.000000000000000000, -1.000000000000000000, 0.000000000000000000 ) ) ;
#7495=EDGE_LOOP ( 'NONE', ( #90806, #83704, #75712, #49989, #34012 ) ) ;
#7508=EDGE_CURVE ( 'NONE', #104209, #8019, #8204, .T. ) ;
#7564=CIRCLE ( 'NONE', #66171, 4.172000000000009479 ) ;
#7578=DIRECTION ( 'NONE',  ( -1.000000000000000000, -1.224606353822377258E-16, -0.000000000000000000 ) ) ;
#7588=CARTESIAN_POINT ( 'NONE',  ( 0.000000000000000000, 0.000000000000000000, 0.000000000000000000 ) ) ;
#7602=ORIENTED_EDGE ( 'NONE', *, *, #98176, .F. ) ;
#7622=LINE ( 'NONE', #98762, #82157 ) ;
#7663=ORIENTED_EDGE ( 'NONE', *, *, #24892, .T. ) ;
#7664=EDGE_CURVE ( 'NONE', #37699, #89169, #86353, .T. ) ;
#7675=ADVANCED_FACE ( 'NONE', ( #21841 ), #54683, .F. ) ;
#7682=DIRECTION ( 'NONE',  ( 0.000000000000000000, 1.000000000000000000, 0.000000000000000000 ) ) ;
#7783=CARTESIAN_POINT ( 'NONE',  ( 0.7145311798163219708, 4.618802153517003184, -8.000000000000000000 ) ) ;
#7841=VERTEX_POINT ( 'NONE', #44910 ) ;
#7864=AXIS2_PLACEMENT_3D ( 'NONE', #30488, #6713, #96800 ) ;
#7874=EDGE_CURVE ( 'NONE', #102684, #5546, #12505, .T. ) ;
#7877=FACE_OUTER_BOUND ( 'NONE', #63942, .T. ) ;
#7882=CARTESIAN_POINT ( 'NONE',  ( 91.37578371391791165, 6.123233995736582872E-16, -5.000000000000011546 ) ) ;
#7892=CARTESIAN_POINT ( 'NONE',  ( 93.97977184163765685, 1.030564683017419500E-14, 0.000000000000000000 ) ) ;
#7899=CARTESIAN_POINT ( 'NONE',  ( 95.42421628608209971, 1.030564683017419500E-14, 0.000000000000000000 ) ) ;
#7908=AXIS2_PLACEMENT_3D ( 'NONE', #102885, #19887, #103410 ) ;
#7913=DIRECTION ( 'NONE',  ( -1.000000000000000000, -1.224606353822377258E-16, -0.000000000000000000 ) ) ;
#7935=EDGE_CURVE ( 'NONE', #6102, #87544, #15693, .T. ) ;
#7947=ADVANCED_FACE ( 'NONE', ( #58281 ), #8131, .T. ) ;
#7953=VERTEX_POINT ( 'NONE', #73924 ) ;
#7967=ORIENTED_EDGE ( 'NONE', *, *, #25364, .T. ) ;
#7984=AXIS2_PLACEMENT_3D ( 'NONE', #38624, #6759, #24046 ) ;
#7998=CARTESIAN_POINT ( 'NONE',  ( 0.000000000000000000, 6.123233995736767268E-16, -5.000000000000000888 ) ) ;
#8019=VERTEX_POINT ( 'NONE', #39986 ) ;
#8073=CIRCLE ( 'NONE', #9832, 5.000000000000011546 ) ;
#8089=FACE_OUTER_BOUND ( 'NONE', #48617, .T. ) ;
#8114=EDGE_LOOP ( 'NONE', ( #70024, #74343, #13491, #10170, #36410 ) ) ;
#8131=CYLINDRICAL_SURFACE ( 'NONE', #22679, 5.000000000000000888 ) ;
#8154=ORIENTED_EDGE ( 'NONE', *, *, #11882, .T. ) ;
#8168=ORIENTED_EDGE ( 'NONE', *, *, #48102, .T. ) ;
#8191=DIRECTION ( 'NONE',  ( 0.000000000000000000, -1.000000000000000000, 0.000000000000000000 ) ) ;
#8204=CIRCLE ( 'NONE', #37507, 5.000000000000011546 ) ;
#8226=CARTESIAN_POINT ( 'NONE',  ( 83.86866073052654258, 1.030564683017419500E-14, 0.000000000000000000 ) ) ;
#8253=CARTESIAN_POINT ( 'NONE',  ( 104.0908829527487711, 5.000000000000021316, 0.000000000000000000 ) ) ;
#8280=DIRECTION ( 'NONE',  ( 0.000000000000000000, -1.000000000000000000, 0.000000000000000000 ) ) ;
#8306=CARTESIAN_POINT ( 'NONE',  ( 99.17777777777777715, -4.171999999999998820, 0.000000000000000000 ) ) ;
#8313=DIRECTION ( 'NONE',  ( 0.000000000000000000, -1.000000000000000000, 0.000000000000000000 ) ) ;
#8336=LINE ( 'NONE', #59033, #78038 ) ;
#8338=AXIS2_PLACEMENT_3D ( 'NONE', #12377, #93844, #27561 ) ;
#8390=CIRCLE ( 'NONE', #79151, 5.000000000000011546 ) ;
#8397=VECTOR ( 'NONE', #25453, 999.9999999999998863 ) ;
#8528=DIRECTION ( 'NONE',  ( 0.000000000000000000, -1.000000000000000000, 0.000000000000000000 ) ) ;
#8535=EDGE_CURVE ( 'NONE', #76618, #35844, #25444, .T. ) ;
#8546=AXIS2_PLACEMENT_3D ( 'NONE', #2202, #68020, #33546 ) ;
#8585=CARTESIAN_POINT ( 'NONE',  ( 104.9555555555555486, 1.023464760207051730E-14, 0.000000000000000000 ) ) ;
#8641=DIRECTION ( 'NONE',  ( 0.5735764363510554853, 0.8191520442889852482, 0.000000000000000000 ) ) ;
#8680=ORIENTED_EDGE ( 'NONE', *, *, #5337, .T. ) ;
#8698=ORIENTED_EDGE ( 'NONE', *, *, #86060, .F. ) ;
#8712=LINE ( 'NONE', #68018, #20269 ) ;
#8728=CARTESIAN_POINT ( 'NONE',  ( 89.93133926947346879, 1.016364837396684119E-14, 0.000000000000000000 ) ) ;
#8738=DIRECTION ( 'NONE',  ( -1.000000000000000000, -1.224606353822377258E-16, -0.000000000000000000 ) ) ;
#8750=AXIS2_PLACEMENT_3D ( 'NONE', #20177, #68144, #51947 ) ;
#8770=( NAMED_UNIT ( * ) PLANE_ANGLE_UNIT ( ) SI_UNIT ( $, .RADIAN. ) );
#8781=EDGE_LOOP ( 'NONE', ( #45126, #62112, #91018, #29371, #103413 ) ) ;
#8820=LINE ( 'NONE', #83765, #18737 ) ;
#8868=EDGE_LOOP ( 'NONE', ( #19880, #87937, #5202, #95447, #13761 ) ) ;
#8962=DIRECTION ( 'NONE',  ( -1.000000000000000000, -1.224606353822377258E-16, -0.000000000000000000 ) ) ;
#8974=VERTEX_POINT ( 'NONE', #57518 ) ;
#8995=ORIENTED_EDGE ( 'NONE', *, *, #86330, .T. ) ;
#9027=DIRECTION ( 'NONE',  ( -1.000000000000000000, -1.224606353822377258E-16, -0.000000000000000000 ) ) ;
#9030=ADVANCED_FACE ( 'NONE', ( #93099 ), #19272, .T. ) ;
#9046=LINE ( 'NONE', #41952, #70107 ) ;
#9048=CARTESIAN_POINT ( 'NONE',  ( 101.2019940638598854, -5.000000000000000000, 6.123233995736778115E-16 ) ) ;
#9076=ORIENTED_EDGE ( 'NONE', *, *, #34757, .F. ) ;
#9078=ORIENTED_EDGE ( 'NONE', *, *, #61209, .T. ) ;
#9153=CARTESIAN_POINT ( 'NONE',  ( 93.39999999999999147, -4.171999999999998820, 0.000000000000000000 ) ) ;
#9175=STYLED_ITEM ( 'NONE', ( #100970 ), #7337 ) ;
#9177=VECTOR ( 'NONE', #780, 1000.000000000000000 ) ;
#9184=EDGE_CURVE ( 'NONE', #231, #101774, #25116, .T. ) ;
#9203=VERTEX_POINT ( 'NONE', #7783 ) ;
#9223=CIRCLE ( 'NONE', #21370, 5.000000000000010658 ) ;
#9233=DIRECTION ( 'NONE',  ( -0.5735764363510459374, -0.8191520442889919096, 0.000000000000000000 ) ) ;
#9245=DIRECTION ( 'NONE',  ( 0.000000000000000000, 0.000000000000000000, 1.000000000000000000 ) ) ;
#9283=ORIENTED_EDGE ( 'NONE', *, *, #1210, .T. ) ;
#9348=CARTESIAN_POINT ( 'NONE',  ( 80.40000000000000568, 1.023464760207051730E-14, 0.000000000000000000 ) ) ;
#9359=EDGE_LOOP ( 'NONE', ( #15153, #33270, #6637, #13882, #35722 ) ) ;
#9363=VERTEX_POINT ( 'NONE', #4493 ) ;
#9366=VERTEX_POINT ( 'NONE', #70296 ) ;
#9367=DIRECTION ( 'NONE',  ( 0.000000000000000000, -1.000000000000000000, 0.000000000000000000 ) ) ;
#9378=AXIS2_PLACEMENT_3D ( 'NONE', #101982, #61018, #76641 ) ;
#9396=VERTEX_POINT ( 'NONE', #35836 ) ;
#9425=DIRECTION ( 'NONE',  ( 0.000000000000000000, -1.000000000000000000, 0.000000000000000000 ) ) ;
#9448=VECTOR ( 'NONE', #38726, 1000.000000000000000 ) ;
#9454=CARTESIAN_POINT ( 'NONE',  ( 84.73333333333332007, -4.171999999999998820, 5.616230220889773285E-16 ) ) ;
#9459=EDGE_CURVE ( 'NONE', #22473, #92048, #14682, .T. ) ;
#9460=ORIENTED_EDGE ( 'NONE', *, *, #101734, .T. ) ;
#9492=EDGE_CURVE ( 'NONE', #4508, #74667, #99318, .T. ) ;
#9497=DIRECTION ( 'NONE',  ( 0.000000000000000000, 1.000000000000000000, 0.000000000000000000 ) ) ;
#9505=EDGE_LOOP ( 'NONE', ( #106211, #96691, #95778, #4962, #32234 ) ) ;
#9506=DIRECTION ( 'NONE',  ( 1.000000000000000000, 1.224606353822377258E-16, 0.000000000000000000 ) ) ;
#9544=DIRECTION ( 'NONE',  ( 0.000000000000000000, 0.000000000000000000, -1.000000000000000000 ) ) ;
#9576=DIRECTION ( 'NONE',  ( 1.000000000000000000, 1.224606353822377258E-16, 0.000000000000000000 ) ) ;
#9614=CIRCLE ( 'NONE', #38986, 8.000000000000000000 ) ;
#9639=PLANE ( 'NONE',  #31218 ) ;
#9659=VERTEX_POINT ( 'NONE', #10836 ) ;
#9688=VECTOR ( 'NONE', #79237, 1000.000000000000000 ) ;
#9713=ORIENTED_EDGE ( 'NONE', *, *, #19686, .F. ) ;
#9714=DIRECTION ( 'NONE',  ( -1.000000000000000000, -1.224606353822377258E-16, -0.000000000000000000 ) ) ;
#9728=VERTEX_POINT ( 'NONE', #74790 ) ;
#9739=DIRECTION ( 'NONE',  ( 0.000000000000000000, 0.000000000000000000, -1.000000000000000000 ) ) ;
#9753=CIRCLE ( 'NONE', #92371, 5.000000000000011546 ) ;
#9767=DIRECTION ( 'NONE',  ( -1.000000000000000000, -1.224606353822377258E-16, -0.000000000000000000 ) ) ;
#9783=DIRECTION ( 'NONE',  ( 0.000000000000000000, 0.000000000000000000, 1.000000000000000000 ) ) ;
#9798=CARTESIAN_POINT ( 'NONE',  ( 0.000000000000000000, 0.000000000000000000, 0.000000000000000000 ) ) ;
#9810=DIRECTION ( 'NONE',  ( 0.000000000000000000, -1.000000000000000000, 0.000000000000000000 ) ) ;
#9828=DIRECTION ( 'NONE',  ( -1.000000000000000000, -1.224606353822377258E-16, -0.000000000000000000 ) ) ;
#9832=AXIS2_PLACEMENT_3D ( 'NONE', #60340, #50087, #35007 ) ;
#9854=CARTESIAN_POINT ( 'NONE',  ( 0.000000000000000000, 0.000000000000000000, 0.000000000000000000 ) ) ;
#9861=VERTEX_POINT ( 'NONE', #23626 ) ;
#9886=CARTESIAN_POINT ( 'NONE',  ( 98.31310517497099966, 1.030564683017419500E-14, 0.000000000000000000 ) ) ;
#9919=CARTESIAN_POINT ( 'NONE',  ( 0.000000000000000000, 0.000000000000000000, 0.000000000000000000 ) ) ;
#9929=AXIS2_PLACEMENT_3D ( 'NONE', #67041, #78827, #11971 ) ;
#9970=FILL_AREA_STYLE_COLOUR ( '', #106677 ) ;
#9979=CARTESIAN_POINT ( 'NONE',  ( 6.400000000000000355, 6.613092715395708453E-16, 5.400000000000001243 ) ) ;
#9994=VECTOR ( 'NONE', #44058, 1000.000000000000000 ) ;
#10036=CARTESIAN_POINT ( 'NONE',  ( 96.28888888888889142, 1.023464760207051730E-14, 0.000000000000000000 ) ) ;
#10053=DIRECTION ( 'NONE',  ( -1.000000000000000000, -1.224606353822377258E-16, -0.000000000000000000 ) ) ;
#10056=AXIS2_PLACEMENT_3D ( 'NONE', #17819, #51212, #34022 ) ;
#10079=CARTESIAN_POINT ( 'NONE',  ( 0.000000000000000000, 0.000000000000000000, 5.000000000000000888 ) ) ;
#10086=CARTESIAN_POINT ( 'NONE',  ( 95.42421628608209971, 5.000000000000020428, 0.000000000000000000 ) ) ;
#10092=DIRECTION ( 'NONE',  ( -1.000000000000000000, -0.000000000000000000, -0.000000000000000000 ) ) ;
#10111=CIRCLE ( 'NONE', #63573, 5.000000000000010658 ) ;
#10116=DIRECTION ( 'NONE',  ( 0.000000000000000000, 1.000000000000000000, 0.000000000000000000 ) ) ;
#10124=AXIS2_PLACEMENT_3D ( 'NONE', #48179, #23417, #66494 ) ;
#10125=EDGE_CURVE ( 'NONE', #73679, #69327, #61839, .T. ) ;
#10150=EDGE_CURVE ( 'NONE', #55214, #85106, #96321, .T. ) ;
#10153=VERTEX_POINT ( 'NONE', #70444 ) ;
#10154=CARTESIAN_POINT ( 'NONE',  ( 83.28888888888889142, 4.172000000000019249, 0.000000000000000000 ) ) ;
#10165=DIRECTION ( 'NONE',  ( 0.000000000000000000, 1.000000000000000000, 0.000000000000000000 ) ) ;
#10170=ORIENTED_EDGE ( 'NONE', *, *, #30121, .F. ) ;
#10173=CARTESIAN_POINT ( 'NONE',  ( 5.799999999999999822, 9.237604307034018802, 0.000000000000000000 ) ) ;
#10202=ORIENTED_EDGE ( 'NONE', *, *, #48668, .F. ) ;
#10219=ORIENTED_EDGE ( 'NONE', *, *, #46903, .T. ) ;
#10221=DIRECTION ( 'NONE',  ( 0.000000000000000000, -1.000000000000000000, 0.000000000000000000 ) ) ;
#10239=AXIS2_PLACEMENT_3D ( 'NONE', #11959, #54004, #44891 ) ;
#10250=CARTESIAN_POINT ( 'NONE',  ( 98.31310517497099966, 5.000000000000021316, 0.000000000000000000 ) ) ;
#10260=FACE_OUTER_BOUND ( 'NONE', #31615, .T. ) ;
#10289=ORIENTED_EDGE ( 'NONE', *, *, #78304, .T. ) ;
#10325=DIRECTION ( 'NONE',  ( 0.000000000000000000, -1.000000000000000000, 0.000000000000000000 ) ) ;
#10327=CONICAL_SURFACE ( 'NONE', #103356, 5.000000000000010658, 0.9599310885968697082 ) ;
#10334=VERTEX_POINT ( 'NONE', #60122 ) ;
#10337=DIRECTION ( 'NONE',  ( -0.5735764363510459374, -0.8191520442889919096, 0.000000000000000000 ) ) ;
#10342=AXIS2_PLACEMENT_3D ( 'NONE', #42676, #75575, #101454 ) ;
#10423=ORIENTED_EDGE ( 'NONE', *, *, #106259, .F. ) ;
#10443=AXIS2_PLACEMENT_3D ( 'NONE', #65125, #40846, #24175 ) ;
#10447=CARTESIAN_POINT ( 'NONE',  ( 97.73333333333333428, 1.023464760207051730E-14, 0.000000000000000000 ) ) ;
#10479=AXIS2_PLACEMENT_3D ( 'NONE', #90611, #82516, #16720 ) ;
#10524=ORIENTED_EDGE ( 'NONE', *, *, #68209, .F. ) ;
#10577=DIRECTION ( 'NONE',  ( -1.000000000000000000, -0.000000000000000000, -0.000000000000000000 ) ) ;
#10611=DIRECTION ( 'NONE',  ( 1.000000000000000000, 0.000000000000000000, -0.000000000000000000 ) ) ;
#10633=DIRECTION ( 'NONE',  ( -0.5735764363510461594, 0.8191520442889916875, 1.003171929053524870E-16 ) ) ;
#10637=LINE ( 'NONE', #84011, #2287 ) ;
#10644=VERTEX_POINT ( 'NONE', #23370 ) ;
#10667=ORIENTED_EDGE ( 'NONE', *, *, #80082, .F. ) ;
#10703=CARTESIAN_POINT ( 'NONE',  ( 85.31310517497098544, 1.030564683017419500E-14, 0.000000000000000000 ) ) ;
#10713=VERTEX_POINT ( 'NONE', #79975 ) ;
#10728=AXIS2_PLACEMENT_3D ( 'NONE', #14983, #57033, #47878 ) ;
#10761=CARTESIAN_POINT ( 'NONE',  ( 103.5111111111111057, 1.023464760207051730E-14, 0.000000000000000000 ) ) ;
#10762=CIRCLE ( 'NONE', #40269, 5.000000000000011546 ) ;
#10775=EDGE_CURVE ( 'NONE', #37699, #33537, #27104, .T. ) ;
#10793=ADVANCED_FACE ( 'NONE', ( #26056 ), #106155, .T. ) ;
#10802=CARTESIAN_POINT ( 'NONE',  ( 100.0424503805845831, 1.016364837396684119E-14, 0.000000000000000000 ) ) ;
#10836=CARTESIAN_POINT ( 'NONE',  ( 83.86866073052654258, 5.000000000000020428, 0.000000000000000000 ) ) ;
#10855=VERTEX_POINT ( 'NONE', #98807 ) ;
#10863=CARTESIAN_POINT ( 'NONE',  ( 89.64643850830432825, -5.000000000000000888, 6.123233995736779101E-16 ) ) ;
#10944=FACE_OUTER_BOUND ( 'NONE', #20673, .T. ) ;
#10963=EDGE_CURVE ( 'NONE', #82194, #102006, #14863, .T. ) ;
#10971=CARTESIAN_POINT ( 'NONE',  ( 91.95555555555554861, 1.023464760207051730E-14, 0.000000000000000000 ) ) ;
#11001=AXIS2_PLACEMENT_3D ( 'NONE', #45568, #6139, #13700 ) ;
#11011=ADVANCED_FACE ( 'NONE', ( #5960 ), #23448, .T. ) ;
#11015=EDGE_CURVE ( 'NONE', #37220, #45973, #9614, .T. ) ;
#11067=CIRCLE ( 'NONE', #71365, 4.172000000000009479 ) ;
#11073=FACE_OUTER_BOUND ( 'NONE', #69947, .T. ) ;
#11143=CIRCLE ( 'NONE', #76585, 5.000000000000011546 ) ;
#11173=ORIENTED_EDGE ( 'NONE', *, *, #47995, .F. ) ;
#11199=EDGE_CURVE ( 'NONE', #77225, #3027, #40656, .T. ) ;
#11221=EDGE_CURVE ( 'NONE', #33725, #9363, #13121, .T. ) ;
#11225=CIRCLE ( 'NONE', #95642, 5.000000000000010658 ) ;
#11259=CARTESIAN_POINT ( 'NONE',  ( 0.7145311798163208605, 4.618802153517005848, 7.999999999999996447 ) ) ;
#11335=EDGE_CURVE ( 'NONE', #63169, #55214, #73361, .T. ) ;
#11378=FACE_OUTER_BOUND ( 'NONE', #19277, .T. ) ;
#11392=AXIS2_PLACEMENT_3D ( 'NONE', #53860, #85726, #93268 ) ;
#11409=DIRECTION ( 'NONE',  ( 0.5735764363510557073, -0.8191520442889850262, 1.003171929053516612E-16 ) ) ;
#11414=VERTEX_POINT ( 'NONE', #2924 ) ;
#11427=ORIENTED_EDGE ( 'NONE', *, *, #100379, .T. ) ;
#11428=CARTESIAN_POINT ( 'NONE',  ( 98.31310517497099966, -2.002967142162725287E-29, 5.000000000000011546 ) ) ;
#11484=ADVANCED_FACE ( 'NONE', ( #49478 ), #95537, .T. ) ;
#11487=ADVANCED_FACE ( 'NONE', ( #43924 ), #76820, .T. ) ;
#11559=ORIENTED_EDGE ( 'NONE', *, *, #5735, .F. ) ;
#11567=ORIENTED_EDGE ( 'NONE', *, *, #101646, .T. ) ;
#11570=CARTESIAN_POINT ( 'NONE',  ( 5.799999999999999822, 0.000000000000000000, 8.000000000000000000 ) ) ;
#11600=ORIENTED_EDGE ( 'NONE', *, *, #7935, .F. ) ;
#11639=CARTESIAN_POINT ( 'NONE',  ( 89.64643850830432825, 1.030564683017419500E-14, 0.000000000000000000 ) ) ;
#11649=EDGE_CURVE ( 'NONE', #6102, #22089, #48998, .T. ) ;
#11667=ORIENTED_EDGE ( 'NONE', *, *, #54336, .T. ) ;
#11700=CARTESIAN_POINT ( 'NONE',  ( 0.000000000000000000, 0.000000000000000000, 0.000000000000000000 ) ) ;
#11726=ORIENTED_EDGE ( 'NONE', *, *, #50059, .T. ) ;
#11777=EDGE_CURVE ( 'NONE', #43097, #31444, #32037, .T. ) ;
#11796=ORIENTED_EDGE ( 'NONE', *, *, #86311, .F. ) ;
#11804=AXIS2_PLACEMENT_3D ( 'NONE', #30935, #96179, #21780 ) ;
#11811=CARTESIAN_POINT ( 'NONE',  ( 5.799999999999999822, -4.618802153517009401, -8.000000000000001776 ) ) ;
#11840=LINE ( 'NONE', #28609, #9688 ) ;
#11877=LINE ( 'NONE', #85803, #20431 ) ;
#11882=EDGE_CURVE ( 'NONE', #92683, #29639, #27889, .T. ) ;
#11924=DIRECTION ( 'NONE',  ( -1.000000000000000000, -0.000000000000000000, -0.000000000000000000 ) ) ;
#11959=CARTESIAN_POINT ( 'NONE',  ( 0.000000000000000000, 0.000000000000000000, 0.000000000000000000 ) ) ;
#11971=DIRECTION ( 'NONE',  ( 0.000000000000000000, -1.000000000000000000, 0.000000000000000000 ) ) ;
#11997=CARTESIAN_POINT ( 'NONE',  ( 89.06666666666666288, 1.023464760207051730E-14, 0.000000000000000000 ) ) ;
#11999=CARTESIAN_POINT ( 'NONE',  ( 0.000000000000000000, 0.000000000000000000, 0.000000000000000000 ) ) ;
#12030=LINE ( 'NONE', #102648, #73676 ) ;
#12043=DIRECTION ( 'NONE',  ( 0.000000000000000000, -1.877893248421449282E-16, 1.000000000000000000 ) ) ;
#12050=LINE ( 'NONE', #93524, #37837 ) ;
#12070=ORIENTED_EDGE ( 'NONE', *, *, #27329, .F. ) ;
#12150=ORIENTED_EDGE ( 'NONE', *, *, #12358, .F. ) ;
#12172=DIRECTION ( 'NONE',  ( -1.000000000000000000, -1.224606353822377258E-16, -0.000000000000000000 ) ) ;
#12210=DIRECTION ( 'NONE',  ( -1.000000000000000000, -1.224606353822377258E-16, -0.000000000000000000 ) ) ;
#12260=DIRECTION ( 'NONE',  ( 1.000000000000000000, 1.224606353822377258E-16, 0.000000000000000000 ) ) ;
#12296=ORIENTED_EDGE ( 'NONE', *, *, #52759, .T. ) ;
#12334=CARTESIAN_POINT ( 'NONE',  ( 0.000000000000000000, 6.928203230275505220, 4.000000000000006217 ) ) ;
#12358=EDGE_CURVE ( 'NONE', #4508, #9366, #68720, .T. ) ;
#12377=CARTESIAN_POINT ( 'NONE',  ( 80.97977184163765685, 1.030564683017419500E-14, 0.000000000000000000 ) ) ;
#12401=LINE ( 'NONE', #85247, #4821 ) ;
#12428=EDGE_CURVE ( 'NONE', #22473, #16299, #99745, .T. ) ;
#12443=CARTESIAN_POINT ( 'NONE',  ( 81.84444444444444855, 4.172000000000019249, 0.000000000000000000 ) ) ;
#12451=DIRECTION ( 'NONE',  ( -1.000000000000000000, -0.000000000000000000, -0.000000000000000000 ) ) ;
#12505=LINE ( 'NONE', #45436, #43212 ) ;
#12510=CARTESIAN_POINT ( 'NONE',  ( 0.3173508448886528388, -8.480771745766398695, -1.310872448937994150 ) ) ;
#12534=LINE ( 'NONE', #53547, #42424 ) ;
#12556=DIRECTION ( 'NONE',  ( -1.000000000000000000, -1.224606353822377258E-16, -0.000000000000000000 ) ) ;
#12575=CARTESIAN_POINT ( 'NONE',  ( 81.26467260280679739, -2.002967142162725287E-29, 5.000000000000011546 ) ) ;
#12593=CARTESIAN_POINT ( 'NONE',  ( 88.48689482502902592, 6.123233995736582872E-16, -5.000000000000011546 ) ) ;
#12638=DIRECTION ( 'NONE',  ( 0.000000000000000000, 0.000000000000000000, 1.000000000000000000 ) ) ;
#12655=CARTESIAN_POINT ( 'NONE',  ( 83.28888888888889142, 1.023464760207051730E-14, 0.000000000000000000 ) ) ;
#12671=DIRECTION ( 'NONE',  ( -1.000000000000000000, -1.224606353822377258E-16, -0.000000000000000000 ) ) ;
#12713=B_SPLINE_CURVE_WITH_KNOTS ( 'NONE', 3,
 ( #44370, #37903, #69711, #103659, #62685, #12510, #79378, #102604 ),
 .UNSPECIFIED., .F., .F.,
 ( 4, 2, 2, 4 ),
 ( 0.004673709593152160051, 0.005837709341827647738, 0.007001709090503134558, 0.009329708587854108198 ),
 .UNSPECIFIED. ) ;
#12738=VECTOR ( 'NONE', #34405, 1000.000000000000000 ) ;
#12741=ORIENTED_EDGE ( 'NONE', *, *, #38225, .T. ) ;
#12841=PLANE ( 'NONE',  #48309 ) ;
#12859=ORIENTED_EDGE ( 'NONE', *, *, #98205, .T. ) ;
#12898=ORIENTED_EDGE ( 'NONE', *, *, #6181, .F. ) ;
#12965=ORIENTED_EDGE ( 'NONE', *, *, #102416, .F. ) ;
#12981=EDGE_LOOP ( 'NONE', ( #76272, #68404, #47011, #34384, #38469 ) ) ;
#13004=DIRECTION ( 'NONE',  ( 1.000000000000000000, 1.224606353822377258E-16, 0.000000000000000000 ) ) ;
#13006=CARTESIAN_POINT ( 'NONE',  ( 5.799999999999999822, 0.000000000000000000, 0.000000000000000000 ) ) ;
#13022=CARTESIAN_POINT ( 'NONE',  ( 96.86866073052655679, 1.030564683017419500E-14, 0.000000000000000000 ) ) ;
#13023=ADVANCED_FACE ( 'NONE', ( #40980 ), #67633, .T. ) ;
#13029=EDGE_CURVE ( 'NONE', #7841, #34210, #45611, .T. ) ;
#13042=EDGE_CURVE ( 'NONE', #31444, #1310, #21524, .T. ) ;
#13057=ORIENTED_EDGE ( 'NONE', *, *, #79476, .T. ) ;
#13063=DIRECTION ( 'NONE',  ( 0.000000000000000000, -1.000000000000000000, 0.000000000000000000 ) ) ;
#13101=EDGE_LOOP ( 'NONE', ( #27321, #2820 ) ) ;
#13121=B_SPLINE_CURVE_WITH_KNOTS ( 'NONE', 3,
 ( #11259, #101882, #52260, #29629, #28563, #12334 ),
 .UNSPECIFIED., .F., .F.,
 ( 4, 2, 4 ),
 ( 2.380731629586569301E-07, 0.002336973833157552933, 0.004673709593152147040 ),
 .UNSPECIFIED. ) ;
#13167=DIRECTION ( 'NONE',  ( 0.000000000000000000, -0.8660254037844381525, -0.5000000000000008882 ) ) ;
#13174=ORIENTED_EDGE ( 'NONE', *, *, #42157, .F. ) ;
#13220=ORIENTED_EDGE ( 'NONE', *, *, #6541, .F. ) ;
#13239=LINE ( 'NONE', #46163, #41563 ) ;
#13241=ORIENTED_EDGE ( 'NONE', *, *, #98530, .T. ) ;
#13275=AXIS2_PLACEMENT_3D ( 'NONE', #44867, #106658, #370 ) ;
#13294=AXIS2_PLACEMENT_3D ( 'NONE', #18980, #9767, #26023 ) ;
#13319=DIRECTION ( 'NONE',  ( 0.000000000000000000, -1.000000000000000000, 0.000000000000000000 ) ) ;
#13325=VERTEX_POINT ( 'NONE', #33872 ) ;
#13329=VERTEX_POINT ( 'NONE', #91564 ) ;
#13346=DIRECTION ( 'NONE',  ( -1.000000000000000000, -1.224606353822377258E-16, -0.000000000000000000 ) ) ;
#13347=VERTEX_POINT ( 'NONE', #94215 ) ;
#13365=VERTEX_POINT ( 'NONE', #28444 ) ;
#13395=CARTESIAN_POINT ( 'NONE',  ( 79.82022815836235452, 1.016364837396684119E-14, 0.000000000000000000 ) ) ;
#13399=AXIS2_PLACEMENT_3D ( 'NONE', #89125, #13623, #63268 ) ;
#13428=CARTESIAN_POINT ( 'NONE',  ( 87.62222222222222001, 1.023464760207051730E-14, 0.000000000000000000 ) ) ;
#13450=FACE_OUTER_BOUND ( 'NONE', #971, .T. ) ;
#13451=ORIENTED_EDGE ( 'NONE', *, *, #41292, .T. ) ;
#13454=ORIENTED_EDGE ( 'NONE', *, *, #90647, .T. ) ;
#13469=VERTEX_POINT ( 'NONE', #87190 ) ;
#13491=ORIENTED_EDGE ( 'NONE', *, *, #36971, .F. ) ;
#13520=CIRCLE ( 'NONE', #20446, 5.000000000000010658 ) ;
#13521=DIRECTION ( 'NONE',  ( -0.5735764363510459374, -0.8191520442889919096, 0.000000000000000000 ) ) ;
#13548=AXIS2_PLACEMENT_3D ( 'NONE', #2766, #50259, #1697 ) ;
#13561=EDGE_LOOP ( 'NONE', ( #85551, #77996, #76616, #20937 ) ) ;
#13564=CARTESIAN_POINT ( 'NONE',  ( 92.82022815836235452, 5.000000000000023093, 6.123233995736781074E-16 ) ) ;
#13596=EDGE_LOOP ( 'NONE', ( #40728, #28399, #63481 ) ) ;
#13619=DIRECTION ( 'NONE',  ( -1.000000000000000000, -1.224606353822377258E-16, -0.000000000000000000 ) ) ;
#13623=DIRECTION ( 'NONE',  ( -1.000000000000000000, -1.224606353822377258E-16, -0.000000000000000000 ) ) ;
#13638=FACE_OUTER_BOUND ( 'NONE', #55374, .T. ) ;
#13643=ADVANCED_FACE ( 'NONE', ( #38388 ), #31897, .T. ) ;
#13653=DIRECTION ( 'NONE',  ( -0.5735764363510459374, -0.8191520442889919096, 0.000000000000000000 ) ) ;
#13666=ADVANCED_FACE ( 'NONE', ( #28186 ), #79346, .T. ) ;
#13700=DIRECTION ( 'NONE',  ( 0.000000000000000000, -1.000000000000000000, 0.000000000000000000 ) ) ;
#13718=DIRECTION ( 'NONE',  ( -1.000000000000000000, -1.224606353822377258E-16, -0.000000000000000000 ) ) ;
#13719=EDGE_LOOP ( 'NONE', ( #48946, #15070, #37737, #73424, #91395, #55704 ) ) ;
#13725=CONICAL_SURFACE ( 'NONE', #62038, 4.172000000000009479, 0.9599310885968813656 ) ;
#13752=ORIENTED_EDGE ( 'NONE', *, *, #11649, .T. ) ;
#13759=CARTESIAN_POINT ( 'NONE',  ( 0.000000000000000000, 3.004629197474323585E-15, 8.000000000000000000 ) ) ;
#13761=ORIENTED_EDGE ( 'NONE', *, *, #6457, .F. ) ;
#13820=AXIS2_PLACEMENT_3D ( 'NONE', #59887, #70084, #69562 ) ;
#13837=LINE ( 'NONE', #94797, #37943 ) ;
#13847=ORIENTED_EDGE ( 'NONE', *, *, #41292, .F. ) ;
#13876=ORIENTED_EDGE ( 'NONE', *, *, #84176, .T. ) ;
#13879=FACE_OUTER_BOUND ( 'NONE', #62993, .T. ) ;
#13882=ORIENTED_EDGE ( 'NONE', *, *, #99777, .F. ) ;
#13885=CARTESIAN_POINT ( 'NONE',  ( 0.000000000000000000, 1.502314598737159228E-15, -8.000000000000000000 ) ) ;
#13894=AXIS2_PLACEMENT_3D ( 'NONE', #81641, #74094, #180 ) ;
#13913=FACE_OUTER_BOUND ( 'NONE', #13561, .T. ) ;
#13973=CARTESIAN_POINT ( 'NONE',  ( 95.70911704725124025, 6.123233995736582872E-16, -5.000000000000011546 ) ) ;
#14037=EDGE_CURVE ( 'NONE', #34646, #43584, #80003, .T. ) ;
#14051=VECTOR ( 'NONE', #49027, 1000.000000000000000 ) ;
#14064=DIRECTION ( 'NONE',  ( 0.000000000000000000, -1.000000000000000000, 0.000000000000000000 ) ) ;
#14073=EDGE_CURVE ( 'NONE', #36994, #95902, #48687, .T. ) ;
#14119=VECTOR ( 'NONE', #25702, 999.9999999999998863 ) ;
#14124=ORIENTED_EDGE ( 'NONE', *, *, #41092, .T. ) ;
#14193=ADVANCED_FACE ( 'NONE', ( #35756 ), #4400, .T. ) ;
#14202=ORIENTED_EDGE ( 'NONE', *, *, #70487, .T. ) ;
#14215=CARTESIAN_POINT ( 'NONE',  ( 104.9555555555555486, 1.023464760207051730E-14, 0.000000000000000000 ) ) ;
#14261=CARTESIAN_POINT ( 'NONE',  ( 92.53532739719321398, -5.000000000000000888, 6.123233995736779101E-16 ) ) ;
#14302=DIRECTION ( 'NONE',  ( -0.5735764363510459374, -0.8191520442889919096, 0.000000000000000000 ) ) ;
#14304=DIRECTION ( 'NONE',  ( -1.000000000000000000, -1.224606353822377258E-16, -0.000000000000000000 ) ) ;
#14314=CIRCLE ( 'NONE', #53960, 5.400000000000001243 ) ;
#14315=CARTESIAN_POINT ( 'NONE',  ( 0.000000000000000000, 6.123233995736767268E-16, -5.000000000000000888 ) ) ;
#14324=EDGE_LOOP ( 'NONE', ( #76604, #36094, #34161, #82168, #105716 ) ) ;
#14354=ORIENTED_EDGE ( 'NONE', *, *, #39263, .T. ) ;
#14398=ORIENTED_EDGE ( 'NONE', *, *, #84003, .F. ) ;
#14409=CARTESIAN_POINT ( 'NONE',  ( 83.86866073052654258, 5.000000000000021316, 0.000000000000000000 ) ) ;
#14456=EDGE_CURVE ( 'NONE', #33852, #99968, #97462, .T. ) ;
#14501=VERTEX_POINT ( 'NONE', #56665 ) ;
#14512=CARTESIAN_POINT ( 'NONE',  ( 0.06730325657375016424, -1.557442666578367829, 8.000000000000000000 ) ) ;
#14513=DIRECTION ( 'NONE',  ( -1.000000000000000000, -1.224606353822377258E-16, -0.000000000000000000 ) ) ;
#14545=FACE_OUTER_BOUND ( 'NONE', #62338, .T. ) ;
#14552=FACE_OUTER_BOUND ( 'NONE', #76118, .T. ) ;
#14567=DIRECTION ( 'NONE',  ( 0.000000000000000000, -1.000000000000000000, 0.000000000000000000 ) ) ;
#14571=ORIENTED_EDGE ( 'NONE', *, *, #21150, .F. ) ;
#14579=LINE ( 'NONE', #81970, #51759 ) ;
#14580=ORIENTED_EDGE ( 'NONE', *, *, #82398, .T. ) ;
#14609=AXIS2_PLACEMENT_3D ( 'NONE', #79587, #14304, #5696 ) ;
#14617=EDGE_CURVE ( 'NONE', #15530, #25050, #76044, .T. ) ;
#14641=CARTESIAN_POINT ( 'NONE',  ( 0.7145311798163219708, 4.618802153517003184, -8.000000000000000000 ) ) ;
#14682=LINE ( 'NONE', #81528, #16462 ) ;
#14698=ADVANCED_FACE ( 'NONE', ( #18925 ), #37310, .T. ) ;
#14735=CARTESIAN_POINT ( 'NONE',  ( 0.7145311798163234140, -9.237604307034013473, 6.198474679904167468E-16 ) ) ;
#14756=DIRECTION ( 'NONE',  ( -1.000000000000000000, -1.224606353822377258E-16, -0.000000000000000000 ) ) ;
#14763=CARTESIAN_POINT ( 'NONE',  ( 100.0424503805845831, 6.123233995736582872E-16, -5.000000000000011546 ) ) ;
#14768=CIRCLE ( 'NONE', #66450, 5.000000000000010658 ) ;
#14814=EDGE_CURVE ( 'NONE', #16299, #99968, #11840, .T. ) ;
#14849=AXIS2_PLACEMENT_3D ( 'NONE', #8585, #56597, #48502 ) ;
#14863=CIRCLE ( 'NONE', #75128, 4.172000000000009479 ) ;
#14876=AXIS2_PLACEMENT_3D ( 'NONE', #36356, #27734, #77300 ) ;
#14899=CARTESIAN_POINT ( 'NONE',  ( 80.97977184163765685, -5.000000000000000000, 6.123233995736778115E-16 ) ) ;
#14912=CIRCLE ( 'NONE', #94168, 5.000000000000011546 ) ;
#14922=DIRECTION ( 'NONE',  ( 1.000000000000000000, 1.224606353822377258E-16, 0.000000000000000000 ) ) ;
#14983=CARTESIAN_POINT ( 'NONE',  ( 0.000000000000000000, 0.000000000000000000, 0.000000000000000000 ) ) ;
#15028=VERTEX_POINT ( 'NONE', #14763 ) ;
#15031=ADVANCED_FACE ( 'NONE', ( #70372 ), #76923, .T. ) ;
#15045=VERTEX_POINT ( 'NONE', #96254 ) ;
#15070=ORIENTED_EDGE ( 'NONE', *, *, #90174, .T. ) ;
#15141=ORIENTED_EDGE ( 'NONE', *, *, #9492, .F. ) ;
#15153=ORIENTED_EDGE ( 'NONE', *, *, #97685, .T. ) ;
#15193=EDGE_LOOP ( 'NONE', ( #60769, #36893, #36137 ) ) ;
#15197=EDGE_CURVE ( 'NONE', #89220, #74466, #55739, .T. ) ;
#15231=CARTESIAN_POINT ( 'NONE',  ( 85.59800593614014019, 6.123233995736582872E-16, -5.000000000000011546 ) ) ;
#15236=CYLINDRICAL_SURFACE ( 'NONE', #99942, 5.000000000000000888 ) ;
#15294=DIRECTION ( 'NONE',  ( -1.000000000000000000, -1.224606353822377258E-16, -0.000000000000000000 ) ) ;
#15329=CARTESIAN_POINT ( 'NONE',  ( 102.9313392694734688, 1.016364837396684119E-14, 0.000000000000000000 ) ) ;
#15334=ADVANCED_FACE ( 'NONE', ( #27160 ), #45902, .T. ) ;
#15348=LINE ( 'NONE', #97323, #650 ) ;
#15420=DIRECTION ( 'NONE',  ( 1.000000000000000000, 1.224606353822377258E-16, 0.000000000000000000 ) ) ;
#15458=EDGE_CURVE ( 'NONE', #99968, #13469, #47724, .T. ) ;
#15476=CONICAL_SURFACE ( 'NONE', #53368, 5.000000000000010658, 0.9599310885968697082 ) ;
#15483=DIRECTION ( 'NONE',  ( 0.000000000000000000, -1.000000000000000000, 0.000000000000000000 ) ) ;
#15530=VERTEX_POINT ( 'NONE', #26628 ) ;
#15575=CARTESIAN_POINT ( 'NONE',  ( 82.42421628608209971, 1.030564683017419500E-14, 0.000000000000000000 ) ) ;
#15580=ORIENTED_EDGE ( 'NONE', *, *, #12428, .F. ) ;
#15597=CARTESIAN_POINT ( 'NONE',  ( 6.800000000000000711, 6.123233995736767268E-16, -5.000000000000000888 ) ) ;
#15623=ORIENTED_EDGE ( 'NONE', *, *, #49682, .T. ) ;
#15650=DIRECTION ( 'NONE',  ( -1.000000000000000000, -1.224606353822377258E-16, -0.000000000000000000 ) ) ;
#15683=CARTESIAN_POINT ( 'NONE',  ( 86.17777777777776294, 1.023464760207051730E-14, 0.000000000000000000 ) ) ;
#15693=LINE ( 'NONE', #41569, #17512 ) ;
#15710=CIRCLE ( 'NONE', #36415, 5.400000000000001243 ) ;
#15767=DIRECTION ( 'NONE',  ( -1.000000000000000000, -0.000000000000000000, -0.000000000000000000 ) ) ;
#15781=DIRECTION ( 'NONE',  ( -0.5735764363510461594, 0.8191520442889916875, 1.003171929053524870E-16 ) ) ;
#15799=CARTESIAN_POINT ( 'NONE',  ( 0.7145311798163234140, -9.237604307034013473, 6.198474679904167468E-16 ) ) ;
#15827=ORIENTED_EDGE ( 'NONE', *, *, #75125, .F. ) ;
#15830=AXIS2_PLACEMENT_3D ( 'NONE', #21845, #28895, #12638 ) ;
#15881=EDGE_LOOP ( 'NONE', ( #570, #611, #16798, #50920, #15141 ) ) ;
#15887=AXIS2_PLACEMENT_3D ( 'NONE', #24605, #64005, #6795 ) ;
#15923=VECTOR ( 'NONE', #22449, 1000.000000000000000 ) ;
#15964=CARTESIAN_POINT ( 'NONE',  ( 104.3757837139179117, 6.123233995736582872E-16, -5.000000000000011546 ) ) ;
#15970=FACE_OUTER_BOUND ( 'NONE', #73013, .T. ) ;
#15974=ORIENTED_EDGE ( 'NONE', *, *, #86330, .F. ) ;
#15978=VECTOR ( 'NONE', #28983, 1000.000000000000000 ) ;
#15981=ADVANCED_FACE ( 'NONE', ( #55166 ), #71358, .T. ) ;
#16021=ORIENTED_EDGE ( 'NONE', *, *, #97680, .F. ) ;
#16048=AXIS2_PLACEMENT_3D ( 'NONE', #11700, #3096, #77523 ) ;
#16057=DIRECTION ( 'NONE',  ( -1.000000000000000000, -1.224606353822377258E-16, -0.000000000000000000 ) ) ;
#16089=VECTOR ( 'NONE', #103792, 1000.000000000000000 ) ;
#16090=ADVANCED_FACE ( 'NONE', ( #77213 ), #73002, .T. ) ;
#16129=CARTESIAN_POINT ( 'NONE',  ( 0.000000000000000000, 6.928203230275505220, -4.000000000000007105 ) ) ;
#16139=CARTESIAN_POINT ( 'NONE',  ( 105.5353273971932140, -5.000000000000000000, 6.123233995736778115E-16 ) ) ;
#16149=ORIENTED_EDGE ( 'NONE', *, *, #44547, .T. ) ;
#16150=ORIENTED_EDGE ( 'NONE', *, *, #12428, .T. ) ;
#16170=CIRCLE ( 'NONE', #43742, 5.000000000000011546 ) ;
#16183=DIRECTION ( 'NONE',  ( 0.000000000000000000, -1.000000000000000000, 0.000000000000000000 ) ) ;
#16266=VECTOR ( 'NONE', #100704, 1000.000000000000000 ) ;
#16299=VERTEX_POINT ( 'NONE', #5449 ) ;
#16300=EDGE_CURVE ( 'NONE', #17856, #16922, #71756, .T. ) ;
#16317=ORIENTED_EDGE ( 'NONE', *, *, #54899, .T. ) ;
#16334=CARTESIAN_POINT ( 'NONE',  ( 5.799999999999999822, -4.618802153517009401, -8.000000000000001776 ) ) ;
#16349=LINE ( 'NONE', #8253, #41134 ) ;
#16366=ORIENTED_EDGE ( 'NONE', *, *, #33907, .F. ) ;
#16396=DIRECTION ( 'NONE',  ( 1.000000000000000000, 0.000000000000000000, -0.000000000000000000 ) ) ;
#16397=EDGE_LOOP ( 'NONE', ( #65278, #82030, #46752, #83283, #924 ) ) ;
#16408=ADVANCED_FACE ( 'NONE', ( #24317 ), #40309, .T. ) ;
#16431=DIRECTION ( 'NONE',  ( -1.000000000000000000, -1.224606353822377258E-16, -0.000000000000000000 ) ) ;
#16462=VECTOR ( 'NONE', #81015, 1000.000000000000000 ) ;
#16475=LINE ( 'NONE', #80139, #51632 ) ;
#16480=EDGE_CURVE ( 'NONE', #92048, #33852, #60958, .T. ) ;
#16494=DIRECTION ( 'NONE',  ( 0.5735764363510557073, -0.8191520442889850262, 1.003171929053516612E-16 ) ) ;
#16513=CARTESIAN_POINT ( 'NONE',  ( 86.75754961941542831, -2.002967142162725287E-29, 5.000000000000011546 ) ) ;
#16516=CARTESIAN_POINT ( 'NONE',  ( 0.3173508448886485089, -5.375634714784611745, 6.689127551062004962 ) ) ;
#16525=LINE ( 'NONE', #49417, #36279 ) ;
#16536=AXIS2_PLACEMENT_3D ( 'NONE', #84922, #19171, #40861 ) ;
#16556=VERTEX_POINT ( 'NONE', #64744 ) ;
#16568=EDGE_LOOP ( 'NONE', ( #82835, #48822, #66187, #14354, #22692 ) ) ;
#16602=DIRECTION ( 'NONE',  ( 0.000000000000000000, 0.000000000000000000, 1.000000000000000000 ) ) ;
#16615=DIRECTION ( 'NONE',  ( 1.000000000000000000, 1.224606353822377258E-16, 0.000000000000000000 ) ) ;
#16634=ORIENTED_EDGE ( 'NONE', *, *, #91949, .F. ) ;
#16642=ORIENTED_EDGE ( 'NONE', *, *, #18306, .T. ) ;
#16662=DIRECTION ( 'NONE',  ( -1.000000000000000000, -1.224606353822377258E-16, -0.000000000000000000 ) ) ;
#16681=DIRECTION ( 'NONE',  ( -1.000000000000000000, -1.224606353822377258E-16, -0.000000000000000000 ) ) ;
#16720=DIRECTION ( 'NONE',  ( 0.000000000000000000, 1.000000000000000000, 0.000000000000000000 ) ) ;
#16762=EDGE_CURVE ( 'NONE', #21657, #13347, #35247, .T. ) ;
#16784=DIRECTION ( 'NONE',  ( -1.000000000000000000, -0.000000000000000000, -0.000000000000000000 ) ) ;
#16798=ORIENTED_EDGE ( 'NONE', *, *, #70267, .T. ) ;
#16826=CARTESIAN_POINT ( 'NONE',  ( 100.0424503805845831, 5.000000000000023093, 6.123233995736781074E-16 ) ) ;
#16844=CARTESIAN_POINT ( 'NONE',  ( 0.000000000000000000, 0.000000000000000000, 0.000000000000000000 ) ) ;
#16848=AXIS2_PLACEMENT_3D ( 'NONE', #96866, #38137, #4145 ) ;
#16851=ORIENTED_EDGE ( 'NONE', *, *, #21881, .T. ) ;
#16911=CARTESIAN_POINT ( 'NONE',  ( 99.17777777777777715, 1.023464760207051730E-14, 0.000000000000000000 ) ) ;
#16922=VERTEX_POINT ( 'NONE', #48416 ) ;
#16924=EDGE_CURVE ( 'NONE', #40083, #45434, #95514, .T. ) ;
#16943=CARTESIAN_POINT ( 'NONE',  ( 95.42421628608209971, 1.030564683017419500E-14, 0.000000000000000000 ) ) ;
#16947=CARTESIAN_POINT ( 'NONE',  ( 0.000000000000000000, 6.123233995736767268E-16, -5.000000000000000888 ) ) ;
#17071=DIRECTION ( 'NONE',  ( 1.000000000000000000, 0.000000000000000000, -0.000000000000000000 ) ) ;
#17086=AXIS2_PLACEMENT_3D ( 'NONE', #13006, #102573, #45931 ) ;
#17091=FACE_OUTER_BOUND ( 'NONE', #25008, .T. ) ;
#17142=DIRECTION ( 'NONE',  ( 0.000000000000000000, 0.000000000000000000, -1.000000000000000000 ) ) ;
#17162=CARTESIAN_POINT ( 'NONE',  ( 99.75754961941544252, 5.000000000000020428, 0.000000000000000000 ) ) ;
#17172=DIRECTION ( 'NONE',  ( 0.5735764363510557073, -0.8191520442889850262, 1.003171929053516612E-16 ) ) ;
#17201=VECTOR ( 'NONE', #84609, 1000.000000000000000 ) ;
#17235=EDGE_CURVE ( 'NONE', #20011, #36994, #24701, .T. ) ;
#17247=ORIENTED_EDGE ( 'NONE', *, *, #46916, .F. ) ;
#17273=ADVANCED_FACE ( 'NONE', ( #75891 ), #84531, .T. ) ;
#17328=ORIENTED_EDGE ( 'NONE', *, *, #96837, .F. ) ;
#17335=DIRECTION ( 'NONE',  ( -1.000000000000000000, -1.224606353822377258E-16, -0.000000000000000000 ) ) ;
#17336=DIRECTION ( 'NONE',  ( 0.000000000000000000, 1.000000000000000000, 0.000000000000000000 ) ) ;
#17355=VERTEX_POINT ( 'NONE', #79081 ) ;
#17365=AXIS2_PLACEMENT_3D ( 'NONE', #47991, #74269, #42439 ) ;
#17368=CARTESIAN_POINT ( 'NONE',  ( 82.70911704725124025, 1.016364837396684119E-14, 0.000000000000000000 ) ) ;
#17389=DIRECTION ( 'NONE',  ( -1.000000000000000000, -1.224606353822377258E-16, -0.000000000000000000 ) ) ;
#17410=CARTESIAN_POINT ( 'NONE',  ( 101.2019940638598854, 1.030564683017419500E-14, 0.000000000000000000 ) ) ;
#17435=VECTOR ( 'NONE', #13653, 1000.000000000000000 ) ;
#17436=EDGE_CURVE ( 'NONE', #45973, #9363, #74622, .T. ) ;
#17452=FACE_OUTER_BOUND ( 'NONE', #37728, .T. ) ;
#17455=ORIENTED_EDGE ( 'NONE', *, *, #27401, .F. ) ;
#17480=DIRECTION ( 'NONE',  ( -1.000000000000000000, -1.224606353822377258E-16, -0.000000000000000000 ) ) ;
#17506=DIRECTION ( 'NONE',  ( 0.000000000000000000, -1.000000000000000000, 0.000000000000000000 ) ) ;
#17510=VERTEX_POINT ( 'NONE', #65017 ) ;
#17512=VECTOR ( 'NONE', #25424, 1000.000000000000000 ) ;
#17552=CARTESIAN_POINT ( 'NONE',  ( 100.0424503805845831, 1.016364837396684119E-14, 0.000000000000000000 ) ) ;
#17587=DIRECTION ( 'NONE',  ( 0.000000000000000000, -1.000000000000000000, 0.000000000000000000 ) ) ;
#17676=APPLICATION_CONTEXT ( 'automotive_design' ) ;
#17681=CYLINDRICAL_SURFACE ( 'NONE', #55572, 5.000000000000000888 ) ;
#17682=CARTESIAN_POINT ( 'NONE',  ( 0.000000000000000000, 6.123233995736767268E-16, -5.000000000000000888 ) ) ;
#17690=CARTESIAN_POINT ( 'NONE',  ( 98.59800593614012598, 6.123233995736582872E-16, -5.000000000000011546 ) ) ;
#17697=DIRECTION ( 'NONE',  ( 0.000000000000000000, -1.000000000000000000, 0.000000000000000000 ) ) ;
#17698=CYLINDRICAL_SURFACE ( 'NONE', #88884, 5.000000000000000888 ) ;
#17769=ORIENTED_EDGE ( 'NONE', *, *, #46663, .T. ) ;
#17819=CARTESIAN_POINT ( 'NONE',  ( 94.26467260280679739, 1.016364837396684119E-14, 0.000000000000000000 ) ) ;
#17843=AXIS2_PLACEMENT_3D ( 'NONE', #99222, #25937, #48551 ) ;
#17845=CARTESIAN_POINT ( 'NONE',  ( 87.62222222222222001, 1.023464760207051730E-14, 0.000000000000000000 ) ) ;
#17856=VERTEX_POINT ( 'NONE', #57179 ) ;
#17909=VERTEX_POINT ( 'NONE', #35076 ) ;
#17915=CARTESIAN_POINT ( 'NONE',  ( 104.3757837139179117, 1.016364837396684119E-14, 0.000000000000000000 ) ) ;
#18031=CARTESIAN_POINT ( 'NONE',  ( 0.7145311798163208605, 4.618802153517005848, 7.999999999999996447 ) ) ;
#18094=CARTESIAN_POINT ( 'NONE',  ( 91.09088295274877112, 6.123233995736568081E-16, -5.000000000000011546 ) ) ;
#18112=LINE ( 'NONE', #60178, #14119 ) ;
#18127=CARTESIAN_POINT ( 'NONE',  ( 94.84444444444443434, -4.171999999999998820, 5.616230220889773285E-16 ) ) ;
#18135=DIRECTION ( 'NONE',  ( 0.000000000000000000, -1.000000000000000000, 0.000000000000000000 ) ) ;
#18149=ADVANCED_FACE ( 'NONE', ( #25261 ), #65693, .T. ) ;
#18174=LINE ( 'NONE', #58626, #27266 ) ;
#18208=LINE ( 'NONE', #101758, #12738 ) ;
#18227=CARTESIAN_POINT ( 'NONE',  ( 88.20199406385988539, 5.000000000000020428, 0.000000000000000000 ) ) ;
#18271=AXIS2_PLACEMENT_3D ( 'NONE', #18546, #41733, #101568 ) ;
#18272=ORIENTED_EDGE ( 'NONE', *, *, #4552, .T. ) ;
#18279=EDGE_CURVE ( 'NONE', #18574, #35853, #47220, .T. ) ;
#18306=EDGE_CURVE ( 'NONE', #101891, #33852, #2544, .T. ) ;
#18310=ORIENTED_EDGE ( 'NONE', *, *, #44623, .F. ) ;
#18342=CIRCLE ( 'NONE', #14849, 4.172000000000009479 ) ;
#18353=CARTESIAN_POINT ( 'NONE',  ( 0.000000000000000000, 0.000000000000000000, 5.000000000000000888 ) ) ;
#18407=CIRCLE ( 'NONE', #28746, 4.172000000000009479 ) ;
#18475=DIRECTION ( 'NONE',  ( 0.000000000000000000, -1.000000000000000000, 0.000000000000000000 ) ) ;
#18493=DIRECTION ( 'NONE',  ( -1.000000000000000000, -0.000000000000000000, -0.000000000000000000 ) ) ;
#18498=VECTOR ( 'NONE', #91255, 1000.000000000000000 ) ;
#18514=AXIS2_PLACEMENT_3D ( 'NONE', #64986, #16431, #98923 ) ;
#18546=CARTESIAN_POINT ( 'NONE',  ( 87.04245038058458306, 1.016364837396684119E-14, 0.000000000000000000 ) ) ;
#18557=CARTESIAN_POINT ( 'NONE',  ( 91.09088295274877112, 5.000000000000020428, 0.000000000000000000 ) ) ;
#18574=VERTEX_POINT ( 'NONE', #40748 ) ;
#18586=CARTESIAN_POINT ( 'NONE',  ( 91.09088295274877112, 5.000000000000021316, 0.000000000000000000 ) ) ;
#18592=CONICAL_SURFACE ( 'NONE', #78834, 5.000000000000010658, 0.9599310885968697082 ) ;
#18659=EDGE_CURVE ( 'NONE', #54377, #4657, #100510, .T. ) ;
#18677=CARTESIAN_POINT ( 'NONE',  ( 96.86866073052655679, 5.000000000000020428, 0.000000000000000000 ) ) ;
#18713=CIRCLE ( 'NONE', #68665, 5.000000000000010658 ) ;
#18720=ORIENTED_EDGE ( 'NONE', *, *, #73191, .F. ) ;
#18730=ORIENTED_EDGE ( 'NONE', *, *, #79476, .F. ) ;
#18737=VECTOR ( 'NONE', #83242, 1000.000000000000114 ) ;
#18794=EDGE_CURVE ( 'NONE', #19034, #22906, #84411, .T. ) ;
#18875=EDGE_CURVE ( 'NONE', #35853, #65774, #79797, .T. ) ;
#18877=CARTESIAN_POINT ( 'NONE',  ( 105.5353273971932140, 1.030564683017419500E-14, 0.000000000000000000 ) ) ;
#18906=CIRCLE ( 'NONE', #3388, 5.000000000000010658 ) ;
#18920=CIRCLE ( 'NONE', #8546, 5.000000000000010658 ) ;
#18925=FACE_OUTER_BOUND ( 'NONE', #71968, .T. ) ;
#18980=CARTESIAN_POINT ( 'NONE',  ( 103.5111111111111057, 1.023464760207051730E-14, 0.000000000000000000 ) ) ;
#18981=CARTESIAN_POINT ( 'NONE',  ( 0.000000000000000000, 0.000000000000000000, 0.000000000000000000 ) ) ;
#19006=DIRECTION ( 'NONE',  ( 0.000000000000000000, -1.000000000000000000, 0.000000000000000000 ) ) ;
#19034=VERTEX_POINT ( 'NONE', #12443 ) ;
#19126=ADVANCED_FACE ( 'NONE', ( #44257 ), #32933, .T. ) ;
#19171=DIRECTION ( 'NONE',  ( -1.000000000000000000, -1.224606353822377258E-16, -0.000000000000000000 ) ) ;
#19189=CARTESIAN_POINT ( 'NONE',  ( 86.75754961941542831, 1.030564683017419500E-14, 0.000000000000000000 ) ) ;
#19196=ORIENTED_EDGE ( 'NONE', *, *, #18659, .F. ) ;
#19272=CYLINDRICAL_SURFACE ( 'NONE', #3086, 5.000000000000000888 ) ;
#19277=EDGE_LOOP ( 'NONE', ( #6830, #27357, #64753, #36146, #45848 ) ) ;
#19359=CARTESIAN_POINT ( 'NONE',  ( 92.82022815836235452, 1.016364837396684119E-14, 0.000000000000000000 ) ) ;
#19386=ORIENTED_EDGE ( 'NONE', *, *, #88444, .T. ) ;
#19404=ORIENTED_EDGE ( 'NONE', *, *, #106008, .T. ) ;
#19443=ADVANCED_FACE ( 'NONE', ( #95333 ), #52737, .T. ) ;
#19501=DIRECTION ( 'NONE',  ( 0.000000000000000000, -1.000000000000000000, 0.000000000000000000 ) ) ;
#19524=EDGE_CURVE ( 'NONE', #71082, #10644, #53612, .T. ) ;
#19566=CARTESIAN_POINT ( 'NONE',  ( 83.86866073052654258, -5.000000000000000000, 6.123233995736778115E-16 ) ) ;
#19671=DIRECTION ( 'NONE',  ( -0.5735764363510461594, 0.8191520442889916875, 1.003171929053524870E-16 ) ) ;
#19686=EDGE_CURVE ( 'NONE', #44057, #97033, #48878, .T. ) ;
#19749=AXIS2_PLACEMENT_3D ( 'NONE', #33556, #25484, #9245 ) ;
#19805=ADVANCED_FACE ( 'NONE', ( #47699 ), #48228, .T. ) ;
#19837=DIRECTION ( 'NONE',  ( 1.000000000000000000, 0.000000000000000000, -0.000000000000000000 ) ) ;
#19838=DIRECTION ( 'NONE',  ( -1.000000000000000000, -0.000000000000000000, -0.000000000000000000 ) ) ;
#19880=ORIENTED_EDGE ( 'NONE', *, *, #28617, .T. ) ;
#19881=DIRECTION ( 'NONE',  ( 0.000000000000000000, -3.755786496842903988E-16, -1.000000000000000000 ) ) ;
#19887=DIRECTION ( 'NONE',  ( 1.000000000000000000, 1.224606353822377258E-16, 0.000000000000000000 ) ) ;
#19927=AXIS2_PLACEMENT_3D ( 'NONE', #28717, #5465, #61599 ) ;
#19965=CARTESIAN_POINT ( 'NONE',  ( 97.15356149169568312, 1.016364837396684119E-14, 0.000000000000000000 ) ) ;
#19987=CONICAL_SURFACE ( 'NONE', #83594, 5.000000000000010658, 0.9599310885968697082 ) ;
#19988=FACE_OUTER_BOUND ( 'NONE', #71564, .T. ) ;
#20011=VERTEX_POINT ( 'NONE', #33027 ) ;
#20029=DIRECTION ( 'NONE',  ( -1.000000000000000000, -1.224606353822377258E-16, -0.000000000000000000 ) ) ;
#20074=VECTOR ( 'NONE', #35122, 1000.000000000000000 ) ;
#20103=DIRECTION ( 'NONE',  ( 0.000000000000000000, -1.000000000000000000, 0.000000000000000000 ) ) ;
#20111=DIRECTION ( 'NONE',  ( -1.000000000000000000, -1.224606353822377258E-16, -0.000000000000000000 ) ) ;
#20122=CARTESIAN_POINT ( 'NONE',  ( 5.799999999999999822, -4.618802153516994302, 8.000000000000000000 ) ) ;
#20131=ORIENTED_EDGE ( 'NONE', *, *, #29706, .F. ) ;
#20165=ADVANCED_FACE ( 'NONE', ( #85271 ), #77180, .T. ) ;
#20173=ORIENTED_EDGE ( 'NONE', *, *, #87420, .T. ) ;
#20177=CARTESIAN_POINT ( 'NONE',  ( 86.75754961941542831, 1.030564683017419500E-14, 0.000000000000000000 ) ) ;
#20199=DIRECTION ( 'NONE',  ( 0.000000000000000000, 0.000000000000000000, 1.000000000000000000 ) ) ;
#20234=ORIENTED_EDGE ( 'NONE', *, *, #100379, .F. ) ;
#20269=VECTOR ( 'NONE', #59413, 999.9999999999998863 ) ;
#20293=CARTESIAN_POINT ( 'NONE',  ( 90.51111111111110574, -4.171999999999998820, 0.000000000000000000 ) ) ;
#20426=ORIENTED_EDGE ( 'NONE', *, *, #29916, .F. ) ;
#20431=VECTOR ( 'NONE', #44804, 1000.000000000000000 ) ;
#20446=AXIS2_PLACEMENT_3D ( 'NONE', #103827, #29971, #80074 ) ;
#20482=EDGE_CURVE ( 'NONE', #52131, #19034, #33155, .T. ) ;
#20489=DIRECTION ( 'NONE',  ( 1.000000000000000000, 0.000000000000000000, 0.000000000000000000 ) ) ;
#20512=DIRECTION ( 'NONE',  ( -1.000000000000000000, -1.224606353822377258E-16, -0.000000000000000000 ) ) ;
#20588=ORIENTED_EDGE ( 'NONE', *, *, #84003, .T. ) ;
#20613=VERTEX_POINT ( 'NONE', #31064 ) ;
#20655=FACE_OUTER_BOUND ( 'NONE', #58458, .T. ) ;
#20673=EDGE_LOOP ( 'NONE', ( #96961, #9076, #46664, #98467, #76703 ) ) ;
#20715=DIRECTION ( 'NONE',  ( -1.000000000000000000, -1.224606353822377258E-16, -0.000000000000000000 ) ) ;
#20746=LINE ( 'NONE', #18586, #46425 ) ;
#20766=ORIENTED_EDGE ( 'NONE', *, *, #41092, .F. ) ;
#20799=CYLINDRICAL_SURFACE ( 'NONE', #37740, 5.000000000000000888 ) ;
#20810=FACE_OUTER_BOUND ( 'NONE', #23587, .T. ) ;
#20853=AXIS2_PLACEMENT_3D ( 'NONE', #4889, #62600, #30782 ) ;
#20891=ORIENTED_EDGE ( 'NONE', *, *, #102686, .T. ) ;
#20935=CARTESIAN_POINT ( 'NONE',  ( 0.000000000000000000, 0.000000000000000000, 0.000000000000000000 ) ) ;
#20936=CONICAL_SURFACE ( 'NONE', #10479, 5.000000000000010658, 0.9599310885968697082 ) ;
#20937=ORIENTED_EDGE ( 'NONE', *, *, #36601, .F. ) ;
#20968=VECTOR ( 'NONE', #6695, 1000.000000000000000 ) ;
#21114=CARTESIAN_POINT ( 'NONE',  ( 104.0908829527487711, -2.002967142162725287E-29, 5.000000000000011546 ) ) ;
#21150=EDGE_CURVE ( 'NONE', #64162, #93942, #105574, .T. ) ;
#21164=DIRECTION ( 'NONE',  ( -1.000000000000000000, -1.224606353822377258E-16, -0.000000000000000000 ) ) ;
#21182=DIRECTION ( 'NONE',  ( -0.5735764363510459374, -0.8191520442889919096, 0.000000000000000000 ) ) ;
#21184=ORIENTED_EDGE ( 'NONE', *, *, #71183, .T. ) ;
#21236=DIRECTION ( 'NONE',  ( 1.000000000000000000, 0.000000000000000000, -0.000000000000000000 ) ) ;
#21262=ORIENTED_EDGE ( 'NONE', *, *, #55043, .F. ) ;
#21281=ADVANCED_FACE ( 'NONE', ( #106766 ), #64326, .T. ) ;
#21283=ORIENTED_EDGE ( 'NONE', *, *, #102460, .F. ) ;
#21366=VERTEX_POINT ( 'NONE', #92175 ) ;
#21370=AXIS2_PLACEMENT_3D ( 'NONE', #29282, #36838, #102598 ) ;
#21385=ORIENTED_EDGE ( 'NONE', *, *, #100977, .F. ) ;
#21420=DIRECTION ( 'NONE',  ( 0.5735764363510557073, -0.8191520442889850262, 1.003171929053516612E-16 ) ) ;
#21425=AXIS2_PLACEMENT_3D ( 'NONE', #58340, #34108, #8191 ) ;
#21465=CIRCLE ( 'NONE', #2492, 8.000000000000000000 ) ;
#21489=DIRECTION ( 'NONE',  ( 0.000000000000000000, -1.000000000000000000, 0.000000000000000000 ) ) ;
#21524=CIRCLE ( 'NONE', #14609, 5.000000000000010658 ) ;
#21538=EDGE_LOOP ( 'NONE', ( #34058, #24245, #16317, #90718, #30531, #20766 ) ) ;
#21592=AXIS2_PLACEMENT_3D ( 'NONE', #60357, #101328, #4222 ) ;
#21607=CARTESIAN_POINT ( 'NONE',  ( 0.000000000000000000, 1.502314598737159228E-15, -8.000000000000000000 ) ) ;
#21608=DIRECTION ( 'NONE',  ( 0.000000000000000000, 0.000000000000000000, -1.000000000000000000 ) ) ;
#21614=DIRECTION ( 'NONE',  ( -1.000000000000000000, -1.224606353822377258E-16, -0.000000000000000000 ) ) ;
#21649=CIRCLE ( 'NONE', #68106, 4.172000000000009479 ) ;
#21657=VERTEX_POINT ( 'NONE', #3994 ) ;
#21718=ORIENTED_EDGE ( 'NONE', *, *, #42074, .F. ) ;
#21780=DIRECTION ( 'NONE',  ( -0.000000000000000000, 0.000000000000000000, -1.000000000000000000 ) ) ;
#21815=AXIS2_PLACEMENT_3D ( 'NONE', #10703, #43617, #58754 ) ;
#21835=ORIENTED_EDGE ( 'NONE', *, *, #6541, .T. ) ;
#21841=FACE_OUTER_BOUND ( 'NONE', #70, .T. ) ;
#21845=CARTESIAN_POINT ( 'NONE',  ( 0.000000000000000000, 0.000000000000000000, 0.000000000000000000 ) ) ;
#21881=EDGE_CURVE ( 'NONE', #48515, #101241, #47344, .T. ) ;
#21900=AXIS2_PLACEMENT_3D ( 'NONE', #99877, #17389, #1150 ) ;
#21904=CARTESIAN_POINT ( 'NONE',  ( 97.15356149169568312, 1.016364837396684119E-14, 0.000000000000000000 ) ) ;
#21943=AXIS2_PLACEMENT_3D ( 'NONE', #41422, #106683, #17697 ) ;
#21972=AXIS2_PLACEMENT_3D ( 'NONE', #94120, #93599, #36983 ) ;
#21982=EDGE_LOOP ( 'NONE', ( #22752, #55926, #81246 ) ) ;
#22056=DIRECTION ( 'NONE',  ( 0.000000000000000000, -1.000000000000000000, 0.000000000000000000 ) ) ;
#22060=CIRCLE ( 'NONE', #30693, 8.000000000000000000 ) ;
#22089=VERTEX_POINT ( 'NONE', #321 ) ;
#22091=DIRECTION ( 'NONE',  ( -1.000000000000000000, -1.224606353822377258E-16, -0.000000000000000000 ) ) ;
#22124=CARTESIAN_POINT ( 'NONE',  ( 0.7145311798163195283, -4.618802153516994302, 8.000000000000000000 ) ) ;
#22125=DIRECTION ( 'NONE',  ( 0.000000000000000000, -1.000000000000000000, 0.000000000000000000 ) ) ;
#22126=CARTESIAN_POINT ( 'NONE',  ( 84.73333333333332007, 4.172000000000019249, 5.109226446042768454E-16 ) ) ;
#22146=FACE_OUTER_BOUND ( 'NONE', #49735, .T. ) ;
#22157=CYLINDRICAL_SURFACE ( 'NONE', #33575, 5.000000000000000888 ) ;
#22159=VECTOR ( 'NONE', #95770, 1000.000000000000000 ) ;
#22173=CIRCLE ( 'NONE', #91066, 4.172000000000009479 ) ;
#22227=CARTESIAN_POINT ( 'NONE',  ( 87.62222222222222001, 4.172000000000019249, 5.109226446042768454E-16 ) ) ;
#22267=CARTESIAN_POINT ( 'NONE',  ( 88.20199406385988539, 1.030564683017419500E-14, 0.000000000000000000 ) ) ;
#22345=AXIS2_PLACEMENT_3D ( 'NONE', #60801, #33877, #66755 ) ;
#22370=VECTOR ( 'NONE', #65024, 1000.000000000000000 ) ;
#22386=CIRCLE ( 'NONE', #3422, 5.000000000000011546 ) ;
#22390=CIRCLE ( 'NONE', #39616, 4.172000000000009479 ) ;
#22449=DIRECTION ( 'NONE',  ( 0.5735764363510554853, 0.8191520442889852482, 0.000000000000000000 ) ) ;
#22472=ADVANCED_FACE ( 'NONE', ( #96824 ), #83593, .T. ) ;
#22473=VERTEX_POINT ( 'NONE', #72008 ) ;
#22514=CARTESIAN_POINT ( 'NONE',  ( 96.86866073052655679, 6.123233995736568081E-16, -5.000000000000011546 ) ) ;
#22542=CONICAL_SURFACE ( 'NONE', #72470, 4.172000000000009479, 0.9599310885968813656 ) ;
#22551=ADVANCED_FACE ( 'NONE', ( #43361 ), #74964, .T. ) ;
#22565=ORIENTED_EDGE ( 'NONE', *, *, #101267, .F. ) ;
#22622=AXIS2_PLACEMENT_3D ( 'NONE', #83484, #33914, #8528 ) ;
#22665=FACE_BOUND ( 'NONE', #73274, .T. ) ;
#22671=CARTESIAN_POINT ( 'NONE',  ( 91.37578371391791165, 1.016364837396684119E-14, 0.000000000000000000 ) ) ;
#22679=AXIS2_PLACEMENT_3D ( 'NONE', #7588, #99252, #89600 ) ;
#22692=ORIENTED_EDGE ( 'NONE', *, *, #10150, .F. ) ;
#22729=ORIENTED_EDGE ( 'NONE', *, *, #1218, .F. ) ;
#22752=ORIENTED_EDGE ( 'NONE', *, *, #426, .T. ) ;
#22753=AXIS2_PLACEMENT_3D ( 'NONE', #43269, #92870, #58385 ) ;
#22787=CARTESIAN_POINT ( 'NONE',  ( -3.710639583684274633E-15, 6.732211846623394003, -4.339467034331190298 ) ) ;
#22792=ORIENTED_EDGE ( 'NONE', *, *, #87420, .F. ) ;
#22824=EDGE_CURVE ( 'NONE', #55214, #63169, #90533, .T. ) ;
#22891=EDGE_CURVE ( 'NONE', #51522, #33537, #881, .T. ) ;
#22893=CARTESIAN_POINT ( 'NONE',  ( 0.01678220608715901702, 0.7854258608507265205, -8.000000000000001776 ) ) ;
#22895=CARTESIAN_POINT ( 'NONE',  ( 86.17777777777776294, 1.023464760207051730E-14, 0.000000000000000000 ) ) ;
#22900=CONICAL_SURFACE ( 'NONE', #7379, 5.000000000000010658, 0.9599310885968697082 ) ;
#22906=VERTEX_POINT ( 'NONE', #68718 ) ;
#22959=VERTEX_POINT ( 'NONE', #15231 ) ;
#23036=B_SPLINE_CURVE_WITH_KNOTS ( 'NONE', 3,
 ( #48080, #80982, #7098, #24394, #23860, #90151 ),
 .UNSPECIFIED., .F., .F.,
 ( 4, 2, 4 ),
 ( 2.380731629569274211E-07, 0.002336973833157562908, 0.004673709593152167857 ),
 .UNSPECIFIED. ) ;
#23053=DIRECTION ( 'NONE',  ( 0.000000000000000000, 0.000000000000000000, 1.000000000000000000 ) ) ;
#23143=ADVANCED_FACE ( 'NONE', ( #66440 ), #24434, .T. ) ;
#23172=ORIENTED_EDGE ( 'NONE', *, *, #7199, .T. ) ;
#23178=CONICAL_SURFACE ( 'NONE', #21425, 4.172000000000009479, 0.9599310885968813656 ) ;
#23205=DIRECTION ( 'NONE',  ( -1.000000000000000000, -1.224606353822377258E-16, -0.000000000000000000 ) ) ;
#23261=ORIENTED_EDGE ( 'NONE', *, *, #102731, .T. ) ;
#23279=CARTESIAN_POINT ( 'NONE',  ( 0.000000000000000000, 0.000000000000000000, 5.000000000000000888 ) ) ;
#23331=ADVANCED_FACE ( 'NONE', ( #14552 ), #85468, .T. ) ;
#23354=CARTESIAN_POINT ( 'NONE',  ( 90.51111111111110574, 1.023464760207051730E-14, 0.000000000000000000 ) ) ;
#23370=CARTESIAN_POINT ( 'NONE',  ( 79.82022815836235452, 6.123233995736582872E-16, -5.000000000000011546 ) ) ;
#23386=DIRECTION ( 'NONE',  ( 0.000000000000000000, -1.000000000000000000, 0.000000000000000000 ) ) ;
#23396=DIRECTION ( 'NONE',  ( 0.000000000000000000, 0.4999999999999996114, -0.8660254037844388186 ) ) ;
#23417=DIRECTION ( 'NONE',  ( -1.000000000000000000, -0.000000000000000000, -0.000000000000000000 ) ) ;
#23424=CARTESIAN_POINT ( 'NONE',  ( 6.400000000000000355, 4.618802153517003184, -8.000000000000000000 ) ) ;
#23435=ORIENTED_EDGE ( 'NONE', *, *, #4590, .T. ) ;
#23448=CONICAL_SURFACE ( 'NONE', #95810, 8.000000000000000000, 1.047197551196600296 ) ;
#23480=EDGE_CURVE ( 'NONE', #48515, #9861, #50512, .T. ) ;
#23523=AXIS2_PLACEMENT_3D ( 'NONE', #38394, #45936, #54522 ) ;
#23543=CIRCLE ( 'NONE', #82090, 4.172000000000009479 ) ;
#23581=DIRECTION ( 'NONE',  ( -1.000000000000000000, -0.000000000000000000, -0.000000000000000000 ) ) ;
#23587=EDGE_LOOP ( 'NONE', ( #17328, #87800, #87347, #83626, #76462 ) ) ;
#23597=PLANE ( 'NONE',  #59758 ) ;
#23619=FACE_OUTER_BOUND ( 'NONE', #77432, .T. ) ;
#23626=CARTESIAN_POINT ( 'NONE',  ( 85.59800593614014019, -4.999999999999980460, 0.000000000000000000 ) ) ;
#23629=VERTEX_POINT ( 'NONE', #62889 ) ;
#23647=CARTESIAN_POINT ( 'NONE',  ( 79.82022815836235452, 1.016364837396684119E-14, 0.000000000000000000 ) ) ;
#23762=CARTESIAN_POINT ( 'NONE',  ( 5.799999999999999822, 0.000000000000000000, 0.000000000000000000 ) ) ;
#23809=EDGE_CURVE ( 'NONE', #44057, #38733, #24040, .T. ) ;
#23860=CARTESIAN_POINT ( 'NONE',  ( -3.577867169202164632E-15, 7.321656987762870550, -3.318518101603009196 ) ) ;
#23915=LINE ( 'NONE', #56756, #94971 ) ;
#23918=DIRECTION ( 'NONE',  ( 0.000000000000000000, 0.000000000000000000, -1.000000000000000000 ) ) ;
#23959=DIRECTION ( 'NONE',  ( 0.5735764363510554853, 0.8191520442889852482, 0.000000000000000000 ) ) ;
#24024=DIRECTION ( 'NONE',  ( -1.000000000000000000, -1.224606353822377258E-16, -0.000000000000000000 ) ) ;
#24040=LINE ( 'NONE', #89280, #4539 ) ;
#24046=DIRECTION ( 'NONE',  ( 0.000000000000000000, 1.000000000000000000, 0.000000000000000000 ) ) ;
#24057=EDGE_CURVE ( 'NONE', #82194, #60462, #90740, .T. ) ;
#24068=AXIS2_PLACEMENT_3D ( 'NONE', #26662, #92952, #51950 ) ;
#24088=DIRECTION ( 'NONE',  ( 0.000000000000000000, -1.000000000000000000, 0.000000000000000000 ) ) ;
#24153=ORIENTED_EDGE ( 'NONE', *, *, #84683, .F. ) ;
#24175=DIRECTION ( 'NONE',  ( 0.000000000000000000, 1.000000000000000000, 0.000000000000000000 ) ) ;
#24234=FACE_OUTER_BOUND ( 'NONE', #90721, .T. ) ;
#24245=ORIENTED_EDGE ( 'NONE', *, *, #51210, .T. ) ;
#24268=VERTEX_POINT ( 'NONE', #93406 ) ;
#24314=DIRECTION ( 'NONE',  ( 0.000000000000000000, 0.000000000000000000, -1.000000000000000000 ) ) ;
#24317=FACE_OUTER_BOUND ( 'NONE', #92576, .T. ) ;
#24379=VECTOR ( 'NONE', #50052, 1000.000000000000000 ) ;
#24394=CARTESIAN_POINT ( 'NONE',  ( 0.06809871960542752956, 7.710219529346609590, -2.645508037661881584 ) ) ;
#24408=DIRECTION ( 'NONE',  ( -1.000000000000000000, -0.000000000000000000, -0.000000000000000000 ) ) ;
#24428=CIRCLE ( 'NONE', #53640, 4.172000000000009479 ) ;
#24434=CYLINDRICAL_SURFACE ( 'NONE', #68215, 5.000000000000000888 ) ;
#24438=FACE_OUTER_BOUND ( 'NONE', #16397, .T. ) ;
#24463=AXIS2_PLACEMENT_3D ( 'NONE', #36807, #21164, #79344 ) ;
#24497=EDGE_CURVE ( 'NONE', #104741, #18574, #59193, .T. ) ;
#24508=ORIENTED_EDGE ( 'NONE', *, *, #16300, .F. ) ;
#24514=CARTESIAN_POINT ( 'NONE',  ( 83.28888888888889142, 1.023464760207051730E-14, 0.000000000000000000 ) ) ;
#24605=CARTESIAN_POINT ( 'NONE',  ( 94.26467260280679739, 1.016364837396684119E-14, 0.000000000000000000 ) ) ;
#24606=AXIS2_PLACEMENT_3D ( 'NONE', #59438, #92304, #19006 ) ;
#24624=AXIS2_PLACEMENT_3D ( 'NONE', #33343, #9027, #74821 ) ;
#24634=LINE ( 'NONE', #58020, #79424 ) ;
#24686=ORIENTED_EDGE ( 'NONE', *, *, #10150, .T. ) ;
#24701=CIRCLE ( 'NONE', #103891, 8.000000000000000000 ) ;
#24725=DIRECTION ( 'NONE',  ( -1.000000000000000000, -0.000000000000000000, -0.000000000000000000 ) ) ;
#24740=CIRCLE ( 'NONE', #491, 5.000000000000011546 ) ;
#24747=CONICAL_SURFACE ( 'NONE', #60932, 4.172000000000009479, 0.9599310885968813656 ) ;
#24749=ADVANCED_FACE ( 'NONE', ( #49754 ), #27136, .T. ) ;
#24828=ADVANCED_FACE ( 'NONE', ( #78281 ), #37337, .T. ) ;
#24844=VERTEX_POINT ( 'NONE', #70196 ) ;
#24892=EDGE_CURVE ( 'NONE', #49616, #76580, #67422, .T. ) ;
#24970=AXIS2_PLACEMENT_3D ( 'NONE', #57223, #82581, #26518 ) ;
#24981=CARTESIAN_POINT ( 'NONE',  ( 0.4964154566687888903, -8.859816792613642633, 0.6543471694412403838 ) ) ;
#24985=FACE_OUTER_BOUND ( 'NONE', #1707, .T. ) ;
#24987=( NAMED_UNIT ( * ) PLANE_ANGLE_UNIT ( ) SI_UNIT ( $, .RADIAN. ) );
#24998=DIRECTION ( 'NONE',  ( -0.000000000000000000, 0.5000000000000008882, 0.8660254037844381525 ) ) ;
#25008=EDGE_LOOP ( 'NONE', ( #91816, #30078, #82145, #34902, #33532 ) ) ;
#25050=VERTEX_POINT ( 'NONE', #33630 ) ;
#25070=CARTESIAN_POINT ( 'NONE',  ( 0.01678220608715748352, 0.7854258608507237449, 7.999999999999998224 ) ) ;
#25085=ADVANCED_FACE ( 'NONE', ( #33111 ), #50315, .T. ) ;
#25116=CIRCLE ( 'NONE', #105990, 5.000000000000011546 ) ;
#25119=AXIS2_PLACEMENT_3D ( 'NONE', #36381, #85971, #29341 ) ;
#25136=EDGE_CURVE ( 'NONE', #59923, #74667, #92360, .T. ) ;
#25175=CARTESIAN_POINT ( 'NONE',  ( 93.97977184163765685, 1.030564683017419500E-14, 0.000000000000000000 ) ) ;
#25230=ORIENTED_EDGE ( 'NONE', *, *, #85485, .T. ) ;
#25246=ORIENTED_EDGE ( 'NONE', *, *, #68108, .T. ) ;
#25257=VECTOR ( 'NONE', #97251, 1000.000000000000000 ) ;
#25261=FACE_OUTER_BOUND ( 'NONE', #13719, .T. ) ;
#25334=DIRECTION ( 'NONE',  ( -1.000000000000000000, -1.224606353822377258E-16, -0.000000000000000000 ) ) ;
#25364=EDGE_CURVE ( 'NONE', #55179, #15045, #52436, .T. ) ;
#25366=AXIS2_PLACEMENT_3D ( 'NONE', #83224, #68664, #43305 ) ;
#25372=CARTESIAN_POINT ( 'NONE',  ( 5.799999999999999822, -9.237604307034013473, 1.734723475976807094E-15 ) ) ;
#25395=CONICAL_SURFACE ( 'NONE', #97637, 5.000000000000010658, 0.9599310885968697082 ) ;
#25411=DIRECTION ( 'NONE',  ( 1.000000000000000000, 1.224606353822377258E-16, 0.000000000000000000 ) ) ;
#25420=AXIS2_PLACEMENT_3D ( 'NONE', #24514, #6154, #8280 ) ;
#25424=DIRECTION ( 'NONE',  ( -1.000000000000000000, -0.000000000000000000, -0.000000000000000000 ) ) ;
#25444=CIRCLE ( 'NONE', #21972, 8.000000000000000000 ) ;
#25453=DIRECTION ( 'NONE',  ( -0.5735764363510461594, 0.8191520442889916875, 1.003171929053524870E-16 ) ) ;
#25484=DIRECTION ( 'NONE',  ( -1.000000000000000000, -0.000000000000000000, -0.000000000000000000 ) ) ;
#25492=CARTESIAN_POINT ( 'NONE',  ( 99.75754961941544252, 5.000000000000021316, 0.000000000000000000 ) ) ;
#25502=DIRECTION ( 'NONE',  ( 0.000000000000000000, -1.000000000000000000, 0.000000000000000000 ) ) ;
#25519=AXIS2_PLACEMENT_3D ( 'NONE', #16911, #82694, #41707 ) ;
#25542=AXIS2_PLACEMENT_3D ( 'NONE', #66020, #65499, #66553 ) ;
#25548=LINE ( 'NONE', #58407, #38452 ) ;
#25549=ORIENTED_EDGE ( 'NONE', *, *, #71667, .T. ) ;
#25553=EDGE_CURVE ( 'NONE', #7953, #49541, #18407, .T. ) ;
#25582=DIRECTION ( 'NONE',  ( 0.000000000000000000, -1.000000000000000000, 0.000000000000000000 ) ) ;
#25585=DIRECTION ( 'NONE',  ( -1.000000000000000000, -0.000000000000000000, -0.000000000000000000 ) ) ;
#25592=ORIENTED_EDGE ( 'NONE', *, *, #5535, .T. ) ;
#25636=ADVANCED_FACE ( 'NONE', ( #10260 ), #68366, .T. ) ;
#25702=DIRECTION ( 'NONE',  ( -0.5735764363510461594, 0.8191520442889916875, 1.003171929053524870E-16 ) ) ;
#25709=DIRECTION ( 'NONE',  ( -1.000000000000000000, -0.000000000000000000, -0.000000000000000000 ) ) ;
#25714=EDGE_CURVE ( 'NONE', #98133, #76468, #42474, .T. ) ;
#25752=CARTESIAN_POINT ( 'NONE',  ( 101.4868948250290259, 1.016364837396684119E-14, 0.000000000000000000 ) ) ;
#25779=CARTESIAN_POINT ( 'NONE',  ( 86.17777777777776294, -4.171999999999998820, 0.000000000000000000 ) ) ;
#25803=ORIENTED_EDGE ( 'NONE', *, *, #511, .F. ) ;
#25819=CARTESIAN_POINT ( 'NONE',  ( 0.000000000000000000, 0.000000000000000000, 0.000000000000000000 ) ) ;
#25846=CIRCLE ( 'NONE', #87784, 5.000000000000011546 ) ;
#25889=CARTESIAN_POINT ( 'NONE',  ( 94.26467260280679739, 5.000000000000023093, 6.123233995736781074E-16 ) ) ;
#25896=FACE_OUTER_BOUND ( 'NONE', #80628, .T. ) ;
#25937=DIRECTION ( 'NONE',  ( -1.000000000000000000, -1.224606353822377258E-16, -0.000000000000000000 ) ) ;
#25960=ORIENTED_EDGE ( 'NONE', *, *, #68960, .F. ) ;
#25984=ORIENTED_EDGE ( 'NONE', *, *, #59518, .T. ) ;
#25991=ORIENTED_EDGE ( 'NONE', *, *, #66239, .T. ) ;
#26023=DIRECTION ( 'NONE',  ( 0.000000000000000000, -1.000000000000000000, 0.000000000000000000 ) ) ;
#26034=ORIENTED_EDGE ( 'NONE', *, *, #75060, .T. ) ;
#26055=ORIENTED_EDGE ( 'NONE', *, *, #64959, .T. ) ;
#26056=FACE_OUTER_BOUND ( 'NONE', #76411, .T. ) ;
#26057=CARTESIAN_POINT ( 'NONE',  ( 87.62222222222222001, -4.171999999999998820, 0.000000000000000000 ) ) ;
#26089=ORIENTED_EDGE ( 'NONE', *, *, #426, .F. ) ;
#26118=ADVANCED_FACE ( 'NONE', ( #24234 ), #60837, .F. ) ;
#26133=ORIENTED_EDGE ( 'NONE', *, *, #100184, .T. ) ;
#26159=CARTESIAN_POINT ( 'NONE',  ( 0.08285530294364830406, 1.570896314703518870, 8.000000000000000000 ) ) ;
#26165=ORIENTED_EDGE ( 'NONE', *, *, #48532, .T. ) ;
#26171=DIRECTION ( 'NONE',  ( 0.000000000000000000, -1.000000000000000000, 0.000000000000000000 ) ) ;
#26255=EDGE_LOOP ( 'NONE', ( #19404, #5386, #69988 ) ) ;
#26256=CARTESIAN_POINT ( 'NONE',  ( 102.0666666666666629, -4.171999999999998820, 0.000000000000000000 ) ) ;
#26265=ORIENTED_EDGE ( 'NONE', *, *, #73138, .F. ) ;
#26285=CARTESIAN_POINT ( 'NONE',  ( 0.000000000000000000, 0.000000000000000000, 0.000000000000000000 ) ) ;
#26292=ORIENTED_EDGE ( 'NONE', *, *, #89928, .T. ) ;
#26303=ADVANCED_FACE ( 'NONE', ( #78585 ), #39118, .T. ) ;
#26316=ORIENTED_EDGE ( 'NONE', *, *, #65872, .F. ) ;
#26405=CARTESIAN_POINT ( 'NONE',  ( 105.5353273971932140, 1.030564683017419500E-14, 0.000000000000000000 ) ) ;
#26518=DIRECTION ( 'NONE',  ( 0.000000000000000000, 0.000000000000000000, 1.000000000000000000 ) ) ;
#26550=CARTESIAN_POINT ( 'NONE',  ( 98.59800593614012598, 1.016364837396684119E-14, 0.000000000000000000 ) ) ;
#26592=CARTESIAN_POINT ( 'NONE',  ( 101.2019940638598854, 1.030564683017419500E-14, 0.000000000000000000 ) ) ;
#26628=CARTESIAN_POINT ( 'NONE',  ( 97.73333333333333428, 4.172000000000019249, 0.000000000000000000 ) ) ;
#26634=DIRECTION ( 'NONE',  ( 0.5735764363510557073, -0.8191520442889850262, 1.003171929053516612E-16 ) ) ;
#26641=FACE_OUTER_BOUND ( 'NONE', #100656, .T. ) ;
#26662=CARTESIAN_POINT ( 'NONE',  ( 0.000000000000000000, 0.000000000000000000, 0.000000000000000000 ) ) ;
#26686=CARTESIAN_POINT ( 'NONE',  ( 83.86866073052654258, -5.000000000000000888, 6.123233995736779101E-16 ) ) ;
#26709=ORIENTED_EDGE ( 'NONE', *, *, #45674, .T. ) ;
#26735=( NAMED_UNIT ( * ) SI_UNIT ( $, .STERADIAN. ) SOLID_ANGLE_UNIT ( ) );
#26742=DIRECTION ( 'NONE',  ( -1.000000000000000000, -1.224606353822377258E-16, -0.000000000000000000 ) ) ;
#26756=AXIS2_PLACEMENT_3D ( 'NONE', #71898, #7913, #15483 ) ;
#26845=AXIS2_PLACEMENT_3D ( 'NONE', #10447, #57930, #68164 ) ;
#26871=DIRECTION ( 'NONE',  ( -1.000000000000000000, -0.000000000000000000, -0.000000000000000000 ) ) ;
#26931=ORIENTED_EDGE ( 'NONE', *, *, #39644, .T. ) ;
#26985=EDGE_LOOP ( 'NONE', ( #75991, #36864, #85301, #75184, #4530 ) ) ;
#26999=CARTESIAN_POINT ( 'NONE',  ( 101.2019940638598854, 5.000000000000021316, 0.000000000000000000 ) ) ;
#27007=ORIENTED_EDGE ( 'NONE', *, *, #28315, .T. ) ;
#27054=EDGE_CURVE ( 'NONE', #17355, #57657, #39270, .T. ) ;
#27097=DIRECTION ( 'NONE',  ( 1.000000000000000000, 1.224606353822377258E-16, 0.000000000000000000 ) ) ;
#27103=ORIENTED_EDGE ( 'NONE', *, *, #60617, .T. ) ;
#27104=LINE ( 'NONE', #92853, #92383 ) ;
#27107=CARTESIAN_POINT ( 'NONE',  ( 90.51111111111110574, 1.023464760207051730E-14, 0.000000000000000000 ) ) ;
#27134=CARTESIAN_POINT ( 'NONE',  ( 5.799999999999999822, 0.000000000000000000, 0.000000000000000000 ) ) ;
#27136=CONICAL_SURFACE ( 'NONE', #40873, 5.000000000000010658, 0.9599310885968697082 ) ;
#27155=CIRCLE ( 'NONE', #61559, 5.000000000000010658 ) ;
#27160=FACE_OUTER_BOUND ( 'NONE', #78305, .T. ) ;
#27178=VERTEX_POINT ( 'NONE', #10154 ) ;
#27205=VECTOR ( 'NONE', #35004, 1000.000000000000000 ) ;
#27238=DIRECTION ( 'NONE',  ( -1.000000000000000000, -1.224606353822377258E-16, -0.000000000000000000 ) ) ;
#27266=VECTOR ( 'NONE', #75861, 999.9999999999998863 ) ;
#27273=PRESENTATION_STYLE_ASSIGNMENT (( #59609 ) ) ;
#27321=ORIENTED_EDGE ( 'NONE', *, *, #39572, .F. ) ;
#27329=EDGE_CURVE ( 'NONE', #45219, #78511, #73798, .T. ) ;
#27334=ORIENTED_EDGE ( 'NONE', *, *, #102416, .T. ) ;
#27357=ORIENTED_EDGE ( 'NONE', *, *, #73329, .T. ) ;
#27395=AXIS2_PLACEMENT_3D ( 'NONE', #71809, #54551, #29808 ) ;
#27398=CARTESIAN_POINT ( 'NONE',  ( 5.799999999999999822, 0.000000000000000000, 0.000000000000000000 ) ) ;
#27401=EDGE_CURVE ( 'NONE', #101774, #93942, #55261, .T. ) ;
#27434=ORIENTED_EDGE ( 'NONE', *, *, #39263, .F. ) ;
#27438=DIRECTION ( 'NONE',  ( 0.000000000000000000, 1.000000000000000000, -3.755786496842903988E-16 ) ) ;
#27446=EDGE_CURVE ( 'NONE', #82852, #63286, #13520, .T. ) ;
#27453=DIRECTION ( 'NONE',  ( 1.000000000000000000, 0.000000000000000000, 0.000000000000000000 ) ) ;
#27561=DIRECTION ( 'NONE',  ( 0.000000000000000000, -1.000000000000000000, 0.000000000000000000 ) ) ;
#27573=VECTOR ( 'NONE', #7219, 1000.000000000000000 ) ;
#27644=DIRECTION ( 'NONE',  ( 1.000000000000000000, 0.000000000000000000, -0.000000000000000000 ) ) ;
#27652=CARTESIAN_POINT ( 'NONE',  ( 102.6464385083043283, -5.000000000000000888, 6.123233995736779101E-16 ) ) ;
#27669=DIRECTION ( 'NONE',  ( -1.000000000000000000, -1.224606353822377258E-16, -0.000000000000000000 ) ) ;
#27734=DIRECTION ( 'NONE',  ( -1.000000000000000000, -1.224606353822377258E-16, -0.000000000000000000 ) ) ;
#27761=ORIENTED_EDGE ( 'NONE', *, *, #95708, .T. ) ;
#27827=CARTESIAN_POINT ( 'NONE',  ( 6.400000000000000355, 9.237604307034018802, 0.000000000000000000 ) ) ;
#27863=DIRECTION ( 'NONE',  ( -1.000000000000000000, -0.000000000000000000, -0.000000000000000000 ) ) ;
#27866=CYLINDRICAL_SURFACE ( 'NONE', #101766, 5.000000000000000888 ) ;
#27874=CARTESIAN_POINT ( 'NONE',  ( 83.86866073052654258, 6.123233995736568081E-16, -5.000000000000011546 ) ) ;
#27889=LINE ( 'NONE', #84484, #81879 ) ;
#27916=ORIENTED_EDGE ( 'NONE', *, *, #81192, .T. ) ;
#27969=ORIENTED_EDGE ( 'NONE', *, *, #27446, .F. ) ;
#28024=VERTEX_POINT ( 'NONE', #78236 ) ;
#28025=FACE_OUTER_BOUND ( 'NONE', #90621, .T. ) ;
#28054=ORIENTED_EDGE ( 'NONE', *, *, #60865, .T. ) ;
#28060=EDGE_CURVE ( 'NONE', #64539, #77725, #71364, .T. ) ;
#28069=EDGE_CURVE ( 'NONE', #87999, #69327, #52420, .T. ) ;
#28141=DIRECTION ( 'NONE',  ( -1.000000000000000000, -1.224606353822377258E-16, -0.000000000000000000 ) ) ;
#28178=DIRECTION ( 'NONE',  ( -1.000000000000000000, -1.224606353822377258E-16, -0.000000000000000000 ) ) ;
#28186=FACE_OUTER_BOUND ( 'NONE', #2540, .T. ) ;
#28266=AXIS2_PLACEMENT_3D ( 'NONE', #90612, #15650, #16183 ) ;
#28315=EDGE_CURVE ( 'NONE', #44644, #100880, #75149, .T. ) ;
#28399=ORIENTED_EDGE ( 'NONE', *, *, #97680, .T. ) ;
#28424=ORIENTED_EDGE ( 'NONE', *, *, #72187, .F. ) ;
#28444=CARTESIAN_POINT ( 'NONE',  ( 98.59800593614012598, -2.002967142162725287E-29, 5.000000000000011546 ) ) ;
#28489=ORIENTED_EDGE ( 'NONE', *, *, #6415, .T. ) ;
#28495=ORIENTED_EDGE ( 'NONE', *, *, #86457, .F. ) ;
#28519=AXIS2_PLACEMENT_3D ( 'NONE', #30196, #62556, #38813 ) ;
#28555=AXIS2_PLACEMENT_3D ( 'NONE', #39045, #96222, #94086 ) ;
#28563=CARTESIAN_POINT ( 'NONE',  ( -3.901433755053307362E-15, 6.534749472788146107, 4.681481898397000130 ) ) ;
#28602=VERTEX_POINT ( 'NONE', #94138 ) ;
#28603=CARTESIAN_POINT ( 'NONE',  ( 84.15356149169568312, -5.000000000000000000, 0.000000000000000000 ) ) ;
#28609=CARTESIAN_POINT ( 'NONE',  ( 92.53532739719321398, -5.000000000000000000, 6.123233995736778115E-16 ) ) ;
#28617=EDGE_CURVE ( 'NONE', #76468, #98133, #85498, .T. ) ;
#28629=CARTESIAN_POINT ( 'NONE',  ( 97.73333333333333428, 1.023464760207051730E-14, 0.000000000000000000 ) ) ;
#28641=CARTESIAN_POINT ( 'NONE',  ( 0.1306530452038104362, 7.903938623646867612, 2.309976723937611887 ) ) ;
#28693=VERTEX_POINT ( 'NONE', #105412 ) ;
#28702=CARTESIAN_POINT ( 'NONE',  ( 97.73333333333333428, -4.171999999999998820, 0.000000000000000000 ) ) ;
#28717=CARTESIAN_POINT ( 'NONE',  ( 0.000000000000000000, 0.000000000000000000, 0.000000000000000000 ) ) ;
#28746=AXIS2_PLACEMENT_3D ( 'NONE', #36188, #85221, #43696 ) ;
#28792=AXIS2_PLACEMENT_3D ( 'NONE', #83775, #16396, #99419 ) ;
#28885=DIRECTION ( 'NONE',  ( -1.000000000000000000, -1.224606353822377258E-16, -0.000000000000000000 ) ) ;
#28895=DIRECTION ( 'NONE',  ( -1.000000000000000000, -0.000000000000000000, -0.000000000000000000 ) ) ;
#28935=CARTESIAN_POINT ( 'NONE',  ( 101.4868948250290259, 1.016364837396684119E-14, 0.000000000000000000 ) ) ;
#28970=EDGE_LOOP ( 'NONE', ( #4212, #721, #837, #80820, #10524 ) ) ;
#28983=DIRECTION ( 'NONE',  ( -1.000000000000000000, -0.000000000000000000, -0.000000000000000000 ) ) ;
#29002=EDGE_CURVE ( 'NONE', #49140, #10334, #106249, .T. ) ;
#29003=EDGE_CURVE ( 'NONE', #25050, #87544, #76943, .T. ) ;
#29045=DIRECTION ( 'NONE',  ( -1.000000000000000000, -1.224606353822377258E-16, -0.000000000000000000 ) ) ;
#29068=CIRCLE ( 'NONE', #72051, 5.000000000000010658 ) ;
#29072=ADVANCED_FACE ( 'NONE', ( #98887 ), #57984, .T. ) ;
#29148=ORIENTED_EDGE ( 'NONE', *, *, #14456, .F. ) ;
#29173=CIRCLE ( 'NONE', #94596, 5.000000000000011546 ) ;
#29188=CARTESIAN_POINT ( 'NONE',  ( -3.935526831180291373E-15, 7.124194613927623543, 3.660532965668822136 ) ) ;
#29192=CIRCLE ( 'NONE', #51530, 4.172000000000009479 ) ;
#29199=EDGE_LOOP ( 'NONE', ( #53468, #69596, #79367, #80091, #41635, #34774 ) ) ;
#29215=DIRECTION ( 'NONE',  ( 0.000000000000000000, -1.000000000000000000, 0.000000000000000000 ) ) ;
#29282=CARTESIAN_POINT ( 'NONE',  ( 104.0908829527487711, 1.030564683017419500E-14, 0.000000000000000000 ) ) ;
#29337=VECTOR ( 'NONE', #9233, 1000.000000000000000 ) ;
#29341=DIRECTION ( 'NONE',  ( 0.000000000000000000, -1.000000000000000000, 0.000000000000000000 ) ) ;
#29370=EDGE_CURVE ( 'NONE', #92586, #89220, #7622, .T. ) ;
#29371=ORIENTED_EDGE ( 'NONE', *, *, #54216, .F. ) ;
#29415=DIRECTION ( 'NONE',  ( -1.000000000000000000, -1.224606353822377258E-16, -0.000000000000000000 ) ) ;
#29428=DIRECTION ( 'NONE',  ( 0.000000000000000000, -1.000000000000000000, 0.000000000000000000 ) ) ;
#29431=ORIENTED_EDGE ( 'NONE', *, *, #10125, .T. ) ;
#29432=VECTOR ( 'NONE', #81995, 1000.000000000000000 ) ;
#29457=DIRECTION ( 'NONE',  ( -1.000000000000000000, -0.000000000000000000, -0.000000000000000000 ) ) ;
#29497=AXIS2_PLACEMENT_3D ( 'NONE', #39947, #74416, #64752 ) ;
#29516=AXIS2_PLACEMENT_3D ( 'NONE', #10761, #78169, #60942 ) ;
#29591=LINE ( 'NONE', #51690, #17201 ) ;
#29629=CARTESIAN_POINT ( 'NONE',  ( 0.06809871960542691893, 6.146186931204407067, 5.354491962338125077 ) ) ;
#29639=VERTEX_POINT ( 'NONE', #105156 ) ;
#29651=CIRCLE ( 'NONE', #69201, 5.000000000000011546 ) ;
#29672=ORIENTED_EDGE ( 'NONE', *, *, #47917, .T. ) ;
#29706=EDGE_CURVE ( 'NONE', #71316, #43097, #39159, .T. ) ;
#29728=AXIS2_PLACEMENT_3D ( 'NONE', #77024, #36087, #3143 ) ;
#29734=DIRECTION ( 'NONE',  ( -1.000000000000000000, -1.224606353822377258E-16, -0.000000000000000000 ) ) ;
#29763=EDGE_LOOP ( 'NONE', ( #39878, #102042, #71050, #54537, #16634 ) ) ;
#29770=DIRECTION ( 'NONE',  ( 0.000000000000000000, 0.000000000000000000, 1.000000000000000000 ) ) ;
#29808=DIRECTION ( 'NONE',  ( 0.000000000000000000, -1.000000000000000000, 0.000000000000000000 ) ) ;
#29844=DIRECTION ( 'NONE',  ( -0.000000000000000000, 1.000000000000000000, 1.877893248421449282E-16 ) ) ;
#29916=EDGE_CURVE ( 'NONE', #9396, #102684, #84018, .T. ) ;
#29971=DIRECTION ( 'NONE',  ( -1.000000000000000000, -1.224606353822377258E-16, -0.000000000000000000 ) ) ;
#29998=DIRECTION ( 'NONE',  ( 0.000000000000000000, -1.000000000000000000, 0.000000000000000000 ) ) ;
#30022=CIRCLE ( 'NONE', #90267, 5.000000000000011546 ) ;
#30027=CARTESIAN_POINT ( 'NONE',  ( 0.000000000000000000, 0.000000000000000000, 0.000000000000000000 ) ) ;
#30067=LINE ( 'NONE', #14899, #104083 ) ;
#30073=LINE ( 'NONE', #95320, #32024 ) ;
#30078=ORIENTED_EDGE ( 'NONE', *, *, #3341, .T. ) ;
#30081=ORIENTED_EDGE ( 'NONE', *, *, #89092, .F. ) ;
#30121=EDGE_CURVE ( 'NONE', #69327, #86608, #35871, .T. ) ;
#30141=ORIENTED_EDGE ( 'NONE', *, *, #592, .T. ) ;
#30151=DIRECTION ( 'NONE',  ( 0.000000000000000000, -1.000000000000000000, 0.000000000000000000 ) ) ;
#30196=CARTESIAN_POINT ( 'NONE',  ( 88.20199406385988539, 1.030564683017419500E-14, 0.000000000000000000 ) ) ;
#30313=LINE ( 'NONE', #97139, #65349 ) ;
#30358=CARTESIAN_POINT ( 'NONE',  ( 0.000000000000000000, 0.000000000000000000, 0.000000000000000000 ) ) ;
#30362=LINE ( 'NONE', #94570, #36351 ) ;
#30387=DIRECTION ( 'NONE',  ( 0.000000000000000000, -1.000000000000000000, -1.877893248421449282E-16 ) ) ;
#30394=EDGE_CURVE ( 'NONE', #57657, #3401, #37637, .T. ) ;
#30424=DIRECTION ( 'NONE',  ( 0.000000000000000000, 0.000000000000000000, 1.000000000000000000 ) ) ;
#30465=VERTEX_POINT ( 'NONE', #54469 ) ;
#30488=CARTESIAN_POINT ( 'NONE',  ( 94.84444444444443434, 1.023464760207051730E-14, 0.000000000000000000 ) ) ;
#30522=DIRECTION ( 'NONE',  ( 0.5735764363510554853, 0.8191520442889852482, 0.000000000000000000 ) ) ;
#30531=ORIENTED_EDGE ( 'NONE', *, *, #32373, .F. ) ;
#30547=ORIENTED_EDGE ( 'NONE', *, *, #106259, .T. ) ;
#30635=DIRECTION ( 'NONE',  ( 0.000000000000000000, -1.000000000000000000, 0.000000000000000000 ) ) ;
#30693=AXIS2_PLACEMENT_3D ( 'NONE', #85957, #21236, #36886 ) ;
#30751=ORIENTED_EDGE ( 'NONE', *, *, #70267, .F. ) ;
#30782=DIRECTION ( 'NONE',  ( 0.000000000000000000, -1.000000000000000000, 0.000000000000000000 ) ) ;
#30832=DIRECTION ( 'NONE',  ( -1.000000000000000000, -1.224606353822377258E-16, -0.000000000000000000 ) ) ;
#30868=LINE ( 'NONE', #62169, #63469 ) ;
#30883=CARTESIAN_POINT ( 'NONE',  ( 0.1306530452038089374, 5.952467836904150822, -5.690023276062396107 ) ) ;
#30935=CARTESIAN_POINT ( 'NONE',  ( 0.000000000000000000, 9.237604307034020579, -1.850927914596627675E-15 ) ) ;
#30953=ORIENTED_EDGE ( 'NONE', *, *, #37360, .F. ) ;
#30963=CARTESIAN_POINT ( 'NONE',  ( 0.000000000000000000, -6.928203230275504332, 4.000000000000007105 ) ) ;
#30966=ORIENTED_EDGE ( 'NONE', *, *, #64959, .F. ) ;
#31052=ORIENTED_EDGE ( 'NONE', *, *, #2102, .T. ) ;
#31064=CARTESIAN_POINT ( 'NONE',  ( 80.40000000000000568, 4.172000000000019249, 0.000000000000000000 ) ) ;
#31109=CARTESIAN_POINT ( 'NONE',  ( 93.97977184163765685, 1.030564683017419500E-14, 0.000000000000000000 ) ) ;
#31113=DIRECTION ( 'NONE',  ( -1.000000000000000000, -1.224606353822377258E-16, -0.000000000000000000 ) ) ;
#31136=ORIENTED_EDGE ( 'NONE', *, *, #73474, .F. ) ;
#31158=DIRECTION ( 'NONE',  ( 0.000000000000000000, -1.000000000000000000, 0.000000000000000000 ) ) ;
#31218=AXIS2_PLACEMENT_3D ( 'NONE', #101334, #100258, #52773 ) ;
#31275=ORIENTED_EDGE ( 'NONE', *, *, #81833, .F. ) ;
#31356=EDGE_CURVE ( 'NONE', #64937, #28602, #98747, .T. ) ;
#31362=ORIENTED_EDGE ( 'NONE', *, *, #13042, .F. ) ;
#31386=EDGE_CURVE ( 'NONE', #15028, #54088, #80686, .T. ) ;
#31415=CARTESIAN_POINT ( 'NONE',  ( 0.01688885742776662438, 6.535341423375591319, -4.680456609903973941 ) ) ;
#31430=DIRECTION ( 'NONE',  ( 0.000000000000000000, -1.000000000000000000, 0.000000000000000000 ) ) ;
#31444=VERTEX_POINT ( 'NONE', #52335 ) ;
#31497=DIRECTION ( 'NONE',  ( 0.5735764363510557073, -0.8191520442889850262, 1.003171929053516612E-16 ) ) ;
#31541=ORIENTED_EDGE ( 'NONE', *, *, #99147, .F. ) ;
#31615=EDGE_LOOP ( 'NONE', ( #68307, #94407, #55805, #20426, #58670 ) ) ;
#31691=CARTESIAN_POINT ( 'NONE',  ( 85.59800593614014019, 1.016364837396684119E-14, 0.000000000000000000 ) ) ;
#31708=ORIENTED_EDGE ( 'NONE', *, *, #44623, .T. ) ;
#31723=CARTESIAN_POINT ( 'NONE',  ( 101.2019940638598854, 6.123233995736568081E-16, -5.000000000000011546 ) ) ;
#31777=ORIENTED_EDGE ( 'NONE', *, *, #67340, .F. ) ;
#31850=EDGE_CURVE ( 'NONE', #67654, #53206, #29173, .T. ) ;
#31897=CONICAL_SURFACE ( 'NONE', #83532, 5.000000000000010658, 0.9599310885968697082 ) ;
#31905=ORIENTED_EDGE ( 'NONE', *, *, #103451, .T. ) ;
#31981=CARTESIAN_POINT ( 'NONE',  ( 0.4964154566687623005, -4.996589667937438861, -7.345652830558661250 ) ) ;
#31984=ORIENTED_EDGE ( 'NONE', *, *, #42330, .T. ) ;
#31993=DIRECTION ( 'NONE',  ( 0.000000000000000000, -1.000000000000000000, 0.000000000000000000 ) ) ;
#32014=CARTESIAN_POINT ( 'NONE',  ( 5.799999999999999822, 4.618802153517005848, 7.999999999999996447 ) ) ;
#32024=VECTOR ( 'NONE', #86714, 1000.000000000000000 ) ;
#32026=LINE ( 'NONE', #90242, #62620 ) ;
#32037=CIRCLE ( 'NONE', #66428, 5.000000000000010658 ) ;
#32044=AXIS2_PLACEMENT_3D ( 'NONE', #70298, #77323, #3436 ) ;
#32056=ADVANCED_FACE ( 'NONE', ( #2335 ), #60086, .T. ) ;
#32060=LINE ( 'NONE', #2170, #27573 ) ;
#32234=ORIENTED_EDGE ( 'NONE', *, *, #9459, .F. ) ;
#32235=ADVANCED_FACE ( 'NONE', ( #69232 ), #46006, .T. ) ;
#32237=VERTEX_POINT ( 'NONE', #103699 ) ;
#32284=DIRECTION ( 'NONE',  ( 0.000000000000000000, 0.000000000000000000, 1.000000000000000000 ) ) ;
#32294=CIRCLE ( 'NONE', #51197, 4.172000000000009479 ) ;
#32336=ORIENTED_EDGE ( 'NONE', *, *, #70864, .T. ) ;
#32350=AXIS2_PLACEMENT_3D ( 'NONE', #67846, #76998, #85642 ) ;
#32373=EDGE_CURVE ( 'NONE', #72949, #105278, #18920, .T. ) ;
#32390=ORIENTED_EDGE ( 'NONE', *, *, #3212, .T. ) ;
#32396=CARTESIAN_POINT ( 'NONE',  ( 0.000000000000000000, 0.000000000000000000, 0.000000000000000000 ) ) ;
#32424=CARTESIAN_POINT ( 'NONE',  ( 0.000000000000000000, 0.000000000000000000, 5.000000000000000888 ) ) ;
#32463=CARTESIAN_POINT ( 'NONE',  ( 89.64643850830432825, 1.030564683017419500E-14, 0.000000000000000000 ) ) ;
#32478=ORIENTED_EDGE ( 'NONE', *, *, #21150, .T. ) ;
#32493=CARTESIAN_POINT ( 'NONE',  ( 81.26467260280679739, 5.000000000000023093, 6.123233995736781074E-16 ) ) ;
#32501=DIRECTION ( 'NONE',  ( 1.000000000000000000, 0.000000000000000000, 0.000000000000000000 ) ) ;
#32558=ORIENTED_EDGE ( 'NONE', *, *, #5285, .T. ) ;
#32583=AXIS2_PLACEMENT_3D ( 'NONE', #7038, #39954, #72827 ) ;
#32644=EDGE_LOOP ( 'NONE', ( #13220, #31984, #10219, #67468, #65262, #27969 ) ) ;
#32666=FACE_OUTER_BOUND ( 'NONE', #29763, .T. ) ;
#32685=CARTESIAN_POINT ( 'NONE',  ( 103.5111111111111057, 1.023464760207051730E-14, 0.000000000000000000 ) ) ;
#32687=ADVANCED_FACE ( 'NONE', ( #22146 ), #10327, .T. ) ;
#32711=LINE ( 'NONE', #97943, #106137 ) ;
#32736=CARTESIAN_POINT ( 'NONE',  ( 102.6464385083043283, 5.000000000000020428, 0.000000000000000000 ) ) ;
#32742=ORIENTED_EDGE ( 'NONE', *, *, #6380, .T. ) ;
#32770=VERTEX_POINT ( 'NONE', #55920 ) ;
#32777=ADVANCED_FACE ( 'NONE', ( #23619 ), #1700, .T. ) ;
#32814=ORIENTED_EDGE ( 'NONE', *, *, #16480, .F. ) ;
#32817=FACE_OUTER_BOUND ( 'NONE', #63817, .T. ) ;
#32832=DIRECTION ( 'NONE',  ( 0.000000000000000000, 0.8660254037844380415, -0.5000000000000009992 ) ) ;
#32840=AXIS2_PLACEMENT_3D ( 'NONE', #82212, #73043, #98915 ) ;
#32843=EDGE_CURVE ( 'NONE', #54417, #68926, #37708, .T. ) ;
#32873=CARTESIAN_POINT ( 'NONE',  ( 95.42421628608209971, 5.000000000000021316, 0.000000000000000000 ) ) ;
#32904=ORIENTED_EDGE ( 'NONE', *, *, #45581, .F. ) ;
#32933=CONICAL_SURFACE ( 'NONE', #93191, 4.172000000000009479, 0.9599310885968813656 ) ;
#32962=CARTESIAN_POINT ( 'NONE',  ( 96.86866073052655679, 1.030564683017419500E-14, 0.000000000000000000 ) ) ;
#32965=DIRECTION ( 'NONE',  ( -1.000000000000000000, -1.224606353822377258E-16, -0.000000000000000000 ) ) ;
#33014=ADVANCED_FACE ( 'NONE', ( #38478 ), #70828, .F. ) ;
#33027=CARTESIAN_POINT ( 'NONE',  ( 5.799999999999999822, 1.502314598737159426E-15, -8.000000000000000000 ) ) ;
#33030=DIRECTION ( 'NONE',  ( -1.000000000000000000, -0.000000000000000000, -0.000000000000000000 ) ) ;
#33039=CIRCLE ( 'NONE', #91608, 5.000000000000010658 ) ;
#33086=AXIS2_PLACEMENT_3D ( 'NONE', #7241, #73027, #105937 ) ;
#33098=VERTEX_POINT ( 'NONE', #89133 ) ;
#33111=FACE_OUTER_BOUND ( 'NONE', #97077, .T. ) ;
#33133=ORIENTED_EDGE ( 'NONE', *, *, #11199, .F. ) ;
#33135=CARTESIAN_POINT ( 'NONE',  ( 101.4868948250290259, 6.123233995736582872E-16, -5.000000000000011546 ) ) ;
#33141=CARTESIAN_POINT ( 'NONE',  ( 104.0908829527487711, 1.030564683017419500E-14, 0.000000000000000000 ) ) ;
#33148=AXIS2_PLACEMENT_3D ( 'NONE', #95966, #22091, #54945 ) ;
#33155=CIRCLE ( 'NONE', #46899, 4.172000000000009479 ) ;
#33175=EDGE_LOOP ( 'NONE', ( #62795, #43582, #55590, #90601, #85007 ) ) ;
#33177=ORIENTED_EDGE ( 'NONE', *, *, #49773, .F. ) ;
#33207=DIRECTION ( 'NONE',  ( -1.000000000000000000, -1.224606353822377258E-16, -0.000000000000000000 ) ) ;
#33211=DIRECTION ( 'NONE',  ( 0.5735764363510557073, -0.8191520442889850262, 1.003171929053516612E-16 ) ) ;
#33217=DIRECTION ( 'NONE',  ( -1.000000000000000000, -1.224606353822377258E-16, -0.000000000000000000 ) ) ;
#33270=ORIENTED_EDGE ( 'NONE', *, *, #12358, .T. ) ;
#33343=CARTESIAN_POINT ( 'NONE',  ( 82.70911704725124025, 1.016364837396684119E-14, 0.000000000000000000 ) ) ;
#33344=EDGE_LOOP ( 'NONE', ( #50057, #97357, #227 ) ) ;
#33353=DIRECTION ( 'NONE',  ( -1.000000000000000000, -1.224606353822377258E-16, -0.000000000000000000 ) ) ;
#33354=FACE_OUTER_BOUND ( 'NONE', #97836, .T. ) ;
#33361=FACE_OUTER_BOUND ( 'NONE', #34617, .T. ) ;
#33374=ORIENTED_EDGE ( 'NONE', *, *, #73816, .T. ) ;
#33418=ADVANCED_FACE ( 'NONE', ( #11378 ), #84246, .T. ) ;
#33439=DIRECTION ( 'NONE',  ( 0.000000000000000000, 1.000000000000000000, 0.000000000000000000 ) ) ;
#33515=EDGE_CURVE ( 'NONE', #74576, #30465, #8390, .T. ) ;
#33517=EDGE_LOOP ( 'NONE', ( #17455, #26709, #93116, #91118, #74467, #18720 ) ) ;
#33532=ORIENTED_EDGE ( 'NONE', *, *, #18794, .F. ) ;
#33537=VERTEX_POINT ( 'NONE', #101996 ) ;
#33544=CARTESIAN_POINT ( 'NONE',  ( 102.6464385083043283, 6.123233995736568081E-16, -5.000000000000011546 ) ) ;
#33546=DIRECTION ( 'NONE',  ( 0.000000000000000000, -1.000000000000000000, 0.000000000000000000 ) ) ;
#33553=AXIS2_PLACEMENT_3D ( 'NONE', #30027, #19837, #62912 ) ;
#33556=CARTESIAN_POINT ( 'NONE',  ( 0.000000000000000000, 0.000000000000000000, 0.000000000000000000 ) ) ;
#33571=CARTESIAN_POINT ( 'NONE',  ( -3.354250471127029343E-15, -6.534749472788162983, -4.681481898396973484 ) ) ;
#33575=AXIS2_PLACEMENT_3D ( 'NONE', #37293, #38859, #63132 ) ;
#33578=DIRECTION ( 'NONE',  ( -1.000000000000000000, -0.000000000000000000, -0.000000000000000000 ) ) ;
#33605=FILL_AREA_STYLE_COLOUR ( '', #36813 ) ;
#33630=CARTESIAN_POINT ( 'NONE',  ( 98.31310517497099966, 5.000000000000020428, 0.000000000000000000 ) ) ;
#33648=CARTESIAN_POINT ( 'NONE',  ( 92.53532739719321398, 6.123233995736568081E-16, -5.000000000000011546 ) ) ;
#33689=ORIENTED_EDGE ( 'NONE', *, *, #90922, .T. ) ;
#33702=CIRCLE ( 'NONE', #28555, 5.000000000000010658 ) ;
#33725=VERTEX_POINT ( 'NONE', #61976 ) ;
#33738=AXIS2_PLACEMENT_3D ( 'NONE', #83793, #74636, #8313 ) ;
#33773=CIRCLE ( 'NONE', #95742, 5.000000000000011546 ) ;
#33785=EDGE_CURVE ( 'NONE', #86867, #36517, #6779, .T. ) ;
#33852=VERTEX_POINT ( 'NONE', #33648 ) ;
#33872=CARTESIAN_POINT ( 'NONE',  ( 94.26467260280679739, 6.123233995736582872E-16, -5.000000000000011546 ) ) ;
#33877=DIRECTION ( 'NONE',  ( -1.000000000000000000, -1.224606353822377258E-16, -0.000000000000000000 ) ) ;
#33900=CARTESIAN_POINT ( 'NONE',  ( 0.000000000000000000, 0.000000000000000000, 0.000000000000000000 ) ) ;
#33907=EDGE_CURVE ( 'NONE', #49140, #9363, #87720, .T. ) ;
#33914=DIRECTION ( 'NONE',  ( -1.000000000000000000, -1.224606353822377258E-16, -0.000000000000000000 ) ) ;
#33928=CARTESIAN_POINT ( 'NONE',  ( 82.42421628608209971, -2.002967142162725287E-29, 5.000000000000011546 ) ) ;
#33953=ORIENTED_EDGE ( 'NONE', *, *, #19524, .F. ) ;
#34012=ORIENTED_EDGE ( 'NONE', *, *, #31850, .F. ) ;
#34022=DIRECTION ( 'NONE',  ( 0.000000000000000000, -1.000000000000000000, 0.000000000000000000 ) ) ;
#34058=ORIENTED_EDGE ( 'NONE', *, *, #105684, .F. ) ;
#34070=CYLINDRICAL_SURFACE ( 'NONE', #24970, 5.000000000000000888 ) ;
#34075=ADVANCED_FACE ( 'NONE', ( #33354 ), #15476, .T. ) ;
#34106=FACE_OUTER_BOUND ( 'NONE', #21982, .T. ) ;
#34108=DIRECTION ( 'NONE',  ( -1.000000000000000000, -1.224606353822377258E-16, -0.000000000000000000 ) ) ;
#34148=ORIENTED_EDGE ( 'NONE', *, *, #59518, .F. ) ;
#34149=SURFACE_STYLE_FILL_AREA ( #66478 ) ;
#34161=ORIENTED_EDGE ( 'NONE', *, *, #9492, .T. ) ;
#34195=CYLINDRICAL_SURFACE ( 'NONE', #1112, 5.000000000000000888 ) ;
#34210=VERTEX_POINT ( 'NONE', #73778 ) ;
#34250=EDGE_LOOP ( 'NONE', ( #68754, #101711, #17769, #7602, #11173, #2081 ) ) ;
#34273=EDGE_CURVE ( 'NONE', #87999, #64539, #36569, .T. ) ;
#34283=DIRECTION ( 'NONE',  ( -1.000000000000000000, -0.000000000000000000, -0.000000000000000000 ) ) ;
#34294=LINE ( 'NONE', #59077, #81866 ) ;
#34323=ADVANCED_FACE ( 'NONE', ( #46735 ), #60316, .T. ) ;
#34338=CARTESIAN_POINT ( 'NONE',  ( 0.01688885742776283228, -6.535341423375585101, 4.680456609903972165 ) ) ;
#34383=VECTOR ( 'NONE', #43463, 1000.000000000000000 ) ;
#34384=ORIENTED_EDGE ( 'NONE', *, *, #99147, .T. ) ;
#34405=DIRECTION ( 'NONE',  ( 0.000000000000000000, -0.5000000000000009992, -0.8660254037844380415 ) ) ;
#34415=CARTESIAN_POINT ( 'NONE',  ( 5.799999999999999822, 8.000000000000000000, 0.000000000000000000 ) ) ;
#34425=ORIENTED_EDGE ( 'NONE', *, *, #24057, .F. ) ;
#34464=ORIENTED_EDGE ( 'NONE', *, *, #94417, .F. ) ;
#34510=ORIENTED_EDGE ( 'NONE', *, *, #25136, .F. ) ;
#34562=AXIS2_PLACEMENT_3D ( 'NONE', #23354, #56193, #48118 ) ;
#34617=EDGE_LOOP ( 'NONE', ( #16021, #28489, #80798, #60646, #104467, #66980 ) ) ;
#34632=CIRCLE ( 'NONE', #39755, 5.000000000000011546 ) ;
#34643=EDGE_LOOP ( 'NONE', ( #101627, #1297, #21835, #24153, #67657, #47319 ) ) ;
#34646=VERTEX_POINT ( 'NONE', #11570 ) ;
#34657=DIRECTION ( 'NONE',  ( 0.5735764363510557073, -0.8191520442889850262, 1.003171929053516612E-16 ) ) ;
#34687=( LENGTH_UNIT ( ) NAMED_UNIT ( * ) SI_UNIT ( .MILLI., .METRE. ) );
#34722=CARTESIAN_POINT ( 'NONE',  ( 102.6464385083043283, 1.030564683017419500E-14, 0.000000000000000000 ) ) ;
#34757=EDGE_CURVE ( 'NONE', #101241, #48515, #70694, .T. ) ;
#34773=DIRECTION ( 'NONE',  ( -1.000000000000000000, -0.000000000000000000, -0.000000000000000000 ) ) ;
#34774=ORIENTED_EDGE ( 'NONE', *, *, #28060, .F. ) ;
#34802=B_SPLINE_CURVE_WITH_KNOTS ( 'NONE', 3,
 ( #72471, #63874, #105378, #65449, #96240, #22893, #79503, #97800 ),
 .UNSPECIFIED., .F., .F.,
 ( 4, 2, 2, 4 ),
 ( 0.02285338878549946634, 0.02519297481083175930, 0.02636276782349790751, 0.02753256083616405225 ),
 .UNSPECIFIED. ) ;
#34865=ORIENTED_EDGE ( 'NONE', *, *, #94074, .F. ) ;
#34873=DIRECTION ( 'NONE',  ( -1.000000000000000000, -0.000000000000000000, -0.000000000000000000 ) ) ;
#34902=ORIENTED_EDGE ( 'NONE', *, *, #50054, .T. ) ;
#34968=PLANE ( 'NONE',  #85678 ) ;
#35004=DIRECTION ( 'NONE',  ( -1.000000000000000000, -0.000000000000000000, -0.000000000000000000 ) ) ;
#35007=DIRECTION ( 'NONE',  ( 0.000000000000000000, -1.000000000000000000, 0.000000000000000000 ) ) ;
#35015=LINE ( 'NONE', #67880, #91795 ) ;
#35064=DIRECTION ( 'NONE',  ( 0.000000000000000000, -1.000000000000000000, 0.000000000000000000 ) ) ;
#35069=B_SPLINE_CURVE_WITH_KNOTS ( 'NONE', 3,
 ( #99990, #41224, #25070, #26159, #74111, #50366, #198, #18031 ),
 .UNSPECIFIED., .F., .F.,
 ( 4, 2, 2, 4 ),
 ( 0.01336725833835631684, 0.01453745203451946473, 0.01570764573068261435, 0.01804803312300891013 ),
 .UNSPECIFIED. ) ;
#35073=DIRECTION ( 'NONE',  ( -1.000000000000000000, -0.000000000000000000, -0.000000000000000000 ) ) ;
#35076=CARTESIAN_POINT ( 'NONE',  ( 97.15356149169568312, 5.000000000000042633, 6.123233995736805725E-16 ) ) ;
#35103=AXIS2_PLACEMENT_3D ( 'NONE', #56383, #89316, #41281 ) ;
#35109=CARTESIAN_POINT ( 'NONE',  ( 81.84444444444444855, 1.023464760207051730E-14, 0.000000000000000000 ) ) ;
#35122=DIRECTION ( 'NONE',  ( -0.5735764363510459374, -0.8191520442889919096, 0.000000000000000000 ) ) ;
#35138=VERTEX_POINT ( 'NONE', #22514 ) ;
#35172=CARTESIAN_POINT ( 'NONE',  ( 82.42421628608209971, 1.030564683017419500E-14, 0.000000000000000000 ) ) ;
#35183=ORIENTED_EDGE ( 'NONE', *, *, #53296, .F. ) ;
#35247=CIRCLE ( 'NONE', #2497, 5.000000000000010658 ) ;
#35251=DIRECTION ( 'NONE',  ( -1.000000000000000000, -1.224606353822377258E-16, -0.000000000000000000 ) ) ;
#35282=DIRECTION ( 'NONE',  ( -1.000000000000000000, -0.000000000000000000, -0.000000000000000000 ) ) ;
#35309=CARTESIAN_POINT ( 'NONE',  ( 91.09088295274877112, -5.000000000000000000, 6.123233995736778115E-16 ) ) ;
#35379=ORIENTED_EDGE ( 'NONE', *, *, #102752, .T. ) ;
#35398=ORIENTED_EDGE ( 'NONE', *, *, #85309, .F. ) ;
#35438=CARTESIAN_POINT ( 'NONE',  ( 95.70911704725124025, -2.002967142162725287E-29, 5.000000000000011546 ) ) ;
#35468=DIRECTION ( 'NONE',  ( -1.000000000000000000, -1.224606353822377258E-16, -0.000000000000000000 ) ) ;
#35501=AXIS2_PLACEMENT_3D ( 'NONE', #90953, #40784, #65599 ) ;
#35508=DIRECTION ( 'NONE',  ( -1.000000000000000000, -0.000000000000000000, -0.000000000000000000 ) ) ;
#35513=CARTESIAN_POINT ( 'NONE',  ( 104.3757837139179117, 5.000000000000023093, 6.123233995736781074E-16 ) ) ;
#35556=AXIS2_PLACEMENT_3D ( 'NONE', #86607, #12671, #35948 ) ;
#35622=ADVANCED_FACE ( 'NONE', ( #1767 ), #83596, .T. ) ;
#35625=EDGE_CURVE ( 'NONE', #70018, #77725, #68669, .T. ) ;
#35639=DIRECTION ( 'NONE',  ( -1.000000000000000000, -1.224606353822377258E-16, -0.000000000000000000 ) ) ;
#35647=DIRECTION ( 'NONE',  ( 0.000000000000000000, -1.000000000000000000, 0.000000000000000000 ) ) ;
#35665=CARTESIAN_POINT ( 'NONE',  ( 91.09088295274877112, 1.030564683017419500E-14, 0.000000000000000000 ) ) ;
#35683=AXIS2_PLACEMENT_3D ( 'NONE', #87293, #27097, #43245 ) ;
#35722=ORIENTED_EDGE ( 'NONE', *, *, #71183, .F. ) ;
#35727=CARTESIAN_POINT ( 'NONE',  ( 87.62222222222222001, 1.023464760207051730E-14, 0.000000000000000000 ) ) ;
#35739=DIRECTION ( 'NONE',  ( 0.5735764363510557073, -0.8191520442889850262, 1.003171929053516612E-16 ) ) ;
#35756=FACE_OUTER_BOUND ( 'NONE', #80255, .T. ) ;
#35791=DIRECTION ( 'NONE',  ( 0.000000000000000000, 1.000000000000000000, 0.000000000000000000 ) ) ;
#35836=CARTESIAN_POINT ( 'NONE',  ( 81.26467260280679739, -5.000000000000000000, 0.000000000000000000 ) ) ;
#35842=CARTESIAN_POINT ( 'NONE',  ( 100.6222222222222200, -4.171999999999998820, 5.616230220889773285E-16 ) ) ;
#35844=VERTEX_POINT ( 'NONE', #37910 ) ;
#35853=VERTEX_POINT ( 'NONE', #73941 ) ;
#35871=CIRCLE ( 'NONE', #13399, 5.000000000000011546 ) ;
#35948=DIRECTION ( 'NONE',  ( 0.000000000000000000, -1.000000000000000000, 0.000000000000000000 ) ) ;
#35949=ORIENTED_EDGE ( 'NONE', *, *, #45516, .F. ) ;
#36029=FACE_OUTER_BOUND ( 'NONE', #84541, .T. ) ;
#36033=EDGE_CURVE ( 'NONE', #72914, #7841, #948, .T. ) ;
#36041=CYLINDRICAL_SURFACE ( 'NONE', #16048, 5.000000000000000888 ) ;
#36046=VECTOR ( 'NONE', #21182, 1000.000000000000000 ) ;
#36073=ORIENTED_EDGE ( 'NONE', *, *, #106198, .F. ) ;
#36078=EDGE_CURVE ( 'NONE', #53170, #28024, #56090, .T. ) ;
#36087=DIRECTION ( 'NONE',  ( -1.000000000000000000, -1.224606353822377258E-16, -0.000000000000000000 ) ) ;
#36094=ORIENTED_EDGE ( 'NONE', *, *, #64505, .F. ) ;
#36137=ORIENTED_EDGE ( 'NONE', *, *, #2264, .T. ) ;
#36146=ORIENTED_EDGE ( 'NONE', *, *, #53461, .F. ) ;
#36171=AXIS2_PLACEMENT_3D ( 'NONE', #5012, #47042, #102101 ) ;
#36180=EDGE_CURVE ( 'NONE', #16299, #54111, #70522, .T. ) ;
#36188=CARTESIAN_POINT ( 'NONE',  ( 100.6222222222222200, 1.023464760207051730E-14, 0.000000000000000000 ) ) ;
#36205=DIRECTION ( 'NONE',  ( 0.000000000000000000, -1.000000000000000000, 0.000000000000000000 ) ) ;
#36279=VECTOR ( 'NONE', #59128, 1000.000000000000000 ) ;
#36285=CARTESIAN_POINT ( 'NONE',  ( 98.31310517497099966, -5.000000000000000000, 6.123233995736778115E-16 ) ) ;
#36351=VECTOR ( 'NONE', #63254, 1000.000000000000000 ) ;
#36356=CARTESIAN_POINT ( 'NONE',  ( 87.04245038058458306, 1.016364837396684119E-14, 0.000000000000000000 ) ) ;
#36381=CARTESIAN_POINT ( 'NONE',  ( 102.0666666666666629, 1.023464760207051730E-14, 0.000000000000000000 ) ) ;
#36406=DIRECTION ( 'NONE',  ( 0.000000000000000000, -1.000000000000000000, 0.000000000000000000 ) ) ;
#36410=ORIENTED_EDGE ( 'NONE', *, *, #10125, .F. ) ;
#36415=AXIS2_PLACEMENT_3D ( 'NONE', #66462, #75069, #23918 ) ;
#36455=ORIENTED_EDGE ( 'NONE', *, *, #50786, .T. ) ;
#36462=CIRCLE ( 'NONE', #58827, 8.000000000000000000 ) ;
#36517=VERTEX_POINT ( 'NONE', #39090 ) ;
#36539=LINE ( 'NONE', #78017, #9994 ) ;
#36569=LINE ( 'NONE', #43554, #51654 ) ;
#36588=ORIENTED_EDGE ( 'NONE', *, *, #36180, .T. ) ;
#36601=EDGE_CURVE ( 'NONE', #70163, #37934, #87178, .T. ) ;
#36602=ORIENTED_EDGE ( 'NONE', *, *, #15197, .T. ) ;
#36607=ORIENTED_EDGE ( 'NONE', *, *, #84176, .F. ) ;
#36729=ADVANCED_FACE ( 'NONE', ( #26641 ), #34195, .T. ) ;
#36737=ORIENTED_EDGE ( 'NONE', *, *, #60865, .F. ) ;
#36807=CARTESIAN_POINT ( 'NONE',  ( 101.2019940638598854, 1.030564683017419500E-14, 0.000000000000000000 ) ) ;
#36813=COLOUR_RGB ( '', 0.66274510, 0.83137255, 0.94901961) ;
#36814=( NAMED_UNIT ( * ) SI_UNIT ( $, .STERADIAN. ) SOLID_ANGLE_UNIT ( ) );
#36838=DIRECTION ( 'NONE',  ( -1.000000000000000000, -1.224606353822377258E-16, -0.000000000000000000 ) ) ;
#36858=CARTESIAN_POINT ( 'NONE',  ( 101.4868948250290259, -2.002967142162725287E-29, 5.000000000000011546 ) ) ;
#36864=ORIENTED_EDGE ( 'NONE', *, *, #64566, .F. ) ;
#36886=DIRECTION ( 'NONE',  ( 0.000000000000000000, 0.000000000000000000, -1.000000000000000000 ) ) ;
#36893=ORIENTED_EDGE ( 'NONE', *, *, #105138, .T. ) ;
#36920=CARTESIAN_POINT ( 'NONE',  ( 0.000000000000000000, 0.000000000000000000, 0.000000000000000000 ) ) ;
#36922=VERTEX_POINT ( 'NONE', #36858 ) ;
#36932=ORIENTED_EDGE ( 'NONE', *, *, #86397, .T. ) ;
#36946=LINE ( 'NONE', #76298, #75763 ) ;
#36971=EDGE_CURVE ( 'NONE', #86608, #73379, #9753, .T. ) ;
#36983=DIRECTION ( 'NONE',  ( 0.000000000000000000, 0.000000000000000000, -1.000000000000000000 ) ) ;
#36994=VERTEX_POINT ( 'NONE', #91232 ) ;
#37029=ORIENTED_EDGE ( 'NONE', *, *, #93636, .F. ) ;
#37058=DIRECTION ( 'NONE',  ( -1.000000000000000000, -0.000000000000000000, -0.000000000000000000 ) ) ;
#37151=ORIENTED_EDGE ( 'NONE', *, *, #80172, .F. ) ;
#37158=AXIS2_PLACEMENT_3D ( 'NONE', #81595, #15294, #6667 ) ;
#37220=VERTEX_POINT ( 'NONE', #21607 ) ;
#37223=CIRCLE ( 'NONE', #18271, 5.000000000000011546 ) ;
#37233=ORIENTED_EDGE ( 'NONE', *, *, #91402, .F. ) ;
#37237=ORIENTED_EDGE ( 'NONE', *, *, #86113, .F. ) ;
#37238=EDGE_CURVE ( 'NONE', #98133, #53170, #69606, .T. ) ;
#37279=CARTESIAN_POINT ( 'NONE',  ( 95.42421628608209971, -2.002967142162725287E-29, 5.000000000000011546 ) ) ;
#37293=CARTESIAN_POINT ( 'NONE',  ( 0.000000000000000000, 0.000000000000000000, 0.000000000000000000 ) ) ;
#37310=CONICAL_SURFACE ( 'NONE', #87183, 4.172000000000009479, 0.9599310885968813656 ) ;
#37337=CYLINDRICAL_SURFACE ( 'NONE', #68288, 5.000000000000000888 ) ;
#37338=DIRECTION ( 'NONE',  ( 1.000000000000000000, 0.000000000000000000, 0.000000000000000000 ) ) ;
#37340=CARTESIAN_POINT ( 'NONE',  ( 104.0908829527487711, 1.030564683017419500E-14, 0.000000000000000000 ) ) ;
#37360=EDGE_CURVE ( 'NONE', #24844, #63754, #80855, .T. ) ;
#37361=ORIENTED_EDGE ( 'NONE', *, *, #13029, .F. ) ;
#37377=CARTESIAN_POINT ( 'NONE',  ( 88.20199406385988539, 5.000000000000021316, 0.000000000000000000 ) ) ;
#37406=EDGE_LOOP ( 'NONE', ( #59145, #84021, #105152, #5385, #90339, #11559 ) ) ;
#37435=LINE ( 'NONE', #64340, #43145 ) ;
#37491=AXIS2_PLACEMENT_3D ( 'NONE', #41252, #90338, #97894 ) ;
#37495=DIRECTION ( 'NONE',  ( 0.000000000000000000, 0.000000000000000000, 1.000000000000000000 ) ) ;
#37501=EDGE_CURVE ( 'NONE', #40136, #77127, #8073, .T. ) ;
#37507=AXIS2_PLACEMENT_3D ( 'NONE', #50435, #65040, #24088 ) ;
#37544=DIRECTION ( 'NONE',  ( -1.000000000000000000, -1.224606353822377258E-16, -0.000000000000000000 ) ) ;
#37559=ORIENTED_EDGE ( 'NONE', *, *, #7213, .T. ) ;
#37581=CARTESIAN_POINT ( 'NONE',  ( 96.28888888888889142, -4.171999999999998820, 0.000000000000000000 ) ) ;
#37637=CIRCLE ( 'NONE', #78934, 5.000000000000010658 ) ;
#37681=AXIS2_PLACEMENT_3D ( 'NONE', #69651, #94467, #14567 ) ;
#37688=DIRECTION ( 'NONE',  ( 0.000000000000000000, -1.000000000000000000, 0.000000000000000000 ) ) ;
#37699=VERTEX_POINT ( 'NONE', #7368 ) ;
#37707=ADVANCED_FACE ( 'NONE', ( #48361 ), #23597, .F. ) ;
#37708=CIRCLE ( 'NONE', #67158, 5.000000000000010658 ) ;
#37728=EDGE_LOOP ( 'NONE', ( #9460, #36932, #10289 ) ) ;
#37737=ORIENTED_EDGE ( 'NONE', *, *, #29916, .T. ) ;
#37740=AXIS2_PLACEMENT_3D ( 'NONE', #53632, #86566, #37495 ) ;
#37797=CARTESIAN_POINT ( 'NONE',  ( 0.4969600502617521620, 8.860760056385744932, 0.6527133886630304138 ) ) ;
#37837=VECTOR ( 'NONE', #19671, 999.9999999999998863 ) ;
#37903=CARTESIAN_POINT ( 'NONE',  ( -3.460411933849569239E-15, -7.124194613927627984, -3.660532965668814143 ) ) ;
#37910=CARTESIAN_POINT ( 'NONE',  ( 6.400000000000000355, 0.000000000000000000, 8.000000000000000000 ) ) ;
#37931=DIRECTION ( 'NONE',  ( -1.000000000000000000, -1.224606353822377258E-16, -0.000000000000000000 ) ) ;
#37934=VERTEX_POINT ( 'NONE', #60613 ) ;
#37939=FACE_OUTER_BOUND ( 'NONE', #33517, .T. ) ;
#37943=VECTOR ( 'NONE', #72084, 1000.000000000000000 ) ;
#37944=LINE ( 'NONE', #103698, #79104 ) ;
#38002=FACE_OUTER_BOUND ( 'NONE', #34250, .T. ) ;
#38050=ORIENTED_EDGE ( 'NONE', *, *, #90922, .F. ) ;
#38104=VECTOR ( 'NONE', #51633, 1000.000000000000000 ) ;
#38137=DIRECTION ( 'NONE',  ( -1.000000000000000000, -1.224606353822377258E-16, -0.000000000000000000 ) ) ;
#38144=DIRECTION ( 'NONE',  ( -1.000000000000000000, -1.224606353822377258E-16, -0.000000000000000000 ) ) ;
#38171=AXIS2_PLACEMENT_3D ( 'NONE', #13428, #5366, #105117 ) ;
#38172=EDGE_CURVE ( 'NONE', #30465, #42532, #65891, .T. ) ;
#38182=CARTESIAN_POINT ( 'NONE',  ( 91.95555555555554861, -4.171999999999998820, 0.000000000000000000 ) ) ;
#38214=CARTESIAN_POINT ( 'NONE',  ( 102.6464385083043283, 1.030564683017419500E-14, 0.000000000000000000 ) ) ;
#38225=EDGE_CURVE ( 'NONE', #44057, #93631, #59842, .T. ) ;
#38308=EDGE_LOOP ( 'NONE', ( #98871, #86644, #83318, #48577, #37361, #64629 ) ) ;
#38311=EDGE_LOOP ( 'NONE', ( #97726, #66716, #32558, #79569, #53995 ) ) ;
#38333=CARTESIAN_POINT ( 'NONE',  ( 85.31310517497098544, 1.030564683017419500E-14, 0.000000000000000000 ) ) ;
#38351=ORIENTED_EDGE ( 'NONE', *, *, #28069, .F. ) ;
#38383=VECTOR ( 'NONE', #21420, 1000.000000000000000 ) ;
#38388=FACE_OUTER_BOUND ( 'NONE', #12981, .T. ) ;
#38394=CARTESIAN_POINT ( 'NONE',  ( 6.800000000000000711, 6.613092715395708453E-16, 5.400000000000001243 ) ) ;
#38426=ORIENTED_EDGE ( 'NONE', *, *, #46903, .F. ) ;
#38448=ORIENTED_EDGE ( 'NONE', *, *, #31356, .T. ) ;
#38449=CARTESIAN_POINT ( 'NONE',  ( 96.28888888888889142, 1.023464760207051730E-14, 0.000000000000000000 ) ) ;
#38452=VECTOR ( 'NONE', #5234, 1000.000000000000000 ) ;
#38465=CARTESIAN_POINT ( 'NONE',  ( 91.37578371391791165, 5.000000000000023093, 6.123233995736781074E-16 ) ) ;
#38469=ORIENTED_EDGE ( 'NONE', *, *, #3634, .T. ) ;
#38478=FACE_OUTER_BOUND ( 'NONE', #97423, .T. ) ;
#38584=CARTESIAN_POINT ( 'NONE',  ( 0.000000000000000000, 6.123233995736767268E-16, -5.000000000000000888 ) ) ;
#38589=DIRECTION ( 'NONE',  ( -0.5735764363510461594, 0.8191520442889916875, 1.003171929053524870E-16 ) ) ;
#38619=CARTESIAN_POINT ( 'NONE',  ( 102.6464385083043283, 5.000000000000021316, 0.000000000000000000 ) ) ;
#38624=CARTESIAN_POINT ( 'NONE',  ( 88.20199406385988539, 1.030564683017419500E-14, 0.000000000000000000 ) ) ;
#38705=AXIS2_PLACEMENT_3D ( 'NONE', #72699, #16057, #65678 ) ;
#38716=ORIENTED_EDGE ( 'NONE', *, *, #31386, .F. ) ;
#38726=DIRECTION ( 'NONE',  ( 0.5735764363510554853, 0.8191520442889852482, 0.000000000000000000 ) ) ;
#38727=CARTESIAN_POINT ( 'NONE',  ( 0.7145311798161605443, -4.618802153517258979, -8.000000000000001776 ) ) ;
#38733=VERTEX_POINT ( 'NONE', #85594 ) ;
#38744=CIRCLE ( 'NONE', #52495, 8.000000000000000000 ) ;
#38768=EDGE_CURVE ( 'NONE', #21366, #68926, #36539, .T. ) ;
#38769=EDGE_LOOP ( 'NONE', ( #70007, #42502, #36455, #52622, #59771 ) ) ;
#38805=CONICAL_SURFACE ( 'NONE', #28519, 5.000000000000010658, 0.9599310885968697082 ) ;
#38813=DIRECTION ( 'NONE',  ( 0.000000000000000000, 1.000000000000000000, 0.000000000000000000 ) ) ;
#38817=AXIS2_PLACEMENT_3D ( 'NONE', #106741, #100248, #59280 ) ;
#38852=CARTESIAN_POINT ( 'NONE',  ( 95.70911704725124025, 1.016364837396684119E-14, 0.000000000000000000 ) ) ;
#38859=DIRECTION ( 'NONE',  ( -1.000000000000000000, -0.000000000000000000, -0.000000000000000000 ) ) ;
#38865=CARTESIAN_POINT ( 'NONE',  ( 96.28888888888889142, 1.023464760207051730E-14, 0.000000000000000000 ) ) ;
#38882=ORIENTED_EDGE ( 'NONE', *, *, #48532, .F. ) ;
#38884=DIRECTION ( 'NONE',  ( 1.000000000000000000, 0.000000000000000000, 0.000000000000000000 ) ) ;
#38928=ORIENTED_EDGE ( 'NONE', *, *, #90174, .F. ) ;
#38986=AXIS2_PLACEMENT_3D ( 'NONE', #32396, #71753, #57161 ) ;
#39027=ORIENTED_EDGE ( 'NONE', *, *, #92084, .T. ) ;
#39045=CARTESIAN_POINT ( 'NONE',  ( 104.0908829527487711, 1.030564683017419500E-14, 0.000000000000000000 ) ) ;
#39046=CIRCLE ( 'NONE', #21900, 5.000000000000011546 ) ;
#39083=EDGE_CURVE ( 'NONE', #35138, #54417, #97916, .T. ) ;
#39089=ORIENTED_EDGE ( 'NONE', *, *, #81919, .F. ) ;
#39090=CARTESIAN_POINT ( 'NONE',  ( 92.82022815836235452, -2.002967142162725287E-29, 5.000000000000011546 ) ) ;
#39110=DIRECTION ( 'NONE',  ( 0.000000000000000000, -1.000000000000000000, 0.000000000000000000 ) ) ;
#39118=CONICAL_SURFACE ( 'NONE', #94233, 5.000000000000010658, 0.9599310885968697082 ) ;
#39124=VERTEX_POINT ( 'NONE', #58382 ) ;
#39159=CIRCLE ( 'NONE', #99388, 5.000000000000010658 ) ;
#39168=DIRECTION ( 'NONE',  ( 0.000000000000000000, -1.000000000000000000, 0.000000000000000000 ) ) ;
#39221=VERTEX_POINT ( 'NONE', #92332 ) ;
#39232=CYLINDRICAL_SURFACE ( 'NONE', #75880, 5.000000000000000888 ) ;
#39263=EDGE_CURVE ( 'NONE', #105278, #85106, #66904, .T. ) ;
#39270=CIRCLE ( 'NONE', #84056, 5.000000000000010658 ) ;
#39293=ORIENTED_EDGE ( 'NONE', *, *, #105111, .F. ) ;
#39356=ORIENTED_EDGE ( 'NONE', *, *, #82631, .T. ) ;
#39361=ORIENTED_EDGE ( 'NONE', *, *, #9184, .T. ) ;
#39364=CARTESIAN_POINT ( 'NONE',  ( 0.4973051450610294633, -3.866309095671266238, 8.000000000000000000 ) ) ;
#39374=ORIENTED_EDGE ( 'NONE', *, *, #404, .F. ) ;
#39418=ORIENTED_EDGE ( 'NONE', *, *, #98205, .F. ) ;
#39472=CARTESIAN_POINT ( 'NONE',  ( 102.6464385083043283, -2.002967142162725287E-29, 5.000000000000011546 ) ) ;
#39546=CIRCLE ( 'NONE', #1615, 4.172000000000009479 ) ;
#39568=CARTESIAN_POINT ( 'NONE',  ( 0.3167204509598346984, -8.479269695850854660, 1.313474075707213196 ) ) ;
#39572=EDGE_CURVE ( 'NONE', #2944, #32770, #42794, .T. ) ;
#39595=CYLINDRICAL_SURFACE ( 'NONE', #10124, 5.000000000000000888 ) ;
#39598=AXIS2_PLACEMENT_3D ( 'NONE', #31109, #38144, #80667 ) ;
#39616=AXIS2_PLACEMENT_3D ( 'NONE', #83720, #9828, #75636 ) ;
#39623=EDGE_CURVE ( 'NONE', #24268, #86867, #99224, .T. ) ;
#39641=DIRECTION ( 'NONE',  ( 0.000000000000000000, 0.000000000000000000, 1.000000000000000000 ) ) ;
#39644=EDGE_CURVE ( 'NONE', #13347, #40083, #63526, .T. ) ;
#39656=ORIENTED_EDGE ( 'NONE', *, *, #15458, .F. ) ;
#39755=AXIS2_PLACEMENT_3D ( 'NONE', #58083, #75328, #49997 ) ;
#39834=AXIS2_PLACEMENT_3D ( 'NONE', #93932, #27644, #93407 ) ;
#39859=VERTEX_POINT ( 'NONE', #79755 ) ;
#39878=ORIENTED_EDGE ( 'NONE', *, *, #47917, .F. ) ;
#39947=CARTESIAN_POINT ( 'NONE',  ( 80.97977184163765685, 1.030564683017419500E-14, 0.000000000000000000 ) ) ;
#39948=ORIENTED_EDGE ( 'NONE', *, *, #45516, .T. ) ;
#39954=DIRECTION ( 'NONE',  ( -1.000000000000000000, -1.224606353822377258E-16, -0.000000000000000000 ) ) ;
#39986=CARTESIAN_POINT ( 'NONE',  ( 84.15356149169568312, -2.002967142162725287E-29, 5.000000000000011546 ) ) ;
#40004=AXIS2_PLACEMENT_3D ( 'NONE', #8728, #90186, #66985 ) ;
#40072=CARTESIAN_POINT ( 'NONE',  ( 6.400000000000000355, 9.797174393178825657E-16, -8.000000000000000000 ) ) ;
#40083=VERTEX_POINT ( 'NONE', #59755 ) ;
#40136=VERTEX_POINT ( 'NONE', #83215 ) ;
#40216=LINE ( 'NONE', #98448, #22370 ) ;
#40269=AXIS2_PLACEMENT_3D ( 'NONE', #15329, #90284, #66005 ) ;
#40309=CONICAL_SURFACE ( 'NONE', #5810, 4.172000000000009479, 0.9599310885968813656 ) ;
#40369=VECTOR ( 'NONE', #11409, 1000.000000000000000 ) ;
#40395=EDGE_LOOP ( 'NONE', ( #74549, #39356, #103452, #18272, #85413, #52237 ) ) ;
#40414=DIRECTION ( 'NONE',  ( -1.000000000000000000, -1.224606353822377258E-16, -0.000000000000000000 ) ) ;
#40426=EDGE_CURVE ( 'NONE', #27178, #14501, #30313, .T. ) ;
#40543=ORIENTED_EDGE ( 'NONE', *, *, #21881, .F. ) ;
#40572=ADVANCED_FACE ( 'NONE', ( #51772 ), #61496, .T. ) ;
#40609=ORIENTED_EDGE ( 'NONE', *, *, #73796, .T. ) ;
#40636=CIRCLE ( 'NONE', #33738, 4.172000000000009479 ) ;
#40656=CIRCLE ( 'NONE', #11392, 5.000000000000010658 ) ;
#40697=AXIS2_PLACEMENT_3D ( 'NONE', #72963, #46064, #30424 ) ;
#40728=ORIENTED_EDGE ( 'NONE', *, *, #14037, .T. ) ;
#40745=CARTESIAN_POINT ( 'NONE',  ( 84.73333333333332007, -4.171999999999998820, 0.000000000000000000 ) ) ;
#40748=CARTESIAN_POINT ( 'NONE',  ( 86.75754961941542831, 6.123233995736568081E-16, -5.000000000000011546 ) ) ;
#40784=DIRECTION ( 'NONE',  ( 1.000000000000000000, 1.224606353822377258E-16, 0.000000000000000000 ) ) ;
#40846=DIRECTION ( 'NONE',  ( 1.000000000000000000, 1.224606353822377258E-16, 0.000000000000000000 ) ) ;
#40854=CIRCLE ( 'NONE', #13275, 5.000000000000010658 ) ;
#40861=DIRECTION ( 'NONE',  ( 0.000000000000000000, -1.000000000000000000, 0.000000000000000000 ) ) ;
#40873=AXIS2_PLACEMENT_3D ( 'NONE', #17410, #51873, #76685 ) ;
#40874=AXIS2_PLACEMENT_3D ( 'NONE', #27827, #13167, #87618 ) ;
#40893=ADVANCED_FACE ( 'NONE', ( #90408 ), #60000, .T. ) ;
#40899=CARTESIAN_POINT ( 'NONE',  ( 6.400000000000000355, -9.237604307034013473, 7.924929828396943928E-16 ) ) ;
#40910=VERTEX_POINT ( 'NONE', #18677 ) ;
#40916=ORIENTED_EDGE ( 'NONE', *, *, #96837, .T. ) ;
#40922=CIRCLE ( 'NONE', #16848, 5.000000000000011546 ) ;
#40925=ORIENTED_EDGE ( 'NONE', *, *, #5226, .F. ) ;
#40937=CIRCLE ( 'NONE', #44418, 5.000000000000010658 ) ;
#40960=DIRECTION ( 'NONE',  ( 1.000000000000000000, 1.224606353822377258E-16, 0.000000000000000000 ) ) ;
#40965=CARTESIAN_POINT ( 'NONE',  ( 0.7145311798163195283, -4.618802153516994302, 8.000000000000000000 ) ) ;
#40980=FACE_OUTER_BOUND ( 'NONE', #61162, .T. ) ;
#40996=DIRECTION ( 'NONE',  ( -1.000000000000000000, -1.224606353822377258E-16, -0.000000000000000000 ) ) ;
#41031=LINE ( 'NONE', #23279, #59929 ) ;
#41052=VERTEX_POINT ( 'NONE', #69860 ) ;
#41061=DIRECTION ( 'NONE',  ( 0.000000000000000000, -1.000000000000000000, 0.000000000000000000 ) ) ;
#41078=ORIENTED_EDGE ( 'NONE', *, *, #54405, .T. ) ;
#41092=EDGE_CURVE ( 'NONE', #1566, #72949, #29068, .T. ) ;
#41101=CARTESIAN_POINT ( 'NONE',  ( 0.000000000000000000, 0.000000000000000000, 0.000000000000000000 ) ) ;
#41103=CIRCLE ( 'NONE', #84218, 5.000000000000000888 ) ;
#41117=CARTESIAN_POINT ( 'NONE',  ( 0.3167204509598183226, -5.377136764700210847, -6.686525924292708645 ) ) ;
#41122=ORIENTED_EDGE ( 'NONE', *, *, #14037, .F. ) ;
#41131=CARTESIAN_POINT ( 'NONE',  ( 92.82022815836235452, 6.123233995736582872E-16, -5.000000000000011546 ) ) ;
#41134=VECTOR ( 'NONE', #23959, 1000.000000000000000 ) ;
#41224=CARTESIAN_POINT ( 'NONE',  ( -9.967460206814975296E-16, 0.3912769055735432766, 8.000000000000000000 ) ) ;
#41252=CARTESIAN_POINT ( 'NONE',  ( 80.97977184163765685, 1.030564683017419500E-14, 0.000000000000000000 ) ) ;
#41260=EDGE_LOOP ( 'NONE', ( #54510, #25984, #68188, #18310, #100872, #85028 ) ) ;
#41267=ORIENTED_EDGE ( 'NONE', *, *, #105739, .F. ) ;
#41268=VECTOR ( 'NONE', #92527, 1000.000000000000000 ) ;
#41281=DIRECTION ( 'NONE',  ( 0.000000000000000000, -1.000000000000000000, 0.000000000000000000 ) ) ;
#41292=EDGE_CURVE ( 'NONE', #89220, #36994, #8820, .T. ) ;
#41316=DIRECTION ( 'NONE',  ( 0.000000000000000000, 1.000000000000000000, 0.000000000000000000 ) ) ;
#41344=UNCERTAINTY_MEASURE_WITH_UNIT (LENGTH_MEASURE( 1.000000000000000082E-05 ), #34687, 'distance_accuracy_value', 'NONE');
#41349=CARTESIAN_POINT ( 'NONE',  ( 91.37578371391791165, -5.000000000000000000, 0.000000000000000000 ) ) ;
#41409=DIRECTION ( 'NONE',  ( 0.000000000000000000, 0.000000000000000000, 1.000000000000000000 ) ) ;
#41422=CARTESIAN_POINT ( 'NONE',  ( 91.37578371391791165, 1.016364837396684119E-14, 0.000000000000000000 ) ) ;
#41457=ORIENTED_EDGE ( 'NONE', *, *, #42170, .F. ) ;
#41507=DIRECTION ( 'NONE',  ( -1.000000000000000000, -1.224606353822377258E-16, -0.000000000000000000 ) ) ;
#41563=VECTOR ( 'NONE', #79051, 1000.000000000000000 ) ;
#41569=CARTESIAN_POINT ( 'NONE',  ( 0.000000000000000000, 6.123233995736767268E-16, -5.000000000000000888 ) ) ;
#41630=FACE_OUTER_BOUND ( 'NONE', #71935, .T. ) ;
#41635=ORIENTED_EDGE ( 'NONE', *, *, #1210, .F. ) ;
#41707=DIRECTION ( 'NONE',  ( 0.000000000000000000, -1.000000000000000000, 0.000000000000000000 ) ) ;
#41719=LINE ( 'NONE', #51392, #84265 ) ;
#41720=CARTESIAN_POINT ( 'NONE',  ( 92.82022815836235452, 1.016364837396684119E-14, 0.000000000000000000 ) ) ;
#41733=DIRECTION ( 'NONE',  ( -1.000000000000000000, -1.224606353822377258E-16, -0.000000000000000000 ) ) ;
#41734=DIRECTION ( 'NONE',  ( 1.000000000000000000, 1.224606353822377258E-16, 0.000000000000000000 ) ) ;
#41772=VERTEX_POINT ( 'NONE', #27874 ) ;
#41790=ORIENTED_EDGE ( 'NONE', *, *, #69088, .F. ) ;
#41817=ORIENTED_EDGE ( 'NONE', *, *, #39623, .F. ) ;
#41834=CYLINDRICAL_SURFACE ( 'NONE', #53241, 5.000000000000000888 ) ;
#41839=ORIENTED_EDGE ( 'NONE', *, *, #105871, .T. ) ;
#41847=CARTESIAN_POINT ( 'NONE',  ( 80.97977184163765685, 1.030564683017419500E-14, 0.000000000000000000 ) ) ;
#41883=CARTESIAN_POINT ( 'NONE',  ( 98.59800593614012598, 1.016364837396684119E-14, 0.000000000000000000 ) ) ;
#41887=DIRECTION ( 'NONE',  ( -1.000000000000000000, -1.224606353822377258E-16, -0.000000000000000000 ) ) ;
#41888=ORIENTED_EDGE ( 'NONE', *, *, #71793, .F. ) ;
#41910=ORIENTED_EDGE ( 'NONE', *, *, #7664, .T. ) ;
#41925=CARTESIAN_POINT ( 'NONE',  ( 0.000000000000000000, 6.123233995736767268E-16, -5.000000000000000888 ) ) ;
#41948=DIRECTION ( 'NONE',  ( 0.000000000000000000, -1.000000000000000000, 0.000000000000000000 ) ) ;
#41952=CARTESIAN_POINT ( 'NONE',  ( 105.5353273971932140, 5.000000000000021316, 0.000000000000000000 ) ) ;
#41956=DIRECTION ( 'NONE',  ( 0.000000000000000000, -1.000000000000000000, 0.000000000000000000 ) ) ;
#42062=DIRECTION ( 'NONE',  ( -0.5735764363510459374, -0.8191520442889919096, 0.000000000000000000 ) ) ;
#42074=EDGE_CURVE ( 'NONE', #55179, #24268, #42660, .T. ) ;
#42107=CIRCLE ( 'NONE', #62850, 5.000000000000011546 ) ;
#42133=ORIENTED_EDGE ( 'NONE', *, *, #67138, .T. ) ;
#42157=EDGE_CURVE ( 'NONE', #10334, #62320, #22060, .T. ) ;
#42161=DIRECTION ( 'NONE',  ( 0.5735764363510554853, 0.8191520442889852482, 0.000000000000000000 ) ) ;
#42170=EDGE_CURVE ( 'NONE', #15028, #77225, #12030, .T. ) ;
#42173=CONICAL_SURFACE ( 'NONE', #45582, 5.000000000000010658, 0.9599310885968697082 ) ;
#42214=DIRECTION ( 'NONE',  ( 0.000000000000000000, -1.000000000000000000, 0.000000000000000000 ) ) ;
#42330=EDGE_CURVE ( 'NONE', #39221, #43420, #56421, .T. ) ;
#42335=CARTESIAN_POINT ( 'NONE',  ( 106.4000000000000057, 0.000000000000000000, 0.000000000000000000 ) ) ;
#42338=AXIS2_PLACEMENT_3D ( 'NONE', #32463, #57747, #90139 ) ;
#42388=VERTEX_POINT ( 'NONE', #50751 ) ;
#42409=CONICAL_SURFACE ( 'NONE', #7984, 5.000000000000010658, 0.9599310885968697082 ) ;
#42424=VECTOR ( 'NONE', #95600, 1000.000000000000000 ) ;
#42439=DIRECTION ( 'NONE',  ( 0.000000000000000000, -1.000000000000000000, 0.000000000000000000 ) ) ;
#42474=CIRCLE ( 'NONE', #99274, 4.172000000000009479 ) ;
#42502=ORIENTED_EDGE ( 'NONE', *, *, #104401, .T. ) ;
#42514=ADVANCED_FACE ( 'NONE', ( #55525 ), #70684, .T. ) ;
#42532=VERTEX_POINT ( 'NONE', #21114 ) ;
#42563=AXIS2_PLACEMENT_3D ( 'NONE', #83477, #9576, #1481 ) ;
#42586=CARTESIAN_POINT ( 'NONE',  ( 95.70911704725124025, 5.000000000000042633, 6.123233995736805725E-16 ) ) ;
#42654=CARTESIAN_POINT ( 'NONE',  ( 90.51111111111110574, 4.172000000000019249, 5.109226446042768454E-16 ) ) ;
#42660=CIRCLE ( 'NONE', #25542, 4.172000000000009479 ) ;
#42676=CARTESIAN_POINT ( 'NONE',  ( 0.000000000000000000, 0.000000000000000000, 0.000000000000000000 ) ) ;
#42708=LINE ( 'NONE', #75603, #89007 ) ;
#42714=DIRECTION ( 'NONE',  ( 1.000000000000000000, 0.000000000000000000, 0.000000000000000000 ) ) ;
#42722=CONICAL_SURFACE ( 'NONE', #25519, 4.172000000000009479, 0.9599310885968813656 ) ;
#42762=DIRECTION ( 'NONE',  ( -1.000000000000000000, -1.224606353822377258E-16, -0.000000000000000000 ) ) ;
#42766=DIRECTION ( 'NONE',  ( 1.000000000000000000, 0.000000000000000000, 0.000000000000000000 ) ) ;
#42784=CIRCLE ( 'NONE', #85866, 5.000000000000011546 ) ;
#42794=CIRCLE ( 'NONE', #87549, 4.171999999999999709 ) ;
#42838=VECTOR ( 'NONE', #35739, 1000.000000000000000 ) ;
#42856=EDGE_LOOP ( 'NONE', ( #45, #65114, #9283, #105571, #30953 ) ) ;
#42874=FILL_AREA_STYLE ('',( #9970 ) ) ;
#42940=CARTESIAN_POINT ( 'NONE',  ( 103.5111111111111057, -4.171999999999998820, 0.000000000000000000 ) ) ;
#42990=CARTESIAN_POINT ( 'NONE',  ( 92.82022815836235452, -5.000000000000000000, 0.000000000000000000 ) ) ;
#43004=DIRECTION ( 'NONE',  ( -1.000000000000000000, -0.000000000000000000, -0.000000000000000000 ) ) ;
#43023=CIRCLE ( 'NONE', #101534, 5.000000000000010658 ) ;
#43097=VERTEX_POINT ( 'NONE', #18094 ) ;
#43125=DIRECTION ( 'NONE',  ( 0.000000000000000000, -1.000000000000000000, 0.000000000000000000 ) ) ;
#43131=ORIENTED_EDGE ( 'NONE', *, *, #2365, .F. ) ;
#43134=ADVANCED_FACE ( 'NONE', ( #69306 ), #89415, .T. ) ;
#43145=VECTOR ( 'NONE', #70303, 1000.000000000000000 ) ;
#43162=CARTESIAN_POINT ( 'NONE',  ( 100.6222222222222200, 1.023464760207051730E-14, 0.000000000000000000 ) ) ;
#43196=CARTESIAN_POINT ( 'NONE',  ( 88.48689482502902592, 1.016364837396684119E-14, 0.000000000000000000 ) ) ;
#43212=VECTOR ( 'NONE', #70233, 1000.000000000000000 ) ;
#43232=AXIS2_PLACEMENT_3D ( 'NONE', #82524, #72820, #56089 ) ;
#43245=DIRECTION ( 'NONE',  ( 0.000000000000000000, 1.000000000000000000, 0.000000000000000000 ) ) ;
#43256=AXIS2_PLACEMENT_3D ( 'NONE', #45607, #34873, #39641 ) ;
#43265=DIRECTION ( 'NONE',  ( -1.000000000000000000, -1.224606353822377258E-16, -0.000000000000000000 ) ) ;
#43269=CARTESIAN_POINT ( 'NONE',  ( 87.04245038058458306, 1.016364837396684119E-14, 0.000000000000000000 ) ) ;
#43275=DIRECTION ( 'NONE',  ( 0.000000000000000000, -1.000000000000000000, 0.000000000000000000 ) ) ;
#43300=DIRECTION ( 'NONE',  ( 0.5735764363510554853, 0.8191520442889852482, 0.000000000000000000 ) ) ;
#43305=DIRECTION ( 'NONE',  ( 0.000000000000000000, -1.000000000000000000, 0.000000000000000000 ) ) ;
#43307=CARTESIAN_POINT ( 'NONE',  ( 6.400000000000000355, 0.000000000000000000, 0.000000000000000000 ) ) ;
#43319=DIRECTION ( 'NONE',  ( -1.000000000000000000, -1.224606353822377258E-16, -0.000000000000000000 ) ) ;
#43351=ORIENTED_EDGE ( 'NONE', *, *, #24057, .T. ) ;
#43361=FACE_OUTER_BOUND ( 'NONE', #78426, .T. ) ;
#43373=LINE ( 'NONE', #35309, #99476 ) ;
#43388=DIRECTION ( 'NONE',  ( 0.000000000000000000, 0.000000000000000000, 1.000000000000000000 ) ) ;
#43405=AXIS2_PLACEMENT_3D ( 'NONE', #50088, #66274, #1521 ) ;
#43416=CARTESIAN_POINT ( 'NONE',  ( 102.9313392694734688, -2.002967142162725287E-29, 5.000000000000011546 ) ) ;
#43418=CARTESIAN_POINT ( 'NONE',  ( 101.4868948250290259, -5.000000000000000000, 0.000000000000000000 ) ) ;
#43420=VERTEX_POINT ( 'NONE', #98847 ) ;
#43462=ORIENTED_EDGE ( 'NONE', *, *, #95363, .F. ) ;
#43463=DIRECTION ( 'NONE',  ( -0.5735764363510459374, -0.8191520442889919096, 0.000000000000000000 ) ) ;
#43504=EDGE_LOOP ( 'NONE', ( #72405, #26133, #104169, #39089, #33953 ) ) ;
#43514=EDGE_CURVE ( 'NONE', #93631, #32237, #16349, .T. ) ;
#43520=LINE ( 'NONE', #10079, #50093 ) ;
#43547=LINE ( 'NONE', #86159, #38383 ) ;
#43554=CARTESIAN_POINT ( 'NONE',  ( 0.000000000000000000, 6.123233995736767268E-16, -5.000000000000000888 ) ) ;
#43582=ORIENTED_EDGE ( 'NONE', *, *, #27329, .T. ) ;
#43584=VERTEX_POINT ( 'NONE', #20122 ) ;
#43617=DIRECTION ( 'NONE',  ( 1.000000000000000000, 1.224606353822377258E-16, 0.000000000000000000 ) ) ;
#43685=EDGE_CURVE ( 'NONE', #73379, #87999, #75370, .T. ) ;
#43694=DIRECTION ( 'NONE',  ( 0.000000000000000000, -1.000000000000000000, 0.000000000000000000 ) ) ;
#43696=DIRECTION ( 'NONE',  ( 0.000000000000000000, -1.000000000000000000, 0.000000000000000000 ) ) ;
#43718=CARTESIAN_POINT ( 'NONE',  ( 0.3173508448886554478, 8.480771745766404024, 1.310872448937997259 ) ) ;
#43740=LINE ( 'NONE', #2200, #29337 ) ;
#43742=AXIS2_PLACEMENT_3D ( 'NONE', #22671, #21614, #103560 ) ;
#43761=DIRECTION ( 'NONE',  ( 0.000000000000000000, -1.000000000000000000, 0.000000000000000000 ) ) ;
#43855=ORIENTED_EDGE ( 'NONE', *, *, #71469, .T. ) ;
#43924=FACE_OUTER_BOUND ( 'NONE', #26985, .T. ) ;
#43936=EDGE_CURVE ( 'NONE', #13329, #7841, #41031, .T. ) ;
#43966=VECTOR ( 'NONE', #101847, 1000.000000000000114 ) ;
#43983=ADVANCED_FACE ( 'NONE', ( #81999 ), #18592, .T. ) ;
#43994=ORIENTED_EDGE ( 'NONE', *, *, #37360, .T. ) ;
#44020=DIRECTION ( 'NONE',  ( -1.000000000000000000, -1.224606353822377258E-16, -0.000000000000000000 ) ) ;
#44035=CONICAL_SURFACE ( 'NONE', #57785, 4.172000000000009479, 0.9599310885968813656 ) ;
#44046=ORIENTED_EDGE ( 'NONE', *, *, #11777, .T. ) ;
#44057=VERTEX_POINT ( 'NONE', #66908 ) ;
#44058=DIRECTION ( 'NONE',  ( -1.000000000000000000, -0.000000000000000000, -0.000000000000000000 ) ) ;
#44082=DIRECTION ( 'NONE',  ( 0.000000000000000000, 1.000000000000000000, 0.000000000000000000 ) ) ;
#44111=AXIS2_PLACEMENT_3D ( 'NONE', #67676, #48935, #100559 ) ;
#44125=VECTOR ( 'NONE', #65293, 1000.000000000000000 ) ;
#44156=CIRCLE ( 'NONE', #14876, 5.000000000000011546 ) ;
#44193=CARTESIAN_POINT ( 'NONE',  ( 105.5353273971932140, 1.030564683017419500E-14, 0.000000000000000000 ) ) ;
#44237=ORIENTED_EDGE ( 'NONE', *, *, #47995, .T. ) ;
#44257=FACE_OUTER_BOUND ( 'NONE', #95448, .T. ) ;
#44272=AXIS2_PLACEMENT_3D ( 'NONE', #40899, #32832, #394 ) ;
#44277=ORIENTED_EDGE ( 'NONE', *, *, #78057, .T. ) ;
#44290=DIRECTION ( 'NONE',  ( 0.000000000000000000, -1.000000000000000000, 0.000000000000000000 ) ) ;
#44331=ORIENTED_EDGE ( 'NONE', *, *, #22891, .F. ) ;
#44370=CARTESIAN_POINT ( 'NONE',  ( 0.000000000000000000, -6.928203230275511437, -3.999999999999997335 ) ) ;
#44406=CYLINDRICAL_SURFACE ( 'NONE', #100534, 5.000000000000000888 ) ;
#44418=AXIS2_PLACEMENT_3D ( 'NONE', #35665, #20029, #68544 ) ;
#44434=ORIENTED_EDGE ( 'NONE', *, *, #76241, .F. ) ;
#44442=ORIENTED_EDGE ( 'NONE', *, *, #14617, .T. ) ;
#44540=CARTESIAN_POINT ( 'NONE',  ( 0.000000000000000000, 0.000000000000000000, 0.000000000000000000 ) ) ;
#44547=EDGE_CURVE ( 'NONE', #79234, #39124, #30868, .T. ) ;
#44602=DIRECTION ( 'NONE',  ( 0.000000000000000000, -1.000000000000000000, 0.000000000000000000 ) ) ;
#44606=ORIENTED_EDGE ( 'NONE', *, *, #70487, .F. ) ;
#44623=EDGE_CURVE ( 'NONE', #40910, #35138, #63541, .T. ) ;
#44644=VERTEX_POINT ( 'NONE', #95575 ) ;
#44694=DIRECTION ( 'NONE',  ( 0.000000000000000000, -1.000000000000000000, 0.000000000000000000 ) ) ;
#44804=DIRECTION ( 'NONE',  ( 0.000000000000000000, -1.000000000000000000, 3.755786496842903988E-16 ) ) ;
#44853=CARTESIAN_POINT ( 'NONE',  ( 102.0666666666666629, -4.171999999999998820, 5.616230220889773285E-16 ) ) ;
#44867=CARTESIAN_POINT ( 'NONE',  ( 83.86866073052654258, 1.030564683017419500E-14, 0.000000000000000000 ) ) ;
#44888=DIRECTION ( 'NONE',  ( 0.000000000000000000, -1.000000000000000000, 0.000000000000000000 ) ) ;
#44891=DIRECTION ( 'NONE',  ( 0.000000000000000000, 0.000000000000000000, 1.000000000000000000 ) ) ;
#44902=DIRECTION ( 'NONE',  ( -0.5735764363510461594, 0.8191520442889916875, 1.003171929053524870E-16 ) ) ;
#44910=CARTESIAN_POINT ( 'NONE',  ( 89.64643850830432825, -2.002967142162725287E-29, 5.000000000000011546 ) ) ;
#45126=ORIENTED_EDGE ( 'NONE', *, *, #102686, .F. ) ;
#45153=EDGE_LOOP ( 'NONE', ( #20588, #98806, #41839 ) ) ;
#45191=DIRECTION ( 'NONE',  ( 0.000000000000000000, 1.000000000000000000, 0.000000000000000000 ) ) ;
#45219=VERTEX_POINT ( 'NONE', #66796 ) ;
#45220=CARTESIAN_POINT ( 'NONE',  ( 100.0424503805845831, -5.000000000000000000, 0.000000000000000000 ) ) ;
#45249=APPLICATION_CONTEXT ( 'automotive_design' ) ;
#45379=LINE ( 'NONE', #92846, #52562 ) ;
#45434=VERTEX_POINT ( 'NONE', #65068 ) ;
#45436=CARTESIAN_POINT ( 'NONE',  ( 0.000000000000000000, 0.000000000000000000, 5.000000000000000888 ) ) ;
#45445=AXIS2_PLACEMENT_3D ( 'NONE', #15575, #105643, #48467 ) ;
#45516=EDGE_CURVE ( 'NONE', #33537, #64587, #18906, .T. ) ;
#45550=EDGE_CURVE ( 'NONE', #63169, #6761, #100620, .T. ) ;
#45568=CARTESIAN_POINT ( 'NONE',  ( 102.9313392694734688, 1.016364837396684119E-14, 0.000000000000000000 ) ) ;
#45569=DIRECTION ( 'NONE',  ( 0.000000000000000000, -0.8660254037844381525, 0.5000000000000008882 ) ) ;
#45581=EDGE_CURVE ( 'NONE', #41052, #8974, #59651, .T. ) ;
#45582=AXIS2_PLACEMENT_3D ( 'NONE', #87417, #5422, #55533 ) ;
#45605=CONICAL_SURFACE ( 'NONE', #74823, 8.000000000000000000, 1.047197551196600296 ) ;
#45607=CARTESIAN_POINT ( 'NONE',  ( 0.000000000000000000, 0.000000000000000000, 0.000000000000000000 ) ) ;
#45611=CIRCLE ( 'NONE', #66293, 5.000000000000010658 ) ;
#45638=EDGE_LOOP ( 'NONE', ( #102307, #6751, #104406, #20131, #76047, #39374 ) ) ;
#45674=EDGE_CURVE ( 'NONE', #101774, #40136, #65372, .T. ) ;
#45741=CIRCLE ( 'NONE', #2683, 5.000000000000011546 ) ;
#45771=ORIENTED_EDGE ( 'NONE', *, *, #68542, .F. ) ;
#45777=ORIENTED_EDGE ( 'NONE', *, *, #11777, .F. ) ;
#45834=ORIENTED_EDGE ( 'NONE', *, *, #89046, .T. ) ;
#45848=ORIENTED_EDGE ( 'NONE', *, *, #36180, .F. ) ;
#45862=ORIENTED_EDGE ( 'NONE', *, *, #99777, .T. ) ;
#45874=CARTESIAN_POINT ( 'NONE',  ( 0.000000000000000000, 0.000000000000000000, 0.000000000000000000 ) ) ;
#45902=CONICAL_SURFACE ( 'NONE', #106150, 8.000000000000000000, 1.047197551196600296 ) ;
#45931=DIRECTION ( 'NONE',  ( 0.000000000000000000, 0.000000000000000000, 1.000000000000000000 ) ) ;
#45933=VERTEX_POINT ( 'NONE', #15597 ) ;
#45936=DIRECTION ( 'NONE',  ( -0.000000000000000000, 1.000000000000000000, -1.224646799147353207E-16 ) ) ;
#45973=VERTEX_POINT ( 'NONE', #16129 ) ;
#46006=CYLINDRICAL_SURFACE ( 'NONE', #36171, 5.000000000000000888 ) ;
#46014=CARTESIAN_POINT ( 'NONE',  ( 96.86866073052655679, -5.000000000000000888, 6.123233995736779101E-16 ) ) ;
#46047=ORIENTED_EDGE ( 'NONE', *, *, #51210, .F. ) ;
#46064=DIRECTION ( 'NONE',  ( -1.000000000000000000, -0.000000000000000000, -0.000000000000000000 ) ) ;
#46093=PLANE ( 'NONE',  #40874 ) ;
#46143=ORIENTED_EDGE ( 'NONE', *, *, #68349, .F. ) ;
#46163=CARTESIAN_POINT ( 'NONE',  ( 86.75754961941542831, 5.000000000000021316, 0.000000000000000000 ) ) ;
#46179=CIRCLE ( 'NONE', #97811, 5.000000000000010658 ) ;
#46193=AXIS2_PLACEMENT_3D ( 'NONE', #41847, #67731, #41316 ) ;
#46248=ORIENTED_EDGE ( 'NONE', *, *, #6415, .F. ) ;
#46252=DIRECTION ( 'NONE',  ( 0.000000000000000000, 0.000000000000000000, -1.000000000000000000 ) ) ;
#46294=ORIENTED_EDGE ( 'NONE', *, *, #7874, .F. ) ;
#46306=ORIENTED_EDGE ( 'NONE', *, *, #77541, .T. ) ;
#46417=DIRECTION ( 'NONE',  ( 0.000000000000000000, -1.000000000000000000, 0.000000000000000000 ) ) ;
#46425=VECTOR ( 'NONE', #59564, 1000.000000000000000 ) ;
#46489=CARTESIAN_POINT ( 'NONE',  ( 0.000000000000000000, 0.000000000000000000, 0.000000000000000000 ) ) ;
#46541=EDGE_LOOP ( 'NONE', ( #13847, #36602, #39293, #76143, #4559, #89395 ) ) ;
#46546=CARTESIAN_POINT ( 'NONE',  ( 6.400000000000000355, 4.618802153517003184, -8.000000000000000000 ) ) ;
#46609=DIRECTION ( 'NONE',  ( 0.000000000000000000, -1.000000000000000000, 0.000000000000000000 ) ) ;
#46642=ORIENTED_EDGE ( 'NONE', *, *, #2642, .F. ) ;
#46663=EDGE_CURVE ( 'NONE', #35844, #34646, #83659, .T. ) ;
#46664=ORIENTED_EDGE ( 'NONE', *, *, #47901, .T. ) ;
#46669=CARTESIAN_POINT ( 'NONE',  ( 89.64643850830432825, 6.123233995736568081E-16, -5.000000000000011546 ) ) ;
#46682=CONICAL_SURFACE ( 'NONE', #22622, 4.172000000000009479, 0.9599310885968813656 ) ;
#46683=ORIENTED_EDGE ( 'NONE', *, *, #70864, .F. ) ;
#46684=EDGE_LOOP ( 'NONE', ( #13241, #11726, #16642, #32814, #68618, #33177 ) ) ;
#46735=FACE_OUTER_BOUND ( 'NONE', #9505, .T. ) ;
#46752=ORIENTED_EDGE ( 'NONE', *, *, #95363, .T. ) ;
#46760=ORIENTED_EDGE ( 'NONE', *, *, #82631, .F. ) ;
#46774=ORIENTED_EDGE ( 'NONE', *, *, #63165, .T. ) ;
#46796=CARTESIAN_POINT ( 'NONE',  ( 89.06666666666666288, 1.023464760207051730E-14, 0.000000000000000000 ) ) ;
#46802=CARTESIAN_POINT ( 'NONE',  ( 0.06730325657375718640, -1.557442666578432444, -8.000000000000001776 ) ) ;
#46865=ORIENTED_EDGE ( 'NONE', *, *, #72650, .F. ) ;
#46886=CONICAL_SURFACE ( 'NONE', #105421, 4.171999999999999709, 0.7853981633974603804 ) ;
#46895=CARTESIAN_POINT ( 'NONE',  ( 0.000000000000000000, 3.004629197474323585E-15, 8.000000000000000000 ) ) ;
#46899=AXIS2_PLACEMENT_3D ( 'NONE', #86102, #12172, #62348 ) ;
#46903=EDGE_CURVE ( 'NONE', #43420, #9728, #53510, .T. ) ;
#46916=EDGE_CURVE ( 'NONE', #73615, #65096, #89617, .T. ) ;
#46927=AXIS2_PLACEMENT_3D ( 'NONE', #81659, #73575, #82204 ) ;
#46957=EDGE_CURVE ( 'NONE', #59097, #18574, #60388, .T. ) ;
#46987=VERTEX_POINT ( 'NONE', #40965 ) ;
#47011=ORIENTED_EDGE ( 'NONE', *, *, #43514, .T. ) ;
#47042=DIRECTION ( 'NONE',  ( -1.000000000000000000, -0.000000000000000000, -0.000000000000000000 ) ) ;
#47118=DIRECTION ( 'NONE',  ( -1.000000000000000000, -1.224606353822377258E-16, -0.000000000000000000 ) ) ;
#47128=DIRECTION ( 'NONE',  ( -1.000000000000000000, -1.224606353822377258E-16, -0.000000000000000000 ) ) ;
#47180=ADVANCED_FACE ( 'NONE', ( #84618 ), #9639, .F. ) ;
#47220=CIRCLE ( 'NONE', #62793, 5.000000000000010658 ) ;
#47241=DIRECTION ( 'NONE',  ( -1.000000000000000000, -1.224606353822377258E-16, -0.000000000000000000 ) ) ;
#47263=AXIS2_PLACEMENT_3D ( 'NONE', #48105, #13619, #63264 ) ;
#47264=CYLINDRICAL_SURFACE ( 'NONE', #48804, 5.000000000000000888 ) ;
#47319=ORIENTED_EDGE ( 'NONE', *, *, #84026, .F. ) ;
#47323=DIRECTION ( 'NONE',  ( 0.000000000000000000, 1.000000000000000000, 0.000000000000000000 ) ) ;
#47344=CIRCLE ( 'NONE', #26756, 4.172000000000009479 ) ;
#47376=PRODUCT_DEFINITION_FORMATION_WITH_SPECIFIED_SOURCE ( 'ANY', '', #101837, .NOT_KNOWN. ) ;
#47398=ORIENTED_EDGE ( 'NONE', *, *, #103451, .F. ) ;
#47423=CARTESIAN_POINT ( 'NONE',  ( -1.002887009549091601E-15, -0.7818963811860187851, 8.000000000000000000 ) ) ;
#47505=AXIS2_PLACEMENT_3D ( 'NONE', #5836, #79731, #54363 ) ;
#47524=ORIENTED_EDGE ( 'NONE', *, *, #38172, .T. ) ;
#47534=DIRECTION ( 'NONE',  ( 0.000000000000000000, -0.5000000000000008882, 0.8660254037844381525 ) ) ;
#47557=CONICAL_SURFACE ( 'NONE', #83677, 4.172000000000009479, 0.9599310885968813656 ) ;
#47582=ORIENTED_EDGE ( 'NONE', *, *, #46916, .T. ) ;
#47677=CARTESIAN_POINT ( 'NONE',  ( 5.799999999999999822, 4.618802153517003184, -8.000000000000000000 ) ) ;
#47699=FACE_OUTER_BOUND ( 'NONE', #21538, .T. ) ;
#47724=CIRCLE ( 'NONE', #25366, 5.000000000000010658 ) ;
#47731=DIRECTION ( 'NONE',  ( 0.5735764363510557073, -0.8191520442889850262, 1.003171929053516612E-16 ) ) ;
#47791=EDGE_CURVE ( 'NONE', #2944, #37934, #86110, .T. ) ;
#47814=DIRECTION ( 'NONE',  ( -1.000000000000000000, -1.224606353822377258E-16, -0.000000000000000000 ) ) ;
#47822=DIRECTION ( 'NONE',  ( -0.000000000000000000, 0.000000000000000000, 1.000000000000000000 ) ) ;
#47878=DIRECTION ( 'NONE',  ( 1.000000000000000000, 0.000000000000000000, 0.000000000000000000 ) ) ;
#47901=EDGE_CURVE ( 'NONE', #101241, #59097, #13239, .T. ) ;
#47917=EDGE_CURVE ( 'NONE', #41052, #20613, #91557, .T. ) ;
#47929=AXIS2_PLACEMENT_3D ( 'NONE', #64368, #97241, #23386 ) ;
#47991=CARTESIAN_POINT ( 'NONE',  ( 82.42421628608209971, 1.030564683017419500E-14, 0.000000000000000000 ) ) ;
#47995=EDGE_CURVE ( 'NONE', #36994, #92586, #36462, .T. ) ;
#48011=DIRECTION ( 'NONE',  ( -0.5735764363510461594, 0.8191520442889916875, 1.003171929053524870E-16 ) ) ;
#48016=VERTEX_POINT ( 'NONE', #65522 ) ;
#48044=EDGE_CURVE ( 'NONE', #8019, #53170, #83933, .T. ) ;
#48080=CARTESIAN_POINT ( 'NONE',  ( 0.7145311798163270778, 9.237604307034018802, 3.185620757954082679E-16 ) ) ;
#48102=EDGE_CURVE ( 'NONE', #17510, #31444, #43373, .T. ) ;
#48105=CARTESIAN_POINT ( 'NONE',  ( 84.15356149169568312, 1.016364837396684119E-14, 0.000000000000000000 ) ) ;
#48111=AXIS2_PLACEMENT_3D ( 'NONE', #41720, #43319, #100481 ) ;
#48118=DIRECTION ( 'NONE',  ( 0.000000000000000000, -1.000000000000000000, 0.000000000000000000 ) ) ;
#48121=DIRECTION ( 'NONE',  ( 0.000000000000000000, 0.000000000000000000, 1.000000000000000000 ) ) ;
#48172=PRODUCT_CONTEXT ( 'NONE', #17676, 'mechanical' ) ;
#48179=CARTESIAN_POINT ( 'NONE',  ( 0.000000000000000000, 0.000000000000000000, 0.000000000000000000 ) ) ;
#48194=EDGE_CURVE ( 'NONE', #49541, #7953, #32294, .T. ) ;
#48226=LINE ( 'NONE', #8306, #87743 ) ;
#48228=CYLINDRICAL_SURFACE ( 'NONE', #33086, 5.000000000000000888 ) ;
#48244=DIRECTION ( 'NONE',  ( 0.000000000000000000, -1.000000000000000000, 0.000000000000000000 ) ) ;
#48257=VECTOR ( 'NONE', #33030, 1000.000000000000000 ) ;
#48282=AXIS2_PLACEMENT_3D ( 'NONE', #35172, #2768, #10325 ) ;
#48309=AXIS2_PLACEMENT_3D ( 'NONE', #103463, #20489, #60894 ) ;
#48358=CIRCLE ( 'NONE', #65623, 4.172000000000009479 ) ;
#48361=FACE_OUTER_BOUND ( 'NONE', #13101, .T. ) ;
#48369=CIRCLE ( 'NONE', #55219, 5.000000000000010658 ) ;
#48416=CARTESIAN_POINT ( 'NONE',  ( 97.15356149169568312, -5.000000000000020428, 0.000000000000000000 ) ) ;
#48450=EDGE_CURVE ( 'NONE', #58313, #15045, #27155, .T. ) ;
#48451=DIRECTION ( 'NONE',  ( -1.000000000000000000, -1.224606353822377258E-16, -0.000000000000000000 ) ) ;
#48467=DIRECTION ( 'NONE',  ( 0.000000000000000000, -1.000000000000000000, 0.000000000000000000 ) ) ;
#48502=DIRECTION ( 'NONE',  ( 0.000000000000000000, -1.000000000000000000, 0.000000000000000000 ) ) ;
#48515=VERTEX_POINT ( 'NONE', #52790 ) ;
#48532=EDGE_CURVE ( 'NONE', #45434, #21657, #89095, .T. ) ;
#48551=DIRECTION ( 'NONE',  ( 0.000000000000000000, -1.000000000000000000, 0.000000000000000000 ) ) ;
#48577=ORIENTED_EDGE ( 'NONE', *, *, #89928, .F. ) ;
#48617=EDGE_LOOP ( 'NONE', ( #74534, #46865, #23261, #53778, #44046 ) ) ;
#48663=CARTESIAN_POINT ( 'NONE',  ( 79.82022815836235452, 1.016364837396684119E-14, 0.000000000000000000 ) ) ;
#48668=EDGE_CURVE ( 'NONE', #8019, #102339, #29591, .T. ) ;
#48687=LINE ( 'NONE', #16334, #61320 ) ;
#48746=DIRECTION ( 'NONE',  ( -1.000000000000000000, -0.000000000000000000, -0.000000000000000000 ) ) ;
#48747=CARTESIAN_POINT ( 'NONE',  ( 5.799999999999999822, -6.928203230275505220, 4.000000000000007994 ) ) ;
#48781=ORIENTED_EDGE ( 'NONE', *, *, #75060, .F. ) ;
#48794=ADVANCED_FACE ( 'NONE', ( #13879 ), #53383, .T. ) ;
#48800=CONICAL_SURFACE ( 'NONE', #103929, 5.000000000000010658, 0.9599310885968697082 ) ;
#48804=AXIS2_PLACEMENT_3D ( 'NONE', #20935, #53771, #80161 ) ;
#48822=ORIENTED_EDGE ( 'NONE', *, *, #80082, .T. ) ;
#48835=EDGE_CURVE ( 'NONE', #13365, #9366, #22386, .T. ) ;
#48878=LINE ( 'NONE', #42940, #1934 ) ;
#48886=UNCERTAINTY_MEASURE_WITH_UNIT (LENGTH_MEASURE( 1.000000000000000082E-05 ), #114, 'distance_accuracy_value', 'NONE');
#48911=EDGE_LOOP ( 'NONE', ( #37151, #82161, #28054, #52865, #100493 ) ) ;
#48920=FACE_OUTER_BOUND ( 'NONE', #55730, .T. ) ;
#48934=ORIENTED_EDGE ( 'NONE', *, *, #43685, .T. ) ;
#48935=DIRECTION ( 'NONE',  ( 1.000000000000000000, 1.224606353822377258E-16, 0.000000000000000000 ) ) ;
#48946=ORIENTED_EDGE ( 'NONE', *, *, #79774, .F. ) ;
#48975=AXIS2_PLACEMENT_3D ( 'NONE', #98694, #1040, #57699 ) ;
#48998=CIRCLE ( 'NONE', #2519, 5.000000000000011546 ) ;
#49027=DIRECTION ( 'NONE',  ( 0.5735764363510557073, -0.8191520442889850262, 1.003171929053516612E-16 ) ) ;
#49085=VECTOR ( 'NONE', #42161, 1000.000000000000000 ) ;
#49122=VERTEX_POINT ( 'NONE', #46669 ) ;
#49140=VERTEX_POINT ( 'NONE', #13759 ) ;
#49201=FACE_OUTER_BOUND ( 'NONE', #38769, .T. ) ;
#49232=ORIENTED_EDGE ( 'NONE', *, *, #50933, .T. ) ;
#49272=ORIENTED_EDGE ( 'NONE', *, *, #38768, .T. ) ;
#49316=ADVANCED_FACE ( 'NONE', ( #98401 ), #79318, .T. ) ;
#49318=ORIENTED_EDGE ( 'NONE', *, *, #50786, .F. ) ;
#49322=AXIS2_PLACEMENT_3D ( 'NONE', #99382, #57868, #74056 ) ;
#49402=CARTESIAN_POINT ( 'NONE',  ( 0.4969600502617449456, -4.995646404165267285, 7.347286611336970807 ) ) ;
#49417=CARTESIAN_POINT ( 'NONE',  ( 88.20199406385988539, -5.000000000000000000, 6.123233995736778115E-16 ) ) ;
#49425=ORIENTED_EDGE ( 'NONE', *, *, #29370, .T. ) ;
#49436=DIRECTION ( 'NONE',  ( 0.000000000000000000, -1.000000000000000000, 0.000000000000000000 ) ) ;
#49446=CONICAL_SURFACE ( 'NONE', #37491, 5.000000000000010658, 0.9599310885968697082 ) ;
#49450=ORIENTED_EDGE ( 'NONE', *, *, #28060, .T. ) ;
#49458=ADVANCED_FACE ( 'NONE', ( #3439 ), #77326, .T. ) ;
#49463=ORIENTED_EDGE ( 'NONE', *, *, #33907, .T. ) ;
#49478=FACE_OUTER_BOUND ( 'NONE', #38311, .T. ) ;
#49495=VERTEX_POINT ( 'NONE', #26686 ) ;
#49503=DIRECTION ( 'NONE',  ( -1.000000000000000000, -0.000000000000000000, -0.000000000000000000 ) ) ;
#49510=CARTESIAN_POINT ( 'NONE',  ( 85.31310517497098544, 5.000000000000021316, 0.000000000000000000 ) ) ;
#49541=VERTEX_POINT ( 'NONE', #35842 ) ;
#49572=DIRECTION ( 'NONE',  ( 0.000000000000000000, -1.000000000000000000, 0.000000000000000000 ) ) ;
#49616=VERTEX_POINT ( 'NONE', #105316 ) ;
#49682=EDGE_CURVE ( 'NONE', #52131, #9396, #37435, .T. ) ;
#49717=ORIENTED_EDGE ( 'NONE', *, *, #10775, .F. ) ;
#49735=EDGE_LOOP ( 'NONE', ( #18730, #12859, #47582, #11567, #84081 ) ) ;
#49742=ADVANCED_FACE ( 'NONE', ( #24438 ), #15236, .T. ) ;
#49754=FACE_OUTER_BOUND ( 'NONE', #28970, .T. ) ;
#49764=CLOSED_SHELL ( 'NONE', ( #90473, #51356, #43134, #53837, #62095, #15031, #29072, #92333, #21281, #35622, #20165, #63755, #24749, #9030, #59048, #88275, #84085, #22551, #32687, #87467, #57307, #58251, #13666, #99986, #294, #15981, #72054, #56899, #105596, #33418, #34323, #24828, #16090, #65779, #50507, #48794, #101128, #62036, #62029, #88989, #104789, #22472, #103125, #102191, #59938, #88677, #23143, #70074, #83493, #68560, #25636, #54358, #32235, #19126, #101514, #92267, #32056, #99909, #106523, #36729, #17273, #104955, #102932, #19443, #7207, #73745, #65843, #2927, #85640, #11011, #15334, #10793, #71726, #82791, #33014, #47180, #58021, #26118, #58664, #7675, #81324, #40893, #669, #18149, #11487, #86398, #96655, #66769, #50872, #92599, #26303, #16408, #40572, #92721, #69230, #92335, #87883, #79701, #61354, #86532, #79726, #76459, #81664, #14193, #68623, #34075, #78793, #7947, #3243, #104801, #42514, #13023, #67967, #56187, #43983, #23331, #49458, #49316, #52676, #70744, #52029, #51534, #25085, #53850, #14698, #83289, #32777, #79909, #19805, #13643, #92190, #62340, #62358, #11484, #37707, #97543, #49742 ) ) ;
#49773=EDGE_CURVE ( 'NONE', #36517, #13469, #61031, .T. ) ;
#49820=DIRECTION ( 'NONE',  ( -1.000000000000000000, -1.224606353822377258E-16, -0.000000000000000000 ) ) ;
#49824=EDGE_CURVE ( 'NONE', #63286, #4234, #94817, .T. ) ;
#49833=ORIENTED_EDGE ( 'NONE', *, *, #68108, .F. ) ;
#49880=ORIENTED_EDGE ( 'NONE', *, *, #23809, .T. ) ;
#49886=EDGE_LOOP ( 'NONE', ( #11600, #13752, #45862, #76180, #17247, #94051 ) ) ;
#49934=DIRECTION ( 'NONE',  ( -1.000000000000000000, -0.000000000000000000, -0.000000000000000000 ) ) ;
#49989=ORIENTED_EDGE ( 'NONE', *, *, #68521, .F. ) ;
#49997=DIRECTION ( 'NONE',  ( 0.000000000000000000, -1.000000000000000000, 0.000000000000000000 ) ) ;
#50001=CIRCLE ( 'NONE', #91356, 5.000000000000011546 ) ;
#50029=DIRECTION ( 'NONE',  ( -1.000000000000000000, -1.224606353822377258E-16, -0.000000000000000000 ) ) ;
#50035=CARTESIAN_POINT ( 'NONE',  ( 97.73333333333333428, 4.172000000000019249, 5.109226446042768454E-16 ) ) ;
#50052=DIRECTION ( 'NONE',  ( -1.000000000000000000, -0.000000000000000000, -0.000000000000000000 ) ) ;
#50054=EDGE_CURVE ( 'NONE', #4234, #22906, #63868, .T. ) ;
#50057=ORIENTED_EDGE ( 'NONE', *, *, #14073, .T. ) ;
#50059=EDGE_CURVE ( 'NONE', #75948, #101891, #34632, .T. ) ;
#50087=DIRECTION ( 'NONE',  ( -1.000000000000000000, -1.224606353822377258E-16, -0.000000000000000000 ) ) ;
#50088=CARTESIAN_POINT ( 'NONE',  ( 6.400000000000000355, 9.237604307034020579, -1.850927914596627675E-15 ) ) ;
#50093=VECTOR ( 'NONE', #75876, 1000.000000000000000 ) ;
#50094=DIRECTION ( 'NONE',  ( 0.000000000000000000, 1.000000000000000000, 0.000000000000000000 ) ) ;
#50096=ORIENTED_EDGE ( 'NONE', *, *, #135, .T. ) ;
#50147=AXIS2_PLACEMENT_3D ( 'NONE', #50539, #76421, #59733 ) ;
#50203=AXIS2_PLACEMENT_3D ( 'NONE', #72180, #98042, #81836 ) ;
#50240=DIRECTION ( 'NONE',  ( -1.000000000000000000, -1.224606353822377258E-16, -0.000000000000000000 ) ) ;
#50259=DIRECTION ( 'NONE',  ( -1.000000000000000000, -1.224606353822377258E-16, -0.000000000000000000 ) ) ;
#50315=CYLINDRICAL_SURFACE ( 'NONE', #49322, 5.000000000000000888 ) ;
#50343=ORIENTED_EDGE ( 'NONE', *, *, #30394, .T. ) ;
#50366=CARTESIAN_POINT ( 'NONE',  ( 0.3194001229792603480, 3.115132258397520282, 7.999999999999996447 ) ) ;
#50435=CARTESIAN_POINT ( 'NONE',  ( 84.15356149169568312, 1.016364837396684119E-14, 0.000000000000000000 ) ) ;
#50487=CARTESIAN_POINT ( 'NONE',  ( 82.42421628608209971, 1.030564683017419500E-14, 0.000000000000000000 ) ) ;
#50498=ORIENTED_EDGE ( 'NONE', *, *, #42157, .T. ) ;
#50507=ADVANCED_FACE ( 'NONE', ( #83302 ), #85441, .T. ) ;
#50512=LINE ( 'NONE', #25779, #56155 ) ;
#50529=MECHANICAL_DESIGN_GEOMETRIC_PRESENTATION_REPRESENTATION('',(#9175),#74631);
#50539=CARTESIAN_POINT ( 'NONE',  ( 89.93133926947346879, 1.016364837396684119E-14, 0.000000000000000000 ) ) ;
#50546=DIRECTION ( 'NONE',  ( 0.000000000000000000, -1.000000000000000000, 0.000000000000000000 ) ) ;
#50555=LINE ( 'NONE', #49510, #71169 ) ;
#50644=B_SPLINE_CURVE_WITH_KNOTS ( 'NONE', 3,
 ( #15799, #24981, #39568, #63839, #104814, #30963 ),
 .UNSPECIFIED., .F., .F.,
 ( 4, 2, 4 ),
 ( 2.380731629579044207E-07, 0.002336973833157560739, 0.004673709593152165255 ),
 .UNSPECIFIED. ) ;
#50751=CARTESIAN_POINT ( 'NONE',  ( 102.9313392694734688, 5.000000000000023093, 6.123233995736781074E-16 ) ) ;
#50757=CYLINDRICAL_SURFACE ( 'NONE', #81649, 5.000000000000000888 ) ;
#50765=CARTESIAN_POINT ( 'NONE',  ( 0.000000000000000000, 0.000000000000000000, 0.000000000000000000 ) ) ;
#50786=EDGE_CURVE ( 'NONE', #57410, #43420, #95656, .T. ) ;
#50817=DIRECTION ( 'NONE',  ( -0.5735764363510461594, 0.8191520442889916875, 1.003171929053524870E-16 ) ) ;
#50852=DIRECTION ( 'NONE',  ( -1.000000000000000000, -0.000000000000000000, -0.000000000000000000 ) ) ;
#50872=ADVANCED_FACE ( 'NONE', ( #49201 ), #100099, .T. ) ;
#50898=DIRECTION ( 'NONE',  ( 0.000000000000000000, -1.000000000000000000, 0.000000000000000000 ) ) ;
#50920=ORIENTED_EDGE ( 'NONE', *, *, #25136, .T. ) ;
#50921=DIRECTION ( 'NONE',  ( -1.000000000000000000, -1.224606353822377258E-16, -0.000000000000000000 ) ) ;
#50933=EDGE_CURVE ( 'NONE', #99558, #64598, #15710, .T. ) ;
#50955=DIRECTION ( 'NONE',  ( -1.000000000000000000, -1.224606353822377258E-16, -0.000000000000000000 ) ) ;
#51060=DIRECTION ( 'NONE',  ( 0.000000000000000000, -1.000000000000000000, 0.000000000000000000 ) ) ;
#51125=AXIS2_PLACEMENT_3D ( 'NONE', #33141, #41734, #89767 ) ;
#51146=CARTESIAN_POINT ( 'NONE',  ( 101.2019940638598854, 1.030564683017419500E-14, 0.000000000000000000 ) ) ;
#51164=AXIS2_PLACEMENT_3D ( 'NONE', #93727, #19881, #27438 ) ;
#51197=AXIS2_PLACEMENT_3D ( 'NONE', #68729, #67116, #26171 ) ;
#51210=EDGE_CURVE ( 'NONE', #10713, #97033, #98472, .T. ) ;
#51212=DIRECTION ( 'NONE',  ( -1.000000000000000000, -1.224606353822377258E-16, -0.000000000000000000 ) ) ;
#51222=CONICAL_SURFACE ( 'NONE', #70192, 5.000000000000010658, 0.9599310885968697082 ) ;
#51262=DIRECTION ( 'NONE',  ( 1.000000000000000000, 1.224606353822377258E-16, 0.000000000000000000 ) ) ;
#51274=EDGE_LOOP ( 'NONE', ( #425, #5404, #87519, #56905 ) ) ;
#51320=DIRECTION ( 'NONE',  ( 0.000000000000000000, 0.000000000000000000, -1.000000000000000000 ) ) ;
#51325=CIRCLE ( 'NONE', #91007, 5.000000000000010658 ) ;
#51344=DIRECTION ( 'NONE',  ( 0.000000000000000000, 0.000000000000000000, 1.000000000000000000 ) ) ;
#51350=EDGE_LOOP ( 'NONE', ( #30966, #88936, #96403, #26165, #92704 ) ) ;
#51356=ADVANCED_FACE ( 'NONE', ( #68348 ), #46886, .T. ) ;
#51392=CARTESIAN_POINT ( 'NONE',  ( 0.000000000000000000, 6.123233995736767268E-16, -5.000000000000000888 ) ) ;
#51453=DIRECTION ( 'NONE',  ( -0.5735764363510461594, 0.8191520442889916875, 1.003171929053524870E-16 ) ) ;
#51471=CARTESIAN_POINT ( 'NONE',  ( 5.799999999999999822, 4.618802153517003184, -8.000000000000000000 ) ) ;
#51499=CARTESIAN_POINT ( 'NONE',  ( 104.9555555555555486, 1.023464760207051730E-14, 0.000000000000000000 ) ) ;
#51522=VERTEX_POINT ( 'NONE', #95669 ) ;
#51530=AXIS2_PLACEMENT_3D ( 'NONE', #11997, #69203, #60584 ) ;
#51534=ADVANCED_FACE ( 'NONE', ( #24985 ), #89942, .T. ) ;
#51611=DIRECTION ( 'NONE',  ( 0.000000000000000000, 0.000000000000000000, 1.000000000000000000 ) ) ;
#51632=VECTOR ( 'NONE', #33211, 1000.000000000000000 ) ;
#51633=DIRECTION ( 'NONE',  ( -0.7071067811865390240, 8.659560562355038861E-17, -0.7071067811865561215 ) ) ;
#51654=VECTOR ( 'NONE', #76435, 1000.000000000000000 ) ;
#51690=CARTESIAN_POINT ( 'NONE',  ( 0.000000000000000000, 0.000000000000000000, 5.000000000000000888 ) ) ;
#51705=VECTOR ( 'NONE', #50817, 999.9999999999998863 ) ;
#51720=DIRECTION ( 'NONE',  ( -1.000000000000000000, -1.224606353822377258E-16, -0.000000000000000000 ) ) ;
#51724=EDGE_CURVE ( 'NONE', #30465, #59238, #69258, .T. ) ;
#51738=ORIENTED_EDGE ( 'NONE', *, *, #19524, .T. ) ;
#51744=VECTOR ( 'NONE', #14302, 1000.000000000000000 ) ;
#51759=VECTOR ( 'NONE', #48011, 999.9999999999998863 ) ;
#51772=FACE_OUTER_BOUND ( 'NONE', #99248, .T. ) ;
#51774=ORIENTED_EDGE ( 'NONE', *, *, #82938, .F. ) ;
#51797=ORIENTED_EDGE ( 'NONE', *, *, #106403, .F. ) ;
#51802=FACE_OUTER_BOUND ( 'NONE', #42856, .T. ) ;
#51852=FACE_OUTER_BOUND ( 'NONE', #105119, .T. ) ;
#51864=AXIS2_PLACEMENT_3D ( 'NONE', #1435, #82371, #58645 ) ;
#51873=DIRECTION ( 'NONE',  ( 1.000000000000000000, 1.224606353822377258E-16, 0.000000000000000000 ) ) ;
#51947=DIRECTION ( 'NONE',  ( 0.000000000000000000, 1.000000000000000000, 0.000000000000000000 ) ) ;
#51950=DIRECTION ( 'NONE',  ( 0.000000000000000000, 0.000000000000000000, 1.000000000000000000 ) ) ;
#52013=CIRCLE ( 'NONE', #93380, 5.000000000000010658 ) ;
#52029=ADVANCED_FACE ( 'NONE', ( #86704 ), #74598, .T. ) ;
#52045=ORIENTED_EDGE ( 'NONE', *, *, #76810, .F. ) ;
#52131=VERTEX_POINT ( 'NONE', #106022 ) ;
#52237=ORIENTED_EDGE ( 'NONE', *, *, #18279, .F. ) ;
#52260=CARTESIAN_POINT ( 'NONE',  ( 0.3167204509598351980, 5.377136764700157556, 6.686525924292787693 ) ) ;
#52267=CIRCLE ( 'NONE', #81502, 5.000000000000011546 ) ;
#52270=DIRECTION ( 'NONE',  ( -1.000000000000000000, -1.224606353822377258E-16, -0.000000000000000000 ) ) ;
#52335=CARTESIAN_POINT ( 'NONE',  ( 91.09088295274877112, -5.000000000000000888, 6.123233995736779101E-16 ) ) ;
#52397=EDGE_LOOP ( 'NONE', ( #31052, #32742, #75084, #44434, #26265, #46294 ) ) ;
#52420=CIRCLE ( 'NONE', #5911, 5.000000000000011546 ) ;
#52436=LINE ( 'NONE', #78312, #94156 ) ;
#52468=ORIENTED_EDGE ( 'NONE', *, *, #65619, .F. ) ;
#52495=AXIS2_PLACEMENT_3D ( 'NONE', #43307, #58969, #68104 ) ;
#52558=DIRECTION ( 'NONE',  ( 0.000000000000000000, -1.000000000000000000, 0.000000000000000000 ) ) ;
#52562=VECTOR ( 'NONE', #12451, 1000.000000000000000 ) ;
#52622=ORIENTED_EDGE ( 'NONE', *, *, #42330, .F. ) ;
#52623=CARTESIAN_POINT ( 'NONE',  ( 88.48689482502902592, 1.016364837396684119E-14, 0.000000000000000000 ) ) ;
#52666=VECTOR ( 'NONE', #72449, 1000.000000000000000 ) ;
#52667=CARTESIAN_POINT ( 'NONE',  ( 100.6222222222222200, 1.023464760207051730E-14, 0.000000000000000000 ) ) ;
#52676=ADVANCED_FACE ( 'NONE', ( #13450 ), #24747, .T. ) ;
#52717=VECTOR ( 'NONE', #35073, 1000.000000000000000 ) ;
#52737=PLANE ( 'NONE',  #93274 ) ;
#52753=ORIENTED_EDGE ( 'NONE', *, *, #43936, .T. ) ;
#52759=EDGE_CURVE ( 'NONE', #10334, #46987, #100388, .T. ) ;
#52773=DIRECTION ( 'NONE',  ( 0.000000000000000000, -0.4999999999999996114, 0.8660254037844388186 ) ) ;
#52780=ORIENTED_EDGE ( 'NONE', *, *, #102752, .F. ) ;
#52790=CARTESIAN_POINT ( 'NONE',  ( 86.17777777777776294, -4.171999999999998820, 5.616230220889773285E-16 ) ) ;
#52799=ORIENTED_EDGE ( 'NONE', *, *, #18306, .F. ) ;
#52813=CARTESIAN_POINT ( 'NONE',  ( 88.48689482502902592, -2.002967142162725287E-29, 5.000000000000011546 ) ) ;
#52851=DIRECTION ( 'NONE',  ( -1.000000000000000000, -1.224606353822377258E-16, -0.000000000000000000 ) ) ;
#52865=ORIENTED_EDGE ( 'NONE', *, *, #48450, .T. ) ;
#53064=ORIENTED_EDGE ( 'NONE', *, *, #92084, .F. ) ;
#53075=CARTESIAN_POINT ( 'NONE',  ( 89.93133926947346879, 6.123233995736582872E-16, -5.000000000000011546 ) ) ;
#53145=AXIS2_PLACEMENT_3D ( 'NONE', #38214, #106083, #47323 ) ;
#53170=VERTEX_POINT ( 'NONE', #172 ) ;
#53206=VERTEX_POINT ( 'NONE', #33135 ) ;
#53227=AXIS2_PLACEMENT_3D ( 'NONE', #51499, #50955, #52558 ) ;
#53240=EDGE_CURVE ( 'NONE', #42388, #10713, #10762, .T. ) ;
#53241=AXIS2_PLACEMENT_3D ( 'NONE', #60186, #25709, #100071 ) ;
#53296=EDGE_CURVE ( 'NONE', #29639, #45973, #23036, .T. ) ;
#53316=CIRCLE ( 'NONE', #87738, 5.000000000000011546 ) ;
#53335=CARTESIAN_POINT ( 'NONE',  ( 106.4000000000000057, 0.000000000000000000, 0.000000000000000000 ) ) ;
#53353=ORIENTED_EDGE ( 'NONE', *, *, #86606, .F. ) ;
#53368=AXIS2_PLACEMENT_3D ( 'NONE', #67308, #16615, #10116 ) ;
#53383=CONICAL_SURFACE ( 'NONE', #94756, 4.172000000000009479, 0.9599310885968813656 ) ;
#53403=AXIS2_PLACEMENT_3D ( 'NONE', #87632, #103282, #70909 ) ;
#53426=ORIENTED_EDGE ( 'NONE', *, *, #36078, .F. ) ;
#53461=EDGE_CURVE ( 'NONE', #54111, #3901, #16170, .T. ) ;
#53468=ORIENTED_EDGE ( 'NONE', *, *, #34273, .F. ) ;
#53486=LINE ( 'NONE', #36285, #40369 ) ;
#53487=FACE_OUTER_BOUND ( 'NONE', #15193, .T. ) ;
#53510=CIRCLE ( 'NONE', #93085, 5.000000000000011546 ) ;
#53547=CARTESIAN_POINT ( 'NONE',  ( 104.9555555555555486, -4.171999999999998820, 0.000000000000000000 ) ) ;
#53553=DIRECTION ( 'NONE',  ( 0.000000000000000000, -1.000000000000000000, 0.000000000000000000 ) ) ;
#53566=ORIENTED_EDGE ( 'NONE', *, *, #77098, .F. ) ;
#53612=CIRCLE ( 'NONE', #60563, 5.000000000000011546 ) ;
#53632=CARTESIAN_POINT ( 'NONE',  ( 0.000000000000000000, 0.000000000000000000, 0.000000000000000000 ) ) ;
#53640=AXIS2_PLACEMENT_3D ( 'NONE', #91067, #65175, #41956 ) ;
#53653=DIRECTION ( 'NONE',  ( -1.000000000000000000, -1.224606353822377258E-16, -0.000000000000000000 ) ) ;
#53659=FACE_OUTER_BOUND ( 'NONE', #5045, .T. ) ;
#53716=DIRECTION ( 'NONE',  ( -0.5735764363510459374, -0.8191520442889919096, 0.000000000000000000 ) ) ;
#53718=CARTESIAN_POINT ( 'NONE',  ( 100.6222222222222200, -4.171999999999998820, 0.000000000000000000 ) ) ;
#53771=DIRECTION ( 'NONE',  ( -1.000000000000000000, -0.000000000000000000, -0.000000000000000000 ) ) ;
#53778=ORIENTED_EDGE ( 'NONE', *, *, #29706, .T. ) ;
#53782=CIRCLE ( 'NONE', #46927, 5.000000000000011546 ) ;
#53796=ORIENTED_EDGE ( 'NONE', *, *, #16300, .T. ) ;
#53799=ORIENTED_EDGE ( 'NONE', *, *, #80679, .T. ) ;
#53837=ADVANCED_FACE ( 'NONE', ( #60347 ), #22900, .T. ) ;
#53850=ADVANCED_FACE ( 'NONE', ( #3149 ), #64234, .T. ) ;
#53860=CARTESIAN_POINT ( 'NONE',  ( 99.75754961941544252, 1.030564683017419500E-14, 0.000000000000000000 ) ) ;
#53888=EDGE_CURVE ( 'NONE', #87052, #40910, #35015, .T. ) ;
#53899=ORIENTED_EDGE ( 'NONE', *, *, #101734, .F. ) ;
#53948=DIRECTION ( 'NONE',  ( 0.000000000000000000, -1.000000000000000000, 0.000000000000000000 ) ) ;
#53960=AXIS2_PLACEMENT_3D ( 'NONE', #70287, #71333, #104225 ) ;
#53969=DIRECTION ( 'NONE',  ( 0.000000000000000000, -1.000000000000000000, 0.000000000000000000 ) ) ;
#53995=ORIENTED_EDGE ( 'NONE', *, *, #58689, .F. ) ;
#54004=DIRECTION ( 'NONE',  ( -1.000000000000000000, -0.000000000000000000, -0.000000000000000000 ) ) ;
#54088=VERTEX_POINT ( 'NONE', #45220 ) ;
#54111=VERTEX_POINT ( 'NONE', #41349 ) ;
#54145=CARTESIAN_POINT ( 'NONE',  ( 104.9555555555555486, 4.172000000000019249, 5.109226446042768454E-16 ) ) ;
#54216=EDGE_CURVE ( 'NONE', #22959, #9861, #24740, .T. ) ;
#54258=CARTESIAN_POINT ( 'NONE',  ( 87.04245038058458306, 5.000000000000023093, 6.123233995736781074E-16 ) ) ;
#54307=DIRECTION ( 'NONE',  ( -1.000000000000000000, -1.224606353822377258E-16, -0.000000000000000000 ) ) ;
#54336=EDGE_CURVE ( 'NONE', #6761, #36922, #52267, .T. ) ;
#54338=ORIENTED_EDGE ( 'NONE', *, *, #90893, .T. ) ;
#54358=ADVANCED_FACE ( 'NONE', ( #17091 ), #48800, .T. ) ;
#54363=DIRECTION ( 'NONE',  ( 0.000000000000000000, -1.000000000000000000, 0.000000000000000000 ) ) ;
#54377=VERTEX_POINT ( 'NONE', #38465 ) ;
#54405=EDGE_CURVE ( 'NONE', #64598, #99558, #14314, .T. ) ;
#54406=FACE_OUTER_BOUND ( 'NONE', #68603, .T. ) ;
#54417=VERTEX_POINT ( 'NONE', #46014 ) ;
#54469=CARTESIAN_POINT ( 'NONE',  ( 104.3757837139179117, -2.002967142162725287E-29, 5.000000000000011546 ) ) ;
#54510=ORIENTED_EDGE ( 'NONE', *, *, #106717, .T. ) ;
#54522=DIRECTION ( 'NONE',  ( 0.000000000000000000, 1.224646799147353207E-16, 1.000000000000000000 ) ) ;
#54537=ORIENTED_EDGE ( 'NONE', *, *, #73138, .T. ) ;
#54541=VERTEX_POINT ( 'NONE', #4294 ) ;
#54551=DIRECTION ( 'NONE',  ( -1.000000000000000000, -1.224606353822377258E-16, -0.000000000000000000 ) ) ;
#54553=DIRECTION ( 'NONE',  ( 0.5735764363510554853, 0.8191520442889852482, 0.000000000000000000 ) ) ;
#54613=DIRECTION ( 'NONE',  ( 0.000000000000000000, 0.000000000000000000, 1.000000000000000000 ) ) ;
#54614=CARTESIAN_POINT ( 'NONE',  ( 106.4000000000000057, 0.000000000000000000, 4.171999999999999709 ) ) ;
#54627=CONICAL_SURFACE ( 'NONE', #75264, 4.172000000000009479, 0.9599310885968813656 ) ;
#54631=EDGE_CURVE ( 'NONE', #80260, #3027, #10637, .T. ) ;
#54683=PLANE ( 'NONE',  #79384 ) ;
#54763=DIRECTION ( 'NONE',  ( -1.000000000000000000, -1.224606353822377258E-16, -0.000000000000000000 ) ) ;
#54810=CARTESIAN_POINT ( 'NONE',  ( 92.53532739719321398, 1.030564683017419500E-14, 0.000000000000000000 ) ) ;
#54830=CARTESIAN_POINT ( 'NONE',  ( 98.31310517497099966, 1.030564683017419500E-14, 0.000000000000000000 ) ) ;
#54899=EDGE_CURVE ( 'NONE', #97033, #90932, #72970, .T. ) ;
#54920=VECTOR ( 'NONE', #84356, 999.9999999999998863 ) ;
#54934=CIRCLE ( 'NONE', #84285, 5.000000000000011546 ) ;
#54945=DIRECTION ( 'NONE',  ( 0.000000000000000000, -1.000000000000000000, 0.000000000000000000 ) ) ;
#54959=VERTEX_POINT ( 'NONE', #64401 ) ;
#55002=CARTESIAN_POINT ( 'NONE',  ( 82.70911704725124025, 1.016364837396684119E-14, 0.000000000000000000 ) ) ;
#55004=EDGE_LOOP ( 'NONE', ( #93244, #27916, #47398, #71225, #103107 ) ) ;
#55043=EDGE_CURVE ( 'NONE', #42532, #32237, #9223, .T. ) ;
#55166=FACE_OUTER_BOUND ( 'NONE', #5844, .T. ) ;
#55179=VERTEX_POINT ( 'NONE', #80422 ) ;
#55214=VERTEX_POINT ( 'NONE', #535 ) ;
#55219=AXIS2_PLACEMENT_3D ( 'NONE', #101368, #91170, #35064 ) ;
#55237=CONICAL_SURFACE ( 'NONE', #8750, 5.000000000000010658, 0.9599310885968697082 ) ;
#55261=LINE ( 'NONE', #38584, #99598 ) ;
#55275=DIRECTION ( 'NONE',  ( -1.000000000000000000, -1.224606353822377258E-16, -0.000000000000000000 ) ) ;
#55335=AXIS2_PLACEMENT_3D ( 'NONE', #5172, #103850, #29998 ) ;
#55374=EDGE_LOOP ( 'NONE', ( #61908, #3284, #13174, #103102, #49463, #101876 ) ) ;
#55405=CARTESIAN_POINT ( 'NONE',  ( 4.802676810931882923E-16, -0.7818963811860507596, -8.000000000000000000 ) ) ;
#55416=EDGE_CURVE ( 'NONE', #102006, #82194, #11067, .T. ) ;
#55420=ORIENTED_EDGE ( 'NONE', *, *, #23480, .F. ) ;
#55434=VERTEX_POINT ( 'NONE', #101411 ) ;
#55503=AXIS2_PLACEMENT_3D ( 'NONE', #18981, #60493, #61013 ) ;
#55525=FACE_OUTER_BOUND ( 'NONE', #4499, .T. ) ;
#55533=DIRECTION ( 'NONE',  ( 0.000000000000000000, 1.000000000000000000, 0.000000000000000000 ) ) ;
#55535=EDGE_CURVE ( 'NONE', #87544, #73615, #73041, .T. ) ;
#55557=EDGE_LOOP ( 'NONE', ( #52799, #80345, #101816, #4313, #39656, #29148 ) ) ;
#55572=AXIS2_PLACEMENT_3D ( 'NONE', #25819, #26871, #41409 ) ;
#55590=ORIENTED_EDGE ( 'NONE', *, *, #71793, .T. ) ;
#55610=EDGE_CURVE ( 'NONE', #41052, #55434, #30067, .T. ) ;
#55657=VERTEX_POINT ( 'NONE', #3244 ) ;
#55704=ORIENTED_EDGE ( 'NONE', *, *, #95708, .F. ) ;
#55730=EDGE_LOOP ( 'NONE', ( #40543, #71787, #59399, #102785, #60824 ) ) ;
#55735=CARTESIAN_POINT ( 'NONE',  ( 85.59800593614014019, 1.016364837396684119E-14, 0.000000000000000000 ) ) ;
#55739=LINE ( 'NONE', #80559, #82061 ) ;
#55743=ORIENTED_EDGE ( 'NONE', *, *, #106717, .F. ) ;
#55797=DIRECTION ( 'NONE',  ( 0.000000000000000000, -1.000000000000000000, 0.000000000000000000 ) ) ;
#55805=ORIENTED_EDGE ( 'NONE', *, *, #2102, .F. ) ;
#55848=CARTESIAN_POINT ( 'NONE',  ( 0.000000000000000000, 0.000000000000000000, 5.000000000000000888 ) ) ;
#55920=CARTESIAN_POINT ( 'NONE',  ( 106.4000000000000057, 5.616230220889761452E-16, -4.171999999999999709 ) ) ;
#55926=ORIENTED_EDGE ( 'NONE', *, *, #53296, .T. ) ;
#55934=CARTESIAN_POINT ( 'NONE',  ( 86.17777777777776294, 4.172000000000019249, 0.000000000000000000 ) ) ;
#56033=FACE_OUTER_BOUND ( 'NONE', #88903, .T. ) ;
#56049=DIRECTION ( 'NONE',  ( 0.000000000000000000, -1.000000000000000000, 0.000000000000000000 ) ) ;
#56060=ORIENTED_EDGE ( 'NONE', *, *, #58191, .F. ) ;
#56089=DIRECTION ( 'NONE',  ( 0.000000000000000000, -1.000000000000000000, 0.000000000000000000 ) ) ;
#56090=CIRCLE ( 'NONE', #81892, 5.000000000000011546 ) ;
#56101=CARTESIAN_POINT ( 'NONE',  ( 102.6464385083043283, 1.030564683017419500E-14, 0.000000000000000000 ) ) ;
#56135=AXIS2_PLACEMENT_3D ( 'NONE', #19359, #29045, #3660 ) ;
#56136=ORIENTED_EDGE ( 'NONE', *, *, #104685, .T. ) ;
#56155=VECTOR ( 'NONE', #60772, 1000.000000000000000 ) ;
#56187=ADVANCED_FACE ( 'NONE', ( #73403 ), #97686, .T. ) ;
#56193=DIRECTION ( 'NONE',  ( -1.000000000000000000, -1.224606353822377258E-16, -0.000000000000000000 ) ) ;
#56310=ORIENTED_EDGE ( 'NONE', *, *, #25714, .T. ) ;
#56382=ORIENTED_EDGE ( 'NONE', *, *, #104401, .F. ) ;
#56383=CARTESIAN_POINT ( 'NONE',  ( 91.37578371391791165, 1.016364837396684119E-14, 0.000000000000000000 ) ) ;
#56412=DIRECTION ( 'NONE',  ( 0.5735764363510557073, -0.8191520442889850262, 1.003171929053516612E-16 ) ) ;
#56421=CIRCLE ( 'NONE', #66848, 5.000000000000011546 ) ;
#56438=ORIENTED_EDGE ( 'NONE', *, *, #76804, .F. ) ;
#56445=DIRECTION ( 'NONE',  ( -1.000000000000000000, 0.000000000000000000, -0.000000000000000000 ) ) ;
#56469=FACE_OUTER_BOUND ( 'NONE', #60110, .T. ) ;
#56541=B_SPLINE_CURVE_WITH_KNOTS ( 'NONE', 3,
 ( #22124, #39364, #87907, #14512, #47423, #46895 ),
 .UNSPECIFIED., .F., .F.,
 ( 4, 2, 4 ),
 ( 0.008690415911505277452, 0.01102883712493079801, 0.01336725833835631684 ),
 .UNSPECIFIED. ) ;
#56597=DIRECTION ( 'NONE',  ( -1.000000000000000000, -1.224606353822377258E-16, -0.000000000000000000 ) ) ;
#56665=CARTESIAN_POINT ( 'NONE',  ( 82.70911704725124025, 5.000000000000023093, 6.123233995736781074E-16 ) ) ;
#56736=ORIENTED_EDGE ( 'NONE', *, *, #82743, .F. ) ;
#56756=CARTESIAN_POINT ( 'NONE',  ( 102.0666666666666629, 4.172000000000019249, 5.109226446042768454E-16 ) ) ;
#56759=DIRECTION ( 'NONE',  ( -1.000000000000000000, -1.224606353822377258E-16, -0.000000000000000000 ) ) ;
#56770=DIRECTION ( 'NONE',  ( -1.000000000000000000, -0.000000000000000000, -0.000000000000000000 ) ) ;
#56897=AXIS2_PLACEMENT_3D ( 'NONE', #82770, #27238, #101620 ) ;
#56899=ADVANCED_FACE ( 'NONE', ( #71048 ), #19987, .T. ) ;
#56901=AXIS2_PLACEMENT_3D ( 'NONE', #9919, #34773, #20199 ) ;
#56905=ORIENTED_EDGE ( 'NONE', *, *, #47791, .F. ) ;
#56961=DIRECTION ( 'NONE',  ( -1.000000000000000000, -1.224606353822377258E-16, -0.000000000000000000 ) ) ;
#57009=VECTOR ( 'NONE', #54553, 1000.000000000000000 ) ;
#57011=ORIENTED_EDGE ( 'NONE', *, *, #2264, .F. ) ;
#57033=DIRECTION ( 'NONE',  ( 0.000000000000000000, 0.000000000000000000, 1.000000000000000000 ) ) ;
#57161=DIRECTION ( 'NONE',  ( 0.000000000000000000, 0.000000000000000000, -1.000000000000000000 ) ) ;
#57179=CARTESIAN_POINT ( 'NONE',  ( 97.73333333333333428, -4.171999999999998820, 5.616230220889773285E-16 ) ) ;
#57223=CARTESIAN_POINT ( 'NONE',  ( 0.000000000000000000, 0.000000000000000000, 0.000000000000000000 ) ) ;
#57226=DIRECTION ( 'NONE',  ( -1.000000000000000000, -1.224606353822377258E-16, -0.000000000000000000 ) ) ;
#57247=DIRECTION ( 'NONE',  ( 0.000000000000000000, 0.000000000000000000, 1.000000000000000000 ) ) ;
#57304=CIRCLE ( 'NONE', #24624, 5.000000000000011546 ) ;
#57307=ADVANCED_FACE ( 'NONE', ( #70271 ), #47557, .T. ) ;
#57345=AXIS2_PLACEMENT_3D ( 'NONE', #88803, #70506, #95311 ) ;
#57375=CARTESIAN_POINT ( 'NONE',  ( 5.799999999999999822, 9.237604307034018802, 0.000000000000000000 ) ) ;
#57410=VERTEX_POINT ( 'NONE', #7106 ) ;
#57449=CARTESIAN_POINT ( 'NONE',  ( 95.42421628608209971, 6.123233995736568081E-16, -5.000000000000011546 ) ) ;
#57488=CARTESIAN_POINT ( 'NONE',  ( 0.1306530452038046075, -5.952467836904144605, 5.690023276062396107 ) ) ;
#57502=DIRECTION ( 'NONE',  ( 0.000000000000000000, 1.000000000000000000, 0.000000000000000000 ) ) ;
#57518=CARTESIAN_POINT ( 'NONE',  ( 79.82022815836235452, -5.000000000000000000, 0.000000000000000000 ) ) ;
#57522=DIRECTION ( 'NONE',  ( 0.000000000000000000, -1.000000000000000000, 0.000000000000000000 ) ) ;
#57574=DIRECTION ( 'NONE',  ( -1.000000000000000000, -1.224606353822377258E-16, -0.000000000000000000 ) ) ;
#57657=VERTEX_POINT ( 'NONE', #73236 ) ;
#57699=DIRECTION ( 'NONE',  ( 0.000000000000000000, -1.000000000000000000, 0.000000000000000000 ) ) ;
#57747=DIRECTION ( 'NONE',  ( -1.000000000000000000, -1.224606353822377258E-16, -0.000000000000000000 ) ) ;
#57757=CARTESIAN_POINT ( 'NONE',  ( 0.000000000000000000, 6.928203230275505220, -4.000000000000007105 ) ) ;
#57772=ORIENTED_EDGE ( 'NONE', *, *, #37238, .F. ) ;
#57785=AXIS2_PLACEMENT_3D ( 'NONE', #52667, #2517, #44602 ) ;
#57868=DIRECTION ( 'NONE',  ( -1.000000000000000000, -0.000000000000000000, -0.000000000000000000 ) ) ;
#57911=AXIS2_PLACEMENT_3D ( 'NONE', #94565, #20715, #53553 ) ;
#57930=DIRECTION ( 'NONE',  ( -1.000000000000000000, -1.224606353822377258E-16, -0.000000000000000000 ) ) ;
#57940=CARTESIAN_POINT ( 'NONE',  ( 5.799999999999999822, 0.000000000000000000, 0.000000000000000000 ) ) ;
#57968=ORIENTED_EDGE ( 'NONE', *, *, #94074, .T. ) ;
#57984=CONICAL_SURFACE ( 'NONE', #51125, 5.000000000000010658, 0.9599310885968697082 ) ;
#58020=CARTESIAN_POINT ( 'NONE',  ( 0.000000000000000000, 6.123233995736767268E-16, -5.000000000000000888 ) ) ;
#58021=ADVANCED_FACE ( 'NONE', ( #33361 ), #81336, .F. ) ;
#58027=DIRECTION ( 'NONE',  ( 0.000000000000000000, -1.000000000000000000, 0.000000000000000000 ) ) ;
#58028=CARTESIAN_POINT ( 'NONE',  ( 0.000000000000000000, -6.928203230275504332, 4.000000000000007105 ) ) ;
#58039=VERTEX_POINT ( 'NONE', #74318 ) ;
#58083=CARTESIAN_POINT ( 'NONE',  ( 92.82022815836235452, 1.016364837396684119E-14, 0.000000000000000000 ) ) ;
#58121=CARTESIAN_POINT ( 'NONE',  ( 0.000000000000000000, 0.000000000000000000, 0.000000000000000000 ) ) ;
#58191=EDGE_CURVE ( 'NONE', #49541, #55657, #67315, .T. ) ;
#58251=ADVANCED_FACE ( 'NONE', ( #921 ), #92455, .T. ) ;
#58281=FACE_OUTER_BOUND ( 'NONE', #55557, .T. ) ;
#58282=AXIS2_PLACEMENT_3D ( 'NONE', #45874, #63666, #79821 ) ;
#58307=CARTESIAN_POINT ( 'NONE',  ( 95.70911704725124025, 1.016364837396684119E-14, 0.000000000000000000 ) ) ;
#58313=VERTEX_POINT ( 'NONE', #79108 ) ;
#58340=CARTESIAN_POINT ( 'NONE',  ( 87.62222222222222001, 1.023464760207051730E-14, 0.000000000000000000 ) ) ;
#58382=CARTESIAN_POINT ( 'NONE',  ( 5.799999999999999822, 4.618802153517005848, 7.999999999999996447 ) ) ;
#58385=DIRECTION ( 'NONE',  ( 0.000000000000000000, -1.000000000000000000, 0.000000000000000000 ) ) ;
#58407=CARTESIAN_POINT ( 'NONE',  ( 0.000000000000000000, 0.000000000000000000, 5.000000000000000888 ) ) ;
#58414=ORIENTED_EDGE ( 'NONE', *, *, #63092, .T. ) ;
#58424=FACE_OUTER_BOUND ( 'NONE', #9359, .T. ) ;
#58427=VECTOR ( 'NONE', #30522, 1000.000000000000000 ) ;
#58444=DIRECTION ( 'NONE',  ( 0.000000000000000000, 0.000000000000000000, 1.000000000000000000 ) ) ;
#58458=EDGE_LOOP ( 'NONE', ( #43131, #13454, #78078, #48781, #90354 ) ) ;
#58500=ORIENTED_EDGE ( 'NONE', *, *, #43685, .F. ) ;
#58538=DIRECTION ( 'NONE',  ( 0.000000000000000000, 0.000000000000000000, 1.000000000000000000 ) ) ;
#58540=SURFACE_SIDE_STYLE ('',( #91956 ) ) ;
#58626=CARTESIAN_POINT ( 'NONE',  ( 94.84444444444443434, 4.172000000000019249, 5.109226446042768454E-16 ) ) ;
#58633=AXIS2_PLACEMENT_3D ( 'NONE', #27134, #18493, #60023 ) ;
#58643=CIRCLE ( 'NONE', #34562, 4.172000000000009479 ) ;
#58645=DIRECTION ( 'NONE',  ( 0.000000000000000000, -1.000000000000000000, 0.000000000000000000 ) ) ;
#58664=ADVANCED_FACE ( 'NONE', ( #77927 ), #46093, .F. ) ;
#58670=ORIENTED_EDGE ( 'NONE', *, *, #49682, .F. ) ;
#58680=CARTESIAN_POINT ( 'NONE',  ( 91.95555555555554861, 1.023464760207051730E-14, 0.000000000000000000 ) ) ;
#58689=EDGE_CURVE ( 'NONE', #59238, #88742, #75356, .T. ) ;
#58718=EDGE_LOOP ( 'NONE', ( #79169, #90445, #40925, #80705, #34425 ) ) ;
#58726=CARTESIAN_POINT ( 'NONE',  ( 93.97977184163765685, 1.030564683017419500E-14, 0.000000000000000000 ) ) ;
#58754=DIRECTION ( 'NONE',  ( 0.000000000000000000, 1.000000000000000000, 0.000000000000000000 ) ) ;
#58818=CARTESIAN_POINT ( 'NONE',  ( 80.97977184163765685, 5.000000000000021316, 0.000000000000000000 ) ) ;
#58827=AXIS2_PLACEMENT_3D ( 'NONE', #57940, #6747, #66046 ) ;
#58923=CARTESIAN_POINT ( 'NONE',  ( 6.800000000000000711, 0.000000000000000000, 5.000000000000000888 ) ) ;
#58969=DIRECTION ( 'NONE',  ( 1.000000000000000000, 0.000000000000000000, -0.000000000000000000 ) ) ;
#58981=DIRECTION ( 'NONE',  ( 0.000000000000000000, 0.000000000000000000, 1.000000000000000000 ) ) ;
#59013=ORIENTED_EDGE ( 'NONE', *, *, #9459, .T. ) ;
#59033=CARTESIAN_POINT ( 'NONE',  ( 93.39999999999999147, 4.172000000000019249, 5.109226446042768454E-16 ) ) ;
#59048=ADVANCED_FACE ( 'NONE', ( #58424 ), #42722, .T. ) ;
#59070=DIRECTION ( 'NONE',  ( 0.000000000000000000, -1.000000000000000000, 0.000000000000000000 ) ) ;
#59077=CARTESIAN_POINT ( 'NONE',  ( 89.06666666666666288, 4.172000000000019249, 5.109226446042768454E-16 ) ) ;
#59097=VERTEX_POINT ( 'NONE', #71282 ) ;
#59128=DIRECTION ( 'NONE',  ( 0.5735764363510557073, -0.8191520442889850262, 1.003171929053516612E-16 ) ) ;
#59145=ORIENTED_EDGE ( 'NONE', *, *, #48835, .T. ) ;
#59146=DIRECTION ( 'NONE',  ( -1.000000000000000000, -0.000000000000000000, -0.000000000000000000 ) ) ;
#59160=CARTESIAN_POINT ( 'NONE',  ( 96.86866073052655679, 1.030564683017419500E-14, 0.000000000000000000 ) ) ;
#59193=LINE ( 'NONE', #41925, #2989 ) ;
#59238=VERTEX_POINT ( 'NONE', #35513 ) ;
#59261=CARTESIAN_POINT ( 'NONE',  ( 0.000000000000000000, 0.000000000000000000, 5.000000000000000888 ) ) ;
#59267=EDGE_CURVE ( 'NONE', #3901, #54377, #78820, .T. ) ;
#59280=DIRECTION ( 'NONE',  ( 0.000000000000000000, -1.000000000000000000, 0.000000000000000000 ) ) ;
#59368=DIRECTION ( 'NONE',  ( 0.000000000000000000, -1.000000000000000000, 0.000000000000000000 ) ) ;
#59399=ORIENTED_EDGE ( 'NONE', *, *, #18875, .T. ) ;
#59413=DIRECTION ( 'NONE',  ( -0.5735764363510461594, 0.8191520442889916875, 1.003171929053524870E-16 ) ) ;
#59437=CARTESIAN_POINT ( 'NONE',  ( 0.000000000000000000, 0.000000000000000000, 5.000000000000000888 ) ) ;
#59438=CARTESIAN_POINT ( 'NONE',  ( 88.20199406385988539, 1.030564683017419500E-14, 0.000000000000000000 ) ) ;
#59518=EDGE_CURVE ( 'NONE', #17909, #54959, #6360, .T. ) ;
#59564=DIRECTION ( 'NONE',  ( 0.5735764363510554853, 0.8191520442889852482, 0.000000000000000000 ) ) ;
#59601=DIRECTION ( 'NONE',  ( -1.000000000000000000, -1.224606353822377258E-16, -0.000000000000000000 ) ) ;
#59609=SURFACE_STYLE_USAGE ( .BOTH. , #58540 ) ;
#59635=CIRCLE ( 'NONE', #57911, 4.172000000000009479 ) ;
#59651=LINE ( 'NONE', #75273, #41268 ) ;
#59700=EDGE_LOOP ( 'NONE', ( #56438, #56382, #105982, #33689, #88807 ) ) ;
#59716=EDGE_CURVE ( 'NONE', #57410, #27178, #92685, .T. ) ;
#59733=DIRECTION ( 'NONE',  ( 0.000000000000000000, -1.000000000000000000, 0.000000000000000000 ) ) ;
#59755=CARTESIAN_POINT ( 'NONE',  ( 105.5353273971932140, -5.000000000000000888, 6.123233995736779101E-16 ) ) ;
#59758=AXIS2_PLACEMENT_3D ( 'NONE', #96926, #56445, #47822 ) ;
#59771=ORIENTED_EDGE ( 'NONE', *, *, #96152, .F. ) ;
#59778=ORIENTED_EDGE ( 'NONE', *, *, #40426, .T. ) ;
#59842=CIRCLE ( 'NONE', #13294, 4.172000000000009479 ) ;
#59887=CARTESIAN_POINT ( 'NONE',  ( 88.20199406385988539, 1.030564683017419500E-14, 0.000000000000000000 ) ) ;
#59923=VERTEX_POINT ( 'NONE', #70248 ) ;
#59929=VECTOR ( 'NONE', #105755, 1000.000000000000000 ) ;
#59938=ADVANCED_FACE ( 'NONE', ( #93472 ), #54627, .T. ) ;
#59987=LINE ( 'NONE', #69648, #68047 ) ;
#60000=CONICAL_SURFACE ( 'NONE', #46193, 5.000000000000010658, 0.9599310885968697082 ) ;
#60007=DIRECTION ( 'NONE',  ( -1.000000000000000000, -1.224606353822377258E-16, -0.000000000000000000 ) ) ;
#60023=DIRECTION ( 'NONE',  ( 0.000000000000000000, 0.000000000000000000, 1.000000000000000000 ) ) ;
#60034=CARTESIAN_POINT ( 'NONE',  ( 96.86866073052655679, -2.002967142162725287E-29, 5.000000000000011546 ) ) ;
#60086=CYLINDRICAL_SURFACE ( 'NONE', #24068, 8.000000000000000000 ) ;
#60110=EDGE_LOOP ( 'NONE', ( #3734, #12070, #102450, #26292, #8995 ) ) ;
#60122=CARTESIAN_POINT ( 'NONE',  ( 0.000000000000000000, -6.928203230275504332, 4.000000000000007105 ) ) ;
#60178=CARTESIAN_POINT ( 'NONE',  ( 100.6222222222222200, 4.172000000000019249, 5.109226446042768454E-16 ) ) ;
#60186=CARTESIAN_POINT ( 'NONE',  ( 0.000000000000000000, 0.000000000000000000, 0.000000000000000000 ) ) ;
#60195=CARTESIAN_POINT ( 'NONE',  ( 104.9555555555555486, -4.171999999999998820, 5.616230220889773285E-16 ) ) ;
#60201=ORIENTED_EDGE ( 'NONE', *, *, #22891, .T. ) ;
#60202=CARTESIAN_POINT ( 'NONE',  ( 88.48689482502902592, 1.016364837396684119E-14, 0.000000000000000000 ) ) ;
#60224=STYLED_ITEM ( 'NONE', ( #27273 ), #90947 ) ;
#60251=VECTOR ( 'NONE', #74169, 1000.000000000000000 ) ;
#60279=DIRECTION ( 'NONE',  ( 1.000000000000000000, 0.000000000000000000, 0.000000000000000000 ) ) ;
#60316=CONICAL_SURFACE ( 'NONE', #86123, 5.000000000000010658, 0.9599310885968697082 ) ;
#60327=AXIS2_PLACEMENT_3D ( 'NONE', #91471, #97951, #17587 ) ;
#60340=CARTESIAN_POINT ( 'NONE',  ( 88.48689482502902592, 1.016364837396684119E-14, 0.000000000000000000 ) ) ;
#60347=FACE_OUTER_BOUND ( 'NONE', #51350, .T. ) ;
#60351=CIRCLE ( 'NONE', #53403, 5.000000000000010658 ) ;
#60357=CARTESIAN_POINT ( 'NONE',  ( 81.84444444444444855, 1.023464760207051730E-14, 0.000000000000000000 ) ) ;
#60364=ORIENTED_EDGE ( 'NONE', *, *, #48044, .T. ) ;
#60388=CIRCLE ( 'NONE', #20853, 5.000000000000010658 ) ;
#60404=ORIENTED_EDGE ( 'NONE', *, *, #65619, .T. ) ;
#60462=VERTEX_POINT ( 'NONE', #86333 ) ;
#60493=DIRECTION ( 'NONE',  ( -1.000000000000000000, -0.000000000000000000, -0.000000000000000000 ) ) ;
#60522=DIRECTION ( 'NONE',  ( -1.000000000000000000, -1.224606353822377258E-16, -0.000000000000000000 ) ) ;
#60563=AXIS2_PLACEMENT_3D ( 'NONE', #97429, #47814, #31158 ) ;
#60572=CARTESIAN_POINT ( 'NONE',  ( 5.799999999999999822, 8.000000000000000000, 0.000000000000000000 ) ) ;
#60573=DIRECTION ( 'NONE',  ( 0.000000000000000000, 0.000000000000000000, -1.000000000000000000 ) ) ;
#60584=DIRECTION ( 'NONE',  ( 0.000000000000000000, -1.000000000000000000, 0.000000000000000000 ) ) ;
#60613=CARTESIAN_POINT ( 'NONE',  ( 105.5720000000000312, 0.000000000000000000, 5.000000000000000888 ) ) ;
#60617=EDGE_CURVE ( 'NONE', #1310, #71316, #40937, .T. ) ;
#60646=ORIENTED_EDGE ( 'NONE', *, *, #82398, .F. ) ;
#60769=ORIENTED_EDGE ( 'NONE', *, *, #3202, .T. ) ;
#60772=DIRECTION ( 'NONE',  ( -0.5735764363510459374, -0.8191520442889919096, 0.000000000000000000 ) ) ;
#60801=CARTESIAN_POINT ( 'NONE',  ( 94.84444444444443434, 1.023464760207051730E-14, 0.000000000000000000 ) ) ;
#60812=EDGE_CURVE ( 'NONE', #10153, #59923, #1516, .T. ) ;
#60824=ORIENTED_EDGE ( 'NONE', *, *, #47901, .F. ) ;
#60837=PLANE ( 'NONE',  #51164 ) ;
#60865=EDGE_CURVE ( 'NONE', #92963, #58313, #51325, .T. ) ;
#60894=DIRECTION ( 'NONE',  ( 0.000000000000000000, 0.000000000000000000, -1.000000000000000000 ) ) ;
#60920=CARTESIAN_POINT ( 'NONE',  ( 98.31310517497099966, -5.000000000000000888, 6.123233995736779101E-16 ) ) ;
#60932=AXIS2_PLACEMENT_3D ( 'NONE', #28629, #61513, #3792 ) ;
#60942=DIRECTION ( 'NONE',  ( 0.000000000000000000, -1.000000000000000000, 0.000000000000000000 ) ) ;
#60958=CIRCLE ( 'NONE', #28266, 5.000000000000010658 ) ;
#61013=DIRECTION ( 'NONE',  ( 0.000000000000000000, 0.000000000000000000, 1.000000000000000000 ) ) ;
#61018=DIRECTION ( 'NONE',  ( -1.000000000000000000, -1.224606353822377258E-16, -0.000000000000000000 ) ) ;
#61031=LINE ( 'NONE', #59437, #63789 ) ;
#61076=CIRCLE ( 'NONE', #47263, 5.000000000000011546 ) ;
#61124=DIRECTION ( 'NONE',  ( 0.000000000000000000, 0.000000000000000000, 1.000000000000000000 ) ) ;
#61157=AXIS2_PLACEMENT_3D ( 'NONE', #90569, #25334, #99175 ) ;
#61162=EDGE_LOOP ( 'NONE', ( #90203, #4798, #43994, #90962, #49450 ) ) ;
#61209=EDGE_CURVE ( 'NONE', #28024, #41772, #90832, .T. ) ;
#61219=DIRECTION ( 'NONE',  ( 0.000000000000000000, -1.000000000000000000, 0.000000000000000000 ) ) ;
#61223=FACE_OUTER_BOUND ( 'NONE', #97200, .T. ) ;
#61264=CARTESIAN_POINT ( 'NONE',  ( 91.09088295274877112, -2.002967142162725287E-29, 5.000000000000011546 ) ) ;
#61320=VECTOR ( 'NONE', #23396, 1000.000000000000114 ) ;
#61354=ADVANCED_FACE ( 'NONE', ( #37939 ), #44406, .T. ) ;
#61383=VECTOR ( 'NONE', #67965, 1000.000000000000000 ) ;
#61407=AXIS2_PLACEMENT_3D ( 'NONE', #71535, #95307, #70502 ) ;
#61474=CARTESIAN_POINT ( 'NONE',  ( 89.06666666666666288, -4.171999999999998820, 5.616230220889773285E-16 ) ) ;
#61496=CYLINDRICAL_SURFACE ( 'NONE', #73888, 5.000000000000000888 ) ;
#61513=DIRECTION ( 'NONE',  ( -1.000000000000000000, -1.224606353822377258E-16, -0.000000000000000000 ) ) ;
#61559=AXIS2_PLACEMENT_3D ( 'NONE', #80494, #72930, #100277 ) ;
#61599=DIRECTION ( 'NONE',  ( 0.000000000000000000, 0.000000000000000000, 1.000000000000000000 ) ) ;
#61626=CARTESIAN_POINT ( 'NONE',  ( 94.84444444444443434, -4.171999999999998820, 0.000000000000000000 ) ) ;
#61639=DIRECTION ( 'NONE',  ( 0.000000000000000000, 0.000000000000000000, -1.000000000000000000 ) ) ;
#61721=DIRECTION ( 'NONE',  ( -1.000000000000000000, -0.000000000000000000, -0.000000000000000000 ) ) ;
#61760=VECTOR ( 'NONE', #48746, 1000.000000000000000 ) ;
#61783=CARTESIAN_POINT ( 'NONE',  ( 97.15356149169568312, 1.016364837396684119E-14, 0.000000000000000000 ) ) ;
#61829=AXIS2_PLACEMENT_3D ( 'NONE', #104297, #63871, #5612 ) ;
#61839=LINE ( 'NONE', #37581, #3851 ) ;
#61856=ORIENTED_EDGE ( 'NONE', *, *, #53240, .T. ) ;
#61888=CIRCLE ( 'NONE', #70491, 5.000000000000011546 ) ;
#61908=ORIENTED_EDGE ( 'NONE', *, *, #11015, .F. ) ;
#61976=CARTESIAN_POINT ( 'NONE',  ( 0.7145311798163208605, 4.618802153517005848, 7.999999999999996447 ) ) ;
#62029=ADVANCED_FACE ( 'NONE', ( #64842 ), #23178, .T. ) ;
#62036=ADVANCED_FACE ( 'NONE', ( #66979 ), #50757, .T. ) ;
#62038=AXIS2_PLACEMENT_3D ( 'NONE', #79039, #55275, #48244 ) ;
#62047=CARTESIAN_POINT ( 'NONE',  ( 6.400000000000000355, -4.618802153517009401, -8.000000000000001776 ) ) ;
#62086=DIRECTION ( 'NONE',  ( -1.000000000000000000, -1.224606353822377258E-16, -0.000000000000000000 ) ) ;
#62095=ADVANCED_FACE ( 'NONE', ( #41630 ), #73445, .T. ) ;
#62112=ORIENTED_EDGE ( 'NONE', *, *, #34757, .T. ) ;
#62113=CARTESIAN_POINT ( 'NONE',  ( 85.59800593614014019, 5.000000000000002665, 6.123233995736756422E-16 ) ) ;
#62136=DIRECTION ( 'NONE',  ( 0.000000000000000000, 0.000000000000000000, -1.000000000000000000 ) ) ;
#62169=CARTESIAN_POINT ( 'NONE',  ( 5.799999999999999822, 9.237604307034018802, 0.000000000000000000 ) ) ;
#62243=ORIENTED_EDGE ( 'NONE', *, *, #8535, .T. ) ;
#62320=VERTEX_POINT ( 'NONE', #96031 ) ;
#62321=FACE_OUTER_BOUND ( 'NONE', #104505, .T. ) ;
#62338=EDGE_LOOP ( 'NONE', ( #44606, #89890, #75586, #47524, #75272, #64555 ) ) ;
#62340=ADVANCED_FACE ( 'NONE', ( #14545 ), #22157, .T. ) ;
#62348=DIRECTION ( 'NONE',  ( 0.000000000000000000, -1.000000000000000000, 0.000000000000000000 ) ) ;
#62358=ADVANCED_FACE ( 'NONE', ( #96562 ), #42173, .T. ) ;
#62374=ORIENTED_EDGE ( 'NONE', *, *, #46957, .F. ) ;
#62376=LINE ( 'NONE', #85588, #15978 ) ;
#62435=CARTESIAN_POINT ( 'NONE',  ( 84.15356149169568312, 1.016364837396684119E-14, 0.000000000000000000 ) ) ;
#62483=ORIENTED_EDGE ( 'NONE', *, *, #48194, .T. ) ;
#62514=ORIENTED_EDGE ( 'NONE', *, *, #31386, .T. ) ;
#62556=DIRECTION ( 'NONE',  ( 1.000000000000000000, 1.224606353822377258E-16, 0.000000000000000000 ) ) ;
#62577=DIRECTION ( 'NONE',  ( -0.5735764363510461594, 0.8191520442889916875, 1.003171929053524870E-16 ) ) ;
#62578=DIRECTION ( 'NONE',  ( 1.000000000000000000, 0.000000000000000000, -0.000000000000000000 ) ) ;
#62600=DIRECTION ( 'NONE',  ( -1.000000000000000000, -1.224606353822377258E-16, -0.000000000000000000 ) ) ;
#62609=EDGE_LOOP ( 'NONE', ( #91418, #23172, #91896, #82074, #31362, #45777 ) ) ;
#62620=VECTOR ( 'NONE', #24998, 1000.000000000000114 ) ;
#62661=SHAPE_REPRESENTATION ( 'hex bolt gradeab_iso_ISO 4014 - M10 x 100 x 26-S', ( #10728 ), #79871 ) ;
#62685=CARTESIAN_POINT ( 'NONE',  ( 0.1306530452038090484, -7.903938623646867612, -2.309976723937607446 ) ) ;
#62793=AXIS2_PLACEMENT_3D ( 'NONE', #91575, #50029, #82935 ) ;
#62795=ORIENTED_EDGE ( 'NONE', *, *, #64694, .F. ) ;
#62850=AXIS2_PLACEMENT_3D ( 'NONE', #26550, #28141, #44290 ) ;
#62855=CARTESIAN_POINT ( 'NONE',  ( 79.82022815836235452, 5.000000000000023093, 6.123233995736781074E-16 ) ) ;
#62876=ORIENTED_EDGE ( 'NONE', *, *, #68521, .T. ) ;
#62880=LINE ( 'NONE', #88211, #22159 ) ;
#62889=CARTESIAN_POINT ( 'NONE',  ( 94.26467260280679739, -5.000000000000000000, 0.000000000000000000 ) ) ;
#62912=DIRECTION ( 'NONE',  ( 0.000000000000000000, 0.000000000000000000, -1.000000000000000000 ) ) ;
#62934=DIRECTION ( 'NONE',  ( 0.000000000000000000, 1.000000000000000000, 0.000000000000000000 ) ) ;
#62993=EDGE_LOOP ( 'NONE', ( #50096, #69655, #36073, #78248, #41888 ) ) ;
#62998=LINE ( 'NONE', #14409, #9448 ) ;
#63058=DIRECTION ( 'NONE',  ( 0.000000000000000000, -1.000000000000000000, 0.000000000000000000 ) ) ;
#63062=AXIS2_PLACEMENT_3D ( 'NONE', #99401, #25585, #58444 ) ;
#63074=ORIENTED_EDGE ( 'NONE', *, *, #4634, .F. ) ;
#63092=EDGE_CURVE ( 'NONE', #39124, #33725, #45379, .T. ) ;
#63124=CIRCLE ( 'NONE', #71498, 4.172000000000009479 ) ;
#63132=DIRECTION ( 'NONE',  ( 0.000000000000000000, 0.000000000000000000, 1.000000000000000000 ) ) ;
#63165=EDGE_CURVE ( 'NONE', #53206, #3401, #59987, .T. ) ;
#63169=VERTEX_POINT ( 'NONE', #44853 ) ;
#63203=DIRECTION ( 'NONE',  ( -0.5735764363510461594, 0.8191520442889916875, 1.003171929053524870E-16 ) ) ;
#63222=VECTOR ( 'NONE', #23581, 1000.000000000000000 ) ;
#63247=EDGE_LOOP ( 'NONE', ( #63267, #40916, #105941, #82106, #41817 ) ) ;
#63254=DIRECTION ( 'NONE',  ( 0.5735764363510557073, -0.8191520442889850262, 1.003171929053516612E-16 ) ) ;
#63264=DIRECTION ( 'NONE',  ( 0.000000000000000000, -1.000000000000000000, 0.000000000000000000 ) ) ;
#63267=ORIENTED_EDGE ( 'NONE', *, *, #80172, .T. ) ;
#63268=DIRECTION ( 'NONE',  ( 0.000000000000000000, -1.000000000000000000, 0.000000000000000000 ) ) ;
#63286=VERTEX_POINT ( 'NONE', #79844 ) ;
#63309=AXIS2_PLACEMENT_3D ( 'NONE', #88095, #63824, #4512 ) ;
#63319=CARTESIAN_POINT ( 'NONE',  ( 0.000000000000000000, 0.000000000000000000, 5.000000000000000888 ) ) ;
#63412=DIRECTION ( 'NONE',  ( 0.000000000000000000, -1.000000000000000000, 0.000000000000000000 ) ) ;
#63441=CARTESIAN_POINT ( 'NONE',  ( 96.28888888888889142, 4.172000000000019249, 0.000000000000000000 ) ) ;
#63469=VECTOR ( 'NONE', #47534, 1000.000000000000114 ) ;
#63481=ORIENTED_EDGE ( 'NONE', *, *, #98176, .T. ) ;
#63526=CIRCLE ( 'NONE', #32583, 5.000000000000010658 ) ;
#63541=CIRCLE ( 'NONE', #27395, 5.000000000000010658 ) ;
#63573=AXIS2_PLACEMENT_3D ( 'NONE', #100425, #60007, #9810 ) ;
#63580=DIRECTION ( 'NONE',  ( 1.000000000000000000, 0.000000000000000000, 0.000000000000000000 ) ) ;
#63650=ORIENTED_EDGE ( 'NONE', *, *, #54216, .T. ) ;
#63666=DIRECTION ( 'NONE',  ( -1.000000000000000000, -0.000000000000000000, -0.000000000000000000 ) ) ;
#63673=( GEOMETRIC_REPRESENTATION_CONTEXT ( 3 ) GLOBAL_UNCERTAINTY_ASSIGNED_CONTEXT ( ( #90573 ) ) GLOBAL_UNIT_ASSIGNED_CONTEXT ( ( #100043, #91442, #26735 ) ) REPRESENTATION_CONTEXT ( 'NONE', 'WORKASPACE' ) );
#63754=VERTEX_POINT ( 'NONE', #10086 ) ;
#63755=ADVANCED_FACE ( 'NONE', ( #100683 ), #44035, .T. ) ;
#63789=VECTOR ( 'NONE', #101997, 1000.000000000000000 ) ;
#63817=EDGE_LOOP ( 'NONE', ( #102295, #62876, #11667, #71314, #95373, #56736 ) ) ;
#63824=DIRECTION ( 'NONE',  ( -1.000000000000000000, -0.000000000000000000, -0.000000000000000000 ) ) ;
#63839=CARTESIAN_POINT ( 'NONE',  ( 0.06809871960542410174, -7.710219529346603373, 2.645508037661880252 ) ) ;
#63868=CIRCLE ( 'NONE', #17365, 5.000000000000010658 ) ;
#63871=DIRECTION ( 'NONE',  ( -1.000000000000000000, -1.224606353822377258E-16, -0.000000000000000000 ) ) ;
#63874=CARTESIAN_POINT ( 'NONE',  ( 0.4988340113754576310, 3.871605243940358765, -8.000000000000001776 ) ) ;
#63896=AXIS2_PLACEMENT_3D ( 'NONE', #90963, #17071, #82856 ) ;
#63942=EDGE_LOOP ( 'NONE', ( #104325, #8168, #70189, #27103, #80063 ) ) ;
#63978=AXIS2_PLACEMENT_3D ( 'NONE', #106033, #91479, #97960 ) ;
#63995=DIRECTION ( 'NONE',  ( 0.000000000000000000, -1.000000000000000000, 0.000000000000000000 ) ) ;
#64001=DIRECTION ( 'NONE',  ( 0.000000000000000000, -1.000000000000000000, 0.000000000000000000 ) ) ;
#64005=DIRECTION ( 'NONE',  ( -1.000000000000000000, -1.224606353822377258E-16, -0.000000000000000000 ) ) ;
#64068=ORIENTED_EDGE ( 'NONE', *, *, #55416, .F. ) ;
#64079=VERTEX_POINT ( 'NONE', #73228 ) ;
#64162=VERTEX_POINT ( 'NONE', #18227 ) ;
#64210=DIRECTION ( 'NONE',  ( -1.000000000000000000, -1.224606353822377258E-16, -0.000000000000000000 ) ) ;
#64234=CONICAL_SURFACE ( 'NONE', #83161, 5.000000000000010658, 0.9599310885968697082 ) ;
#64239=CIRCLE ( 'NONE', #81442, 5.000000000000010658 ) ;
#64287=CARTESIAN_POINT ( 'NONE',  ( 0.000000000000000000, 0.000000000000000000, 0.000000000000000000 ) ) ;
#64326=CONICAL_SURFACE ( 'NONE', #98700, 4.172000000000009479, 0.9599310885968813656 ) ;
#64340=CARTESIAN_POINT ( 'NONE',  ( 81.84444444444444855, -4.171999999999998820, 0.000000000000000000 ) ) ;
#64358=CIRCLE ( 'NONE', #17843, 5.000000000000010658 ) ;
#64368=CARTESIAN_POINT ( 'NONE',  ( 96.86866073052655679, 1.030564683017419500E-14, 0.000000000000000000 ) ) ;
#64401=CARTESIAN_POINT ( 'NONE',  ( 97.15356149169568312, 6.123233995736582872E-16, -5.000000000000011546 ) ) ;
#64505=EDGE_CURVE ( 'NONE', #4508, #80260, #63124, .T. ) ;
#64539=VERTEX_POINT ( 'NONE', #57449 ) ;
#64552=DIRECTION ( 'NONE',  ( 0.000000000000000000, -1.000000000000000000, 0.000000000000000000 ) ) ;
#64555=ORIENTED_EDGE ( 'NONE', *, *, #3634, .F. ) ;
#64566=EDGE_CURVE ( 'NONE', #19034, #52131, #82027, .T. ) ;
#64579=ORIENTED_EDGE ( 'NONE', *, *, #72187, .T. ) ;
#64587=VERTEX_POINT ( 'NONE', #82268 ) ;
#64598=VERTEX_POINT ( 'NONE', #9979 ) ;
#64611=AXIS2_PLACEMENT_3D ( 'NONE', #64287, #16784, #73942 ) ;
#64629=ORIENTED_EDGE ( 'NONE', *, *, #43936, .F. ) ;
#64694=EDGE_CURVE ( 'NONE', #45219, #231, #34294, .T. ) ;
#64721=DIRECTION ( 'NONE',  ( -1.000000000000000000, -0.000000000000000000, -0.000000000000000000 ) ) ;
#64744=CARTESIAN_POINT ( 'NONE',  ( 88.20199406385988539, -5.000000000000000888, 6.123233995736779101E-16 ) ) ;
#64752=DIRECTION ( 'NONE',  ( 0.000000000000000000, -1.000000000000000000, 0.000000000000000000 ) ) ;
#64753=ORIENTED_EDGE ( 'NONE', *, *, #59267, .F. ) ;
#64757=ORIENTED_EDGE ( 'NONE', *, *, #4076, .T. ) ;
#64777=CIRCLE ( 'NONE', #85503, 4.172000000000009479 ) ;
#64842=FACE_OUTER_BOUND ( 'NONE', #58718, .T. ) ;
#64872=DIRECTION ( 'NONE',  ( 1.000000000000000000, 1.224606353822377258E-16, 0.000000000000000000 ) ) ;
#64905=SHAPE_DEFINITION_REPRESENTATION ( #85495, #62661 ) ;
#64937=VERTEX_POINT ( 'NONE', #88133 ) ;
#64949=CIRCLE ( 'NONE', #21943, 5.000000000000011546 ) ;
#64954=CYLINDRICAL_SURFACE ( 'NONE', #13894, 5.000000000000000888 ) ;
#64959=EDGE_CURVE ( 'NONE', #69907, #64079, #21649, .T. ) ;
#64986=CARTESIAN_POINT ( 'NONE',  ( 84.15356149169568312, 1.016364837396684119E-14, 0.000000000000000000 ) ) ;
#64993=CARTESIAN_POINT ( 'NONE',  ( 102.9313392694734688, -5.000000000000000000, 0.000000000000000000 ) ) ;
#65017=CARTESIAN_POINT ( 'NONE',  ( 90.51111111111110574, -4.171999999999998820, 5.616230220889773285E-16 ) ) ;
#65024=DIRECTION ( 'NONE',  ( -1.000000000000000000, -0.000000000000000000, -0.000000000000000000 ) ) ;
#65040=DIRECTION ( 'NONE',  ( -1.000000000000000000, -1.224606353822377258E-16, -0.000000000000000000 ) ) ;
#65068=CARTESIAN_POINT ( 'NONE',  ( 105.5353273971932140, -2.002967142162725287E-29, 5.000000000000011546 ) ) ;
#65096=VERTEX_POINT ( 'NONE', #11428 ) ;
#65104=VECTOR ( 'NONE', #31497, 1000.000000000000000 ) ;
#65114=ORIENTED_EDGE ( 'NONE', *, *, #35625, .T. ) ;
#65125=CARTESIAN_POINT ( 'NONE',  ( 86.75754961941542831, 1.030564683017419500E-14, 0.000000000000000000 ) ) ;
#65170=CARTESIAN_POINT ( 'NONE',  ( 98.59800593614012598, 1.016364837396684119E-14, 0.000000000000000000 ) ) ;
#65175=DIRECTION ( 'NONE',  ( -1.000000000000000000, -1.224606353822377258E-16, -0.000000000000000000 ) ) ;
#65262=ORIENTED_EDGE ( 'NONE', *, *, #49824, .F. ) ;
#65278=ORIENTED_EDGE ( 'NONE', *, *, #66239, .F. ) ;
#65293=DIRECTION ( 'NONE',  ( -1.000000000000000000, -0.000000000000000000, -0.000000000000000000 ) ) ;
#65349=VECTOR ( 'NONE', #63203, 999.9999999999998863 ) ;
#65372=CIRCLE ( 'NONE', #106694, 5.000000000000011546 ) ;
#65449=CARTESIAN_POINT ( 'NONE',  ( 0.1317522424410015880, 1.959574484677832018, -8.000000000000003553 ) ) ;
#65463=CIRCLE ( 'NONE', #60327, 4.172000000000009479 ) ;
#65477=EDGE_CURVE ( 'NONE', #101891, #86867, #102692, .T. ) ;
#65481=ORIENTED_EDGE ( 'NONE', *, *, #27401, .T. ) ;
#65499=DIRECTION ( 'NONE',  ( -1.000000000000000000, -1.224606353822377258E-16, -0.000000000000000000 ) ) ;
#65522=CARTESIAN_POINT ( 'NONE',  ( 0.7145311798161605443, -4.618802153517258979, -8.000000000000001776 ) ) ;
#65562=ORIENTED_EDGE ( 'NONE', *, *, #77519, .F. ) ;
#65599=DIRECTION ( 'NONE',  ( 0.000000000000000000, 1.000000000000000000, 0.000000000000000000 ) ) ;
#65619=EDGE_CURVE ( 'NONE', #13325, #10855, #30073, .T. ) ;
#65623=AXIS2_PLACEMENT_3D ( 'NONE', #73915, #32965, #66364 ) ;
#65678=DIRECTION ( 'NONE',  ( 0.000000000000000000, -1.000000000000000000, 0.000000000000000000 ) ) ;
#65682=LINE ( 'NONE', #105088, #93192 ) ;
#65693=CYLINDRICAL_SURFACE ( 'NONE', #83413, 5.000000000000000888 ) ;
#65695=AXIS2_PLACEMENT_3D ( 'NONE', #36920, #61721, #43388 ) ;
#65709=DIRECTION ( 'NONE',  ( 1.000000000000000000, 0.000000000000000000, 0.000000000000000000 ) ) ;
#65774=VERTEX_POINT ( 'NONE', #16513 ) ;
#65779=ADVANCED_FACE ( 'NONE', ( #7877 ), #68197, .T. ) ;
#65830=AXIS2_PLACEMENT_3D ( 'NONE', #56101, #30832, #14064 ) ;
#65832=DIRECTION ( 'NONE',  ( 0.000000000000000000, 1.000000000000000000, 0.000000000000000000 ) ) ;
#65843=ADVANCED_FACE ( 'NONE', ( #38002 ), #96738, .T. ) ;
#65870=CARTESIAN_POINT ( 'NONE',  ( 0.08224679563971280805, 6.145890662064650733, -5.355005115540897087 ) ) ;
#65872=EDGE_CURVE ( 'NONE', #90932, #105278, #88116, .T. ) ;
#65891=LINE ( 'NONE', #75028, #18498 ) ;
#65901=DIRECTION ( 'NONE',  ( -1.000000000000000000, -0.000000000000000000, -0.000000000000000000 ) ) ;
#65941=ORIENTED_EDGE ( 'NONE', *, *, #61209, .F. ) ;
#65967=FACE_OUTER_BOUND ( 'NONE', #62609, .T. ) ;
#66005=DIRECTION ( 'NONE',  ( 0.000000000000000000, -1.000000000000000000, 0.000000000000000000 ) ) ;
#66016=DIRECTION ( 'NONE',  ( -0.5735764363510459374, -0.8191520442889919096, 0.000000000000000000 ) ) ;
#66020=CARTESIAN_POINT ( 'NONE',  ( 93.39999999999999147, 1.023464760207051730E-14, 0.000000000000000000 ) ) ;
#66046=DIRECTION ( 'NONE',  ( 0.000000000000000000, 0.000000000000000000, 1.000000000000000000 ) ) ;
#66074=ORIENTED_EDGE ( 'NONE', *, *, #100184, .F. ) ;
#66171=AXIS2_PLACEMENT_3D ( 'NONE', #76405, #35468, #3607 ) ;
#66174=ORIENTED_EDGE ( 'NONE', *, *, #38172, .F. ) ;
#66176=VECTOR ( 'NONE', #13521, 1000.000000000000000 ) ;
#66187=ORIENTED_EDGE ( 'NONE', *, *, #32373, .T. ) ;
#66239=EDGE_CURVE ( 'NONE', #70163, #13347, #6224, .T. ) ;
#66274=DIRECTION ( 'NONE',  ( 1.000000000000000000, 0.000000000000000000, -0.000000000000000000 ) ) ;
#66293=AXIS2_PLACEMENT_3D ( 'NONE', #103344, #54763, #104385 ) ;
#66364=DIRECTION ( 'NONE',  ( 0.000000000000000000, -1.000000000000000000, 0.000000000000000000 ) ) ;
#66401=ORIENTED_EDGE ( 'NONE', *, *, #106403, .T. ) ;
#66428=AXIS2_PLACEMENT_3D ( 'NONE', #100651, #44020, #75851 ) ;
#66440=FACE_OUTER_BOUND ( 'NONE', #94428, .T. ) ;
#66450=AXIS2_PLACEMENT_3D ( 'NONE', #16943, #49820, #82725 ) ;
#66462=CARTESIAN_POINT ( 'NONE',  ( 6.400000000000000355, 0.000000000000000000, 0.000000000000000000 ) ) ;
#66478=FILL_AREA_STYLE ('',( #33605 ) ) ;
#66494=DIRECTION ( 'NONE',  ( 0.000000000000000000, 0.000000000000000000, 1.000000000000000000 ) ) ;
#66531=LINE ( 'NONE', #47677, #20968 ) ;
#66540=VERTEX_POINT ( 'NONE', #51471 ) ;
#66553=DIRECTION ( 'NONE',  ( 0.000000000000000000, -1.000000000000000000, 0.000000000000000000 ) ) ;
#66580=ORIENTED_EDGE ( 'NONE', *, *, #82743, .T. ) ;
#66616=DIRECTION ( 'NONE',  ( -1.000000000000000000, -1.224606353822377258E-16, -0.000000000000000000 ) ) ;
#66716=ORIENTED_EDGE ( 'NONE', *, *, #88636, .T. ) ;
#66755=DIRECTION ( 'NONE',  ( 0.000000000000000000, -1.000000000000000000, 0.000000000000000000 ) ) ;
#66769=ADVANCED_FACE ( 'NONE', ( #81555 ), #51222, .T. ) ;
#66796=CARTESIAN_POINT ( 'NONE',  ( 89.06666666666666288, 4.172000000000019249, 0.000000000000000000 ) ) ;
#66813=DIRECTION ( 'NONE',  ( 0.000000000000000000, -1.000000000000000000, 0.000000000000000000 ) ) ;
#66848=AXIS2_PLACEMENT_3D ( 'NONE', #17368, #50240, #73975 ) ;
#66857=CARTESIAN_POINT ( 'NONE',  ( 102.0666666666666629, 1.023464760207051730E-14, 0.000000000000000000 ) ) ;
#66904=CIRCLE ( 'NONE', #70370, 5.000000000000010658 ) ;
#66906=ORIENTED_EDGE ( 'NONE', *, *, #82986, .T. ) ;
#66908=CARTESIAN_POINT ( 'NONE',  ( 103.5111111111111057, -4.171999999999998820, 5.616230220889773285E-16 ) ) ;
#66979=FACE_OUTER_BOUND ( 'NONE', #70404, .T. ) ;
#66980=ORIENTED_EDGE ( 'NONE', *, *, #29370, .F. ) ;
#66985=DIRECTION ( 'NONE',  ( 0.000000000000000000, -1.000000000000000000, 0.000000000000000000 ) ) ;
#66990=VECTOR ( 'NONE', #42062, 1000.000000000000000 ) ;
#67035=VECTOR ( 'NONE', #44902, 999.9999999999998863 ) ;
#67041=CARTESIAN_POINT ( 'NONE',  ( 95.70911704725124025, 1.016364837396684119E-14, 0.000000000000000000 ) ) ;
#67077=ORIENTED_EDGE ( 'NONE', *, *, #51724, .T. ) ;
#67085=ORIENTED_EDGE ( 'NONE', *, *, #36033, .T. ) ;
#67116=DIRECTION ( 'NONE',  ( -1.000000000000000000, -1.224606353822377258E-16, -0.000000000000000000 ) ) ;
#67123=ORIENTED_EDGE ( 'NONE', *, *, #93201, .F. ) ;
#67138=EDGE_CURVE ( 'NONE', #49495, #102339, #40854, .T. ) ;
#67158=AXIS2_PLACEMENT_3D ( 'NONE', #59160, #82890, #102121 ) ;
#67173=ORIENTED_EDGE ( 'NONE', *, *, #80679, .F. ) ;
#67206=DIRECTION ( 'NONE',  ( -0.5735764363510459374, -0.8191520442889919096, 0.000000000000000000 ) ) ;
#67230=ORIENTED_EDGE ( 'NONE', *, *, #33, .T. ) ;
#67302=AXIS2_PLACEMENT_3D ( 'NONE', #80880, #62086, #53948 ) ;
#67307=CARTESIAN_POINT ( 'NONE',  ( 106.4000000000000057, 5.109226446042757607E-16, -4.171999999999999709 ) ) ;
#67308=CARTESIAN_POINT ( 'NONE',  ( 92.53532739719321398, 1.030564683017419500E-14, 0.000000000000000000 ) ) ;
#67314=DIRECTION ( 'NONE',  ( -1.000000000000000000, -0.000000000000000000, -0.000000000000000000 ) ) ;
#67315=LINE ( 'NONE', #9048, #89071 ) ;
#67340=EDGE_CURVE ( 'NONE', #9861, #37699, #40922, .T. ) ;
#67385=ORIENTED_EDGE ( 'NONE', *, *, #11882, .F. ) ;
#67422=LINE ( 'NONE', #18353, #52717 ) ;
#67467=CIRCLE ( 'NONE', #100178, 5.000000000000011546 ) ;
#67468=ORIENTED_EDGE ( 'NONE', *, *, #84026, .T. ) ;
#67596=CARTESIAN_POINT ( 'NONE',  ( 95.42421628608209971, -5.000000000000000000, 6.123233995736778115E-16 ) ) ;
#67633=CONICAL_SURFACE ( 'NONE', #95196, 5.000000000000010658, 0.9599310885968697082 ) ;
#67654=VERTEX_POINT ( 'NONE', #101645 ) ;
#67657=ORIENTED_EDGE ( 'NONE', *, *, #50054, .F. ) ;
#67676=CARTESIAN_POINT ( 'NONE',  ( 82.42421628608209971, 1.030564683017419500E-14, 0.000000000000000000 ) ) ;
#67685=DIRECTION ( 'NONE',  ( 0.000000000000000000, -1.000000000000000000, 0.000000000000000000 ) ) ;
#67731=DIRECTION ( 'NONE',  ( 1.000000000000000000, 1.224606353822377258E-16, 0.000000000000000000 ) ) ;
#67743=EDGE_CURVE ( 'NONE', #48515, #35853, #74567, .T. ) ;
#67758=DIRECTION ( 'NONE',  ( 0.000000000000000000, -1.000000000000000000, 0.000000000000000000 ) ) ;
#67780=ORIENTED_EDGE ( 'NONE', *, *, #105111, .T. ) ;
#67821=CARTESIAN_POINT ( 'NONE',  ( 83.86866073052654258, 1.030564683017419500E-14, 0.000000000000000000 ) ) ;
#67827=LINE ( 'NONE', #50035, #89322 ) ;
#67831=CARTESIAN_POINT ( 'NONE',  ( 5.799999999999999822, 8.000000000000000000, 0.000000000000000000 ) ) ;
#67846=CARTESIAN_POINT ( 'NONE',  ( 91.37578371391791165, 1.016364837396684119E-14, 0.000000000000000000 ) ) ;
#67880=CARTESIAN_POINT ( 'NONE',  ( 96.86866073052655679, 5.000000000000021316, 0.000000000000000000 ) ) ;
#67952=LINE ( 'NONE', #26999, #101297 ) ;
#67965=DIRECTION ( 'NONE',  ( 0.5735764363510554853, 0.8191520442889852482, 0.000000000000000000 ) ) ;
#67967=ADVANCED_FACE ( 'NONE', ( #20655 ), #78876, .T. ) ;
#68000=DIRECTION ( 'NONE',  ( -1.000000000000000000, -1.224606353822377258E-16, -0.000000000000000000 ) ) ;
#68018=CARTESIAN_POINT ( 'NONE',  ( 80.40000000000000568, 4.172000000000019249, 5.109226446042768454E-16 ) ) ;
#68020=DIRECTION ( 'NONE',  ( -1.000000000000000000, -1.224606353822377258E-16, -0.000000000000000000 ) ) ;
#68047=VECTOR ( 'NONE', #11924, 1000.000000000000000 ) ;
#68079=SURFACE_STYLE_USAGE ( .BOTH. , #2258 ) ;
#68104=DIRECTION ( 'NONE',  ( 0.000000000000000000, 0.000000000000000000, -1.000000000000000000 ) ) ;
#68106=AXIS2_PLACEMENT_3D ( 'NONE', #14215, #47118, #42214 ) ;
#68108=EDGE_CURVE ( 'NONE', #23629, #44644, #90990, .T. ) ;
#68144=DIRECTION ( 'NONE',  ( 1.000000000000000000, 1.224606353822377258E-16, 0.000000000000000000 ) ) ;
#68164=DIRECTION ( 'NONE',  ( 0.000000000000000000, -1.000000000000000000, 0.000000000000000000 ) ) ;
#68188=ORIENTED_EDGE ( 'NONE', *, *, #2642, .T. ) ;
#68197=CONICAL_SURFACE ( 'NONE', #35501, 5.000000000000010658, 0.9599310885968697082 ) ;
#68209=EDGE_CURVE ( 'NONE', #7953, #57657, #67952, .T. ) ;
#68215=AXIS2_PLACEMENT_3D ( 'NONE', #50765, #91791, #9783 ) ;
#68222=DIRECTION ( 'NONE',  ( -1.000000000000000000, -0.000000000000000000, -0.000000000000000000 ) ) ;
#68288=AXIS2_PLACEMENT_3D ( 'NONE', #70728, #103622, #29770 ) ;
#68307=ORIENTED_EDGE ( 'NONE', *, *, #20482, .T. ) ;
#68348=FACE_OUTER_BOUND ( 'NONE', #51274, .T. ) ;
#68349=EDGE_CURVE ( 'NONE', #101881, #49122, #90502, .T. ) ;
#68366=CONICAL_SURFACE ( 'NONE', #4620, 4.172000000000009479, 0.9599310885968813656 ) ;
#68404=ORIENTED_EDGE ( 'NONE', *, *, #77541, .F. ) ;
#68406=VECTOR ( 'NONE', #86772, 999.9999999999998863 ) ;
#68521=EDGE_CURVE ( 'NONE', #53206, #6761, #6657, .T. ) ;
#68542=EDGE_CURVE ( 'NONE', #73679, #87052, #106518, .T. ) ;
#68544=DIRECTION ( 'NONE',  ( 0.000000000000000000, -1.000000000000000000, 0.000000000000000000 ) ) ;
#68560=ADVANCED_FACE ( 'NONE', ( #94654 ), #20799, .T. ) ;
#68603=EDGE_LOOP ( 'NONE', ( #25960, #103777, #43351, #46760, #20234 ) ) ;
#68618=ORIENTED_EDGE ( 'NONE', *, *, #104465, .F. ) ;
#68623=ADVANCED_FACE ( 'NONE', ( #65967 ), #39595, .T. ) ;
#68664=DIRECTION ( 'NONE',  ( -1.000000000000000000, -1.224606353822377258E-16, -0.000000000000000000 ) ) ;
#68665=AXIS2_PLACEMENT_3D ( 'NONE', #7899, #8962, #73699 ) ;
#68669=LINE ( 'NONE', #67596, #6143 ) ;
#68718=CARTESIAN_POINT ( 'NONE',  ( 82.42421628608209971, 5.000000000000020428, 0.000000000000000000 ) ) ;
#68720=LINE ( 'NONE', #75174, #54920 ) ;
#68729=CARTESIAN_POINT ( 'NONE',  ( 100.6222222222222200, 1.023464760207051730E-14, 0.000000000000000000 ) ) ;
#68745=ORIENTED_EDGE ( 'NONE', *, *, #93701, .F. ) ;
#68754=ORIENTED_EDGE ( 'NONE', *, *, #73796, .F. ) ;
#68820=EDGE_LOOP ( 'NONE', ( #90013, #8154, #26089, #91498, #96585, #104931 ) ) ;
#68895=AXIS2_PLACEMENT_3D ( 'NONE', #98255, #24408, #57247 ) ;
#68926=VERTEX_POINT ( 'NONE', #60034 ) ;
#68947=EDGE_CURVE ( 'NONE', #68926, #40910, #92888, .T. ) ;
#68960=EDGE_CURVE ( 'NONE', #102006, #6367, #103645, .T. ) ;
#68974=FACE_OUTER_BOUND ( 'NONE', #69467, .T. ) ;
#68981=ORIENTED_EDGE ( 'NONE', *, *, #72650, .T. ) ;
#69078=CARTESIAN_POINT ( 'NONE',  ( 0.7145311798163270778, 9.237604307034018802, 3.185620757954082679E-16 ) ) ;
#69088=EDGE_CURVE ( 'NONE', #70018, #23629, #5486, .T. ) ;
#69161=SHAPE_REPRESENTATION_RELATIONSHIP ( 'NONE' , 'NONE' ,  #62661, #7337 ) ;
#69191=DIRECTION ( 'NONE',  ( 1.000000000000000000, 0.000000000000000000, -0.000000000000000000 ) ) ;
#69201=AXIS2_PLACEMENT_3D ( 'NONE', #43196, #76611, #2182 ) ;
#69203=DIRECTION ( 'NONE',  ( -1.000000000000000000, -1.224606353822377258E-16, -0.000000000000000000 ) ) ;
#69230=ADVANCED_FACE ( 'NONE', ( #81463 ), #96310, .T. ) ;
#69232=FACE_OUTER_BOUND ( 'NONE', #52397, .T. ) ;
#69258=CIRCLE ( 'NONE', #33148, 5.000000000000011546 ) ;
#69306=FACE_OUTER_BOUND ( 'NONE', #97019, .T. ) ;
#69327=VERTEX_POINT ( 'NONE', #88883 ) ;
#69388=LINE ( 'NONE', #53718, #51744 ) ;
#69467=EDGE_LOOP ( 'NONE', ( #37233, #92526, #15623, #38928, #2050 ) ) ;
#69562=DIRECTION ( 'NONE',  ( 0.000000000000000000, -1.000000000000000000, 0.000000000000000000 ) ) ;
#69577=DIRECTION ( 'NONE',  ( -1.000000000000000000, -0.000000000000000000, -0.000000000000000000 ) ) ;
#69596=ORIENTED_EDGE ( 'NONE', *, *, #28069, .T. ) ;
#69606=LINE ( 'NONE', #22126, #94246 ) ;
#69648=CARTESIAN_POINT ( 'NONE',  ( 0.000000000000000000, 6.123233995736767268E-16, -5.000000000000000888 ) ) ;
#69651=CARTESIAN_POINT ( 'NONE',  ( 89.93133926947346879, 1.016364837396684119E-14, 0.000000000000000000 ) ) ;
#69655=ORIENTED_EDGE ( 'NONE', *, *, #64694, .T. ) ;
#69711=CARTESIAN_POINT ( 'NONE',  ( 0.01688885742776657928, -7.321065037175427115, -3.319543390096029611 ) ) ;
#69773=ORIENTED_EDGE ( 'NONE', *, *, #135, .F. ) ;
#69860=CARTESIAN_POINT ( 'NONE',  ( 80.40000000000000568, -4.171999999999998820, 5.616230220889773285E-16 ) ) ;
#69904=CARTESIAN_POINT ( 'NONE',  ( 106.4000000000000057, 0.000000000000000000, 4.171999999999999709 ) ) ;
#69907=VERTEX_POINT ( 'NONE', #60195 ) ;
#69947=EDGE_LOOP ( 'NONE', ( #32390, #61856, #102876, #71490, #27434, #26316 ) ) ;
#69988=ORIENTED_EDGE ( 'NONE', *, *, #11015, .T. ) ;
#70007=ORIENTED_EDGE ( 'NONE', *, *, #40426, .F. ) ;
#70018=VERTEX_POINT ( 'NONE', #18127 ) ;
#70024=ORIENTED_EDGE ( 'NONE', *, *, #68542, .T. ) ;
#70071=AXIS2_PLACEMENT_3D ( 'NONE', #88150, #104859, #80031 ) ;
#70074=ADVANCED_FACE ( 'NONE', ( #53659 ), #6890, .T. ) ;
#70084=DIRECTION ( 'NONE',  ( -1.000000000000000000, -1.224606353822377258E-16, -0.000000000000000000 ) ) ;
#70107=VECTOR ( 'NONE', #100721, 1000.000000000000000 ) ;
#70163=VERTEX_POINT ( 'NONE', #86591 ) ;
#70174=AXIS2_PLACEMENT_3D ( 'NONE', #3462, #50921, #36406 ) ;
#70189=ORIENTED_EDGE ( 'NONE', *, *, #13042, .T. ) ;
#70192=AXIS2_PLACEMENT_3D ( 'NONE', #8226, #64872, #7682 ) ;
#70196=CARTESIAN_POINT ( 'NONE',  ( 94.84444444444443434, 4.172000000000019249, 0.000000000000000000 ) ) ;
#70230=ORIENTED_EDGE ( 'NONE', *, *, #104685, .F. ) ;
#70233=DIRECTION ( 'NONE',  ( -1.000000000000000000, -0.000000000000000000, -0.000000000000000000 ) ) ;
#70248=CARTESIAN_POINT ( 'NONE',  ( 99.75754961941544252, -2.002967142162725287E-29, 5.000000000000011546 ) ) ;
#70267=EDGE_CURVE ( 'NONE', #3027, #59923, #60351, .T. ) ;
#70271=FACE_OUTER_BOUND ( 'NONE', #8114, .T. ) ;
#70287=CARTESIAN_POINT ( 'NONE',  ( 6.400000000000000355, 0.000000000000000000, 0.000000000000000000 ) ) ;
#70295=CARTESIAN_POINT ( 'NONE',  ( 88.20199406385988539, 6.123233995736568081E-16, -5.000000000000011546 ) ) ;
#70296=CARTESIAN_POINT ( 'NONE',  ( 98.59800593614012598, 5.000000000000042633, 6.123233995736805725E-16 ) ) ;
#70298=CARTESIAN_POINT ( 'NONE',  ( 85.31310517497098544, 1.030564683017419500E-14, 0.000000000000000000 ) ) ;
#70303=DIRECTION ( 'NONE',  ( -0.5735764363510459374, -0.8191520442889919096, 0.000000000000000000 ) ) ;
#70370=AXIS2_PLACEMENT_3D ( 'NONE', #100961, #43265, #20103 ) ;
#70372=FACE_OUTER_BOUND ( 'NONE', #1092, .T. ) ;
#70384=DIRECTION ( 'NONE',  ( -1.000000000000000000, -1.224606353822377258E-16, -0.000000000000000000 ) ) ;
#70404=EDGE_LOOP ( 'NONE', ( #74749, #39361, #65481, #14571, #53064, #15827 ) ) ;
#70444=CARTESIAN_POINT ( 'NONE',  ( 100.0424503805845831, -2.002967142162725287E-29, 5.000000000000011546 ) ) ;
#70468=EDGE_LOOP ( 'NONE', ( #76387, #32336, #8680, #39027, #7402 ) ) ;
#70487=EDGE_CURVE ( 'NONE', #88742, #58039, #32060, .T. ) ;
#70491=AXIS2_PLACEMENT_3D ( 'NONE', #92384, #35251, #25582 ) ;
#70502=DIRECTION ( 'NONE',  ( 0.000000000000000000, -1.000000000000000000, 0.000000000000000000 ) ) ;
#70506=DIRECTION ( 'NONE',  ( 1.000000000000000000, 1.224606353822377258E-16, 0.000000000000000000 ) ) ;
#70522=LINE ( 'NONE', #38182, #20074 ) ;
#70629=CIRCLE ( 'NONE', #58633, 8.000000000000000000 ) ;
#70684=CYLINDRICAL_SURFACE ( 'NONE', #58282, 5.000000000000000888 ) ;
#70694=CIRCLE ( 'NONE', #84475, 4.172000000000009479 ) ;
#70696=ORIENTED_EDGE ( 'NONE', *, *, #75342, .T. ) ;
#70728=CARTESIAN_POINT ( 'NONE',  ( 0.000000000000000000, 0.000000000000000000, 0.000000000000000000 ) ) ;
#70744=ADVANCED_FACE ( 'NONE', ( #95868 ), #39232, .T. ) ;
#70764=LINE ( 'NONE', #37377, #57009 ) ;
#70771=TOROIDAL_SURFACE ( 'NONE', #39834, 5.400000000000001243, 0.4000000000000000222 ) ;
#70828=PLANE ( 'NONE',  #96270 ) ;
#70850=DIRECTION ( 'NONE',  ( -0.000000000000000000, 0.5000000000000008882, 0.8660254037844381525 ) ) ;
#70864=EDGE_CURVE ( 'NONE', #82194, #16556, #16525, .T. ) ;
#70904=DIRECTION ( 'NONE',  ( 0.000000000000000000, -1.000000000000000000, 0.000000000000000000 ) ) ;
#70909=DIRECTION ( 'NONE',  ( 0.000000000000000000, -1.000000000000000000, 0.000000000000000000 ) ) ;
#70913=CARTESIAN_POINT ( 'NONE',  ( 102.6464385083043283, 1.030564683017419500E-14, 0.000000000000000000 ) ) ;
#70959=EDGE_LOOP ( 'NONE', ( #65941, #25230, #90876, #72833, #80304, #77939 ) ) ;
#71048=FACE_OUTER_BOUND ( 'NONE', #48911, .T. ) ;
#71050=ORIENTED_EDGE ( 'NONE', *, *, #81040, .T. ) ;
#71082=VERTEX_POINT ( 'NONE', #62855 ) ;
#71092=ORIENTED_EDGE ( 'NONE', *, *, #16762, .T. ) ;
#71169=VECTOR ( 'NONE', #83473, 1000.000000000000000 ) ;
#71183=EDGE_CURVE ( 'NONE', #80260, #22089, #48226, .T. ) ;
#71190=EDGE_LOOP ( 'NONE', ( #45771, #43855, #95353, #82024, #78324 ) ) ;
#71194=DIRECTION ( 'NONE',  ( 0.000000000000000000, -1.000000000000000000, 0.000000000000000000 ) ) ;
#71225=ORIENTED_EDGE ( 'NONE', *, *, #54336, .F. ) ;
#71282=CARTESIAN_POINT ( 'NONE',  ( 86.75754961941542831, 5.000000000000020428, 0.000000000000000000 ) ) ;
#71314=ORIENTED_EDGE ( 'NONE', *, *, #4634, .T. ) ;
#71316=VERTEX_POINT ( 'NONE', #18557 ) ;
#71331=AXIS2_PLACEMENT_3D ( 'NONE', #27107, #60522, #75067 ) ;
#71333=DIRECTION ( 'NONE',  ( -1.000000000000000000, -0.000000000000000000, 0.000000000000000000 ) ) ;
#71358=CYLINDRICAL_SURFACE ( 'NONE', #63309, 5.000000000000000888 ) ;
#71364=CIRCLE ( 'NONE', #93787, 5.000000000000010658 ) ;
#71365=AXIS2_PLACEMENT_3D ( 'NONE', #17845, #9714, #43694 ) ;
#71469=EDGE_CURVE ( 'NONE', #73679, #54417, #30362, .T. ) ;
#71490=ORIENTED_EDGE ( 'NONE', *, *, #82986, .F. ) ;
#71498=AXIS2_PLACEMENT_3D ( 'NONE', #104972, #31113, #64001 ) ;
#71535=CARTESIAN_POINT ( 'NONE',  ( 94.26467260280679739, 1.016364837396684119E-14, 0.000000000000000000 ) ) ;
#71551=EDGE_CURVE ( 'NONE', #95902, #20011, #37944, .T. ) ;
#71564=EDGE_LOOP ( 'NONE', ( #22565, #46306, #4761, #46047, #106711 ) ) ;
#71581=EDGE_LOOP ( 'NONE', ( #56060, #81314, #101024, #50343, #66580 ) ) ;
#71633=DIRECTION ( 'NONE',  ( -1.000000000000000000, -0.000000000000000000, -0.000000000000000000 ) ) ;
#71667=EDGE_CURVE ( 'NONE', #37934, #70163, #75789, .T. ) ;
#71679=DIRECTION ( 'NONE',  ( -1.000000000000000000, -0.000000000000000000, -0.000000000000000000 ) ) ;
#71717=AXIS2_PLACEMENT_3D ( 'NONE', #2414, #26742, #1328 ) ;
#71726=ADVANCED_FACE ( 'NONE', ( #83650 ), #87821, .T. ) ;
#71731=DIRECTION ( 'NONE',  ( 0.000000000000000000, -1.000000000000000000, 0.000000000000000000 ) ) ;
#71753=DIRECTION ( 'NONE',  ( 1.000000000000000000, 0.000000000000000000, -0.000000000000000000 ) ) ;
#71756=LINE ( 'NONE', #28702, #66176 ) ;
#71787=ORIENTED_EDGE ( 'NONE', *, *, #67743, .T. ) ;
#71793=EDGE_CURVE ( 'NONE', #78511, #40136, #43740, .T. ) ;
#71809=CARTESIAN_POINT ( 'NONE',  ( 96.86866073052655679, 1.030564683017419500E-14, 0.000000000000000000 ) ) ;
#71898=CARTESIAN_POINT ( 'NONE',  ( 86.17777777777776294, 1.023464760207051730E-14, 0.000000000000000000 ) ) ;
#71935=EDGE_LOOP ( 'NONE', ( #67077, #1553, #14202, #31541, #21262, #66174 ) ) ;
#71968=EDGE_LOOP ( 'NONE', ( #70230, #80000, #53799, #38716, #22792 ) ) ;
#72008=CARTESIAN_POINT ( 'NONE',  ( 91.95555555555554861, 4.172000000000019249, 0.000000000000000000 ) ) ;
#72040=AXIS2_PLACEMENT_3D ( 'NONE', #74477, #51262, #17336 ) ;
#72051=AXIS2_PLACEMENT_3D ( 'NONE', #70913, #7223, #104328 ) ;
#72054=ADVANCED_FACE ( 'NONE', ( #87677 ), #13725, .T. ) ;
#72084=DIRECTION ( 'NONE',  ( 0.5735764363510557073, -0.8191520442889850262, 1.003171929053516612E-16 ) ) ;
#72098=CONICAL_SURFACE ( 'NONE', #85913, 4.172000000000009479, 0.9599310885968813656 ) ;
#72103=EDGE_LOOP ( 'NONE', ( #31905, #102505, #46774, #83893, #101098, #63074 ) ) ;
#72107=CARTESIAN_POINT ( 'NONE',  ( 0.000000000000000000, 0.000000000000000000, 0.000000000000000000 ) ) ;
#72180=CARTESIAN_POINT ( 'NONE',  ( 102.9313392694734688, 1.016364837396684119E-14, 0.000000000000000000 ) ) ;
#72187=EDGE_CURVE ( 'NONE', #10153, #85648, #50001, .T. ) ;
#72395=ORIENTED_EDGE ( 'NONE', *, *, #36971, .T. ) ;
#72405=ORIENTED_EDGE ( 'NONE', *, *, #1705, .F. ) ;
#72449=DIRECTION ( 'NONE',  ( 0.000000000000000000, -1.000000000000000000, 3.755786496842903988E-16 ) ) ;
#72460=ORIENTED_EDGE ( 'NONE', *, *, #73329, .F. ) ;
#72470=AXIS2_PLACEMENT_3D ( 'NONE', #58680, #33353, #41948 ) ;
#72471=CARTESIAN_POINT ( 'NONE',  ( 0.7145311798163219708, 4.618802153517003184, -8.000000000000000000 ) ) ;
#72590=LINE ( 'NONE', #55848, #89954 ) ;
#72650=EDGE_CURVE ( 'NONE', #64937, #17510, #58643, .T. ) ;
#72677=ORIENTED_EDGE ( 'NONE', *, *, #25714, .F. ) ;
#72699=CARTESIAN_POINT ( 'NONE',  ( 105.5353273971932140, 1.030564683017419500E-14, 0.000000000000000000 ) ) ;
#72778=DIRECTION ( 'NONE',  ( -1.000000000000000000, -1.224606353822377258E-16, -0.000000000000000000 ) ) ;
#72820=DIRECTION ( 'NONE',  ( -1.000000000000000000, -1.224606353822377258E-16, -0.000000000000000000 ) ) ;
#72827=DIRECTION ( 'NONE',  ( 0.000000000000000000, -1.000000000000000000, 0.000000000000000000 ) ) ;
#72833=ORIENTED_EDGE ( 'NONE', *, *, #48668, .T. ) ;
#72867=CARTESIAN_POINT ( 'NONE',  ( 104.0908829527487711, 1.030564683017419500E-14, 0.000000000000000000 ) ) ;
#72887=EDGE_LOOP ( 'NONE', ( #62483, #56136, #28424, #65562, #67173 ) ) ;
#72914=VERTEX_POINT ( 'NONE', #10863 ) ;
#72930=DIRECTION ( 'NONE',  ( -1.000000000000000000, -1.224606353822377258E-16, -0.000000000000000000 ) ) ;
#72941=VECTOR ( 'NONE', #56770, 1000.000000000000000 ) ;
#72949=VERTEX_POINT ( 'NONE', #27652 ) ;
#72963=CARTESIAN_POINT ( 'NONE',  ( 0.000000000000000000, 0.000000000000000000, 0.000000000000000000 ) ) ;
#72970=CIRCLE ( 'NONE', #11001, 5.000000000000011546 ) ;
#72998=ORIENTED_EDGE ( 'NONE', *, *, #6457, .T. ) ;
#73002=CONICAL_SURFACE ( 'NONE', #71331, 4.172000000000009479, 0.9599310885968813656 ) ;
#73013=EDGE_LOOP ( 'NONE', ( #46143, #33374, #57968, #52753, #89257, #15974 ) ) ;
#73027=DIRECTION ( 'NONE',  ( -1.000000000000000000, -0.000000000000000000, -0.000000000000000000 ) ) ;
#73037=AXIS2_PLACEMENT_3D ( 'NONE', #5803, #89399, #103445 ) ;
#73041=CIRCLE ( 'NONE', #74740, 5.000000000000010658 ) ;
#73043=DIRECTION ( 'NONE',  ( 1.000000000000000000, 1.224606353822377258E-16, 0.000000000000000000 ) ) ;
#73138=EDGE_CURVE ( 'NONE', #5546, #33098, #1861, .T. ) ;
#73168=DIRECTION ( 'NONE',  ( -1.000000000000000000, -1.224606353822377258E-16, -0.000000000000000000 ) ) ;
#73191=EDGE_CURVE ( 'NONE', #93942, #16556, #93127, .T. ) ;
#73228=CARTESIAN_POINT ( 'NONE',  ( 104.9555555555555486, 4.172000000000019249, 0.000000000000000000 ) ) ;
#73236=CARTESIAN_POINT ( 'NONE',  ( 101.2019940638598854, 5.000000000000020428, 0.000000000000000000 ) ) ;
#73274=EDGE_LOOP ( 'NONE', ( #49232, #41078 ) ) ;
#73329=EDGE_CURVE ( 'NONE', #22473, #54377, #14579, .T. ) ;
#73339=CARTESIAN_POINT ( 'NONE',  ( 0.000000000000000000, 0.000000000000000000, 0.000000000000000000 ) ) ;
#73356=DIRECTION ( 'NONE',  ( -1.000000000000000000, -0.000000000000000000, -0.000000000000000000 ) ) ;
#73361=CIRCLE ( 'NONE', #47505, 4.172000000000009479 ) ;
#73379=VERTEX_POINT ( 'NONE', #42586 ) ;
#73403=FACE_OUTER_BOUND ( 'NONE', #29199, .T. ) ;
#73424=ORIENTED_EDGE ( 'NONE', *, *, #7874, .T. ) ;
#73431=CIRCLE ( 'NONE', #97523, 5.000000000000010658 ) ;
#73445=CYLINDRICAL_SURFACE ( 'NONE', #19749, 5.000000000000000888 ) ;
#73474=EDGE_CURVE ( 'NONE', #74667, #77225, #48369, .T. ) ;
#73476=ORIENTED_EDGE ( 'NONE', *, *, #11221, .T. ) ;
#73513=EDGE_CURVE ( 'NONE', #49616, #71082, #91437, .T. ) ;
#73575=DIRECTION ( 'NONE',  ( -1.000000000000000000, -1.224606353822377258E-16, -0.000000000000000000 ) ) ;
#73591=ORIENTED_EDGE ( 'NONE', *, *, #13029, .T. ) ;
#73615=VERTEX_POINT ( 'NONE', #60920 ) ;
#73658=ORIENTED_EDGE ( 'NONE', *, *, #38225, .F. ) ;
#73676=VECTOR ( 'NONE', #35282, 1000.000000000000000 ) ;
#73679=VERTEX_POINT ( 'NONE', #78662 ) ;
#73699=DIRECTION ( 'NONE',  ( 0.000000000000000000, -1.000000000000000000, 0.000000000000000000 ) ) ;
#73712=DIRECTION ( 'NONE',  ( -1.000000000000000000, -1.224606353822377258E-16, -0.000000000000000000 ) ) ;
#73726=EDGE_LOOP ( 'NONE', ( #44277, #77806, #92663, #49833, #41790 ) ) ;
#73727=ORIENTED_EDGE ( 'NONE', *, *, #6369, .F. ) ;
#73745=ADVANCED_FACE ( 'NONE', ( #77624 ), #79739, .T. ) ;
#73766=FACE_OUTER_BOUND ( 'NONE', #80328, .T. ) ;
#73778=CARTESIAN_POINT ( 'NONE',  ( 89.64643850830432825, 5.000000000000020428, 0.000000000000000000 ) ) ;
#73796=EDGE_CURVE ( 'NONE', #76618, #20011, #65682, .T. ) ;
#73798=CIRCLE ( 'NONE', #1422, 4.172000000000009479 ) ;
#73816=EDGE_CURVE ( 'NONE', #101881, #28693, #82875, .T. ) ;
#73849=DIRECTION ( 'NONE',  ( 0.000000000000000000, 1.000000000000000000, 0.000000000000000000 ) ) ;
#73854=CIRCLE ( 'NONE', #1545, 5.000000000000010658 ) ;
#73868=CARTESIAN_POINT ( 'NONE',  ( 95.42421628608209971, 1.030564683017419500E-14, 0.000000000000000000 ) ) ;
#73888=AXIS2_PLACEMENT_3D ( 'NONE', #77124, #69577, #3239 ) ;
#73915=CARTESIAN_POINT ( 'NONE',  ( 97.73333333333333428, 1.023464760207051730E-14, 0.000000000000000000 ) ) ;
#73924=CARTESIAN_POINT ( 'NONE',  ( 100.6222222222222200, 4.172000000000019249, 0.000000000000000000 ) ) ;
#73941=CARTESIAN_POINT ( 'NONE',  ( 86.75754961941542831, -5.000000000000000888, 6.123233995736779101E-16 ) ) ;
#73942=DIRECTION ( 'NONE',  ( 0.000000000000000000, 0.000000000000000000, 1.000000000000000000 ) ) ;
#73943=ORIENTED_EDGE ( 'NONE', *, *, #71469, .F. ) ;
#73975=DIRECTION ( 'NONE',  ( 0.000000000000000000, -1.000000000000000000, 0.000000000000000000 ) ) ;
#73980=DIRECTION ( 'NONE',  ( 0.000000000000000000, 0.000000000000000000, -1.000000000000000000 ) ) ;
#74033=DIRECTION ( 'NONE',  ( -1.000000000000000000, -1.224606353822377258E-16, -0.000000000000000000 ) ) ;
#74056=DIRECTION ( 'NONE',  ( 0.000000000000000000, 0.000000000000000000, 1.000000000000000000 ) ) ;
#74094=DIRECTION ( 'NONE',  ( -1.000000000000000000, -0.000000000000000000, -0.000000000000000000 ) ) ;
#74111=CARTESIAN_POINT ( 'NONE',  ( 0.1317522424410006998, 1.959574484677833794, 7.999999999999998224 ) ) ;
#74169=DIRECTION ( 'NONE',  ( -0.5735764363510459374, -0.8191520442889919096, 0.000000000000000000 ) ) ;
#74219=CIRCLE ( 'NONE', #82855, 5.000000000000011546 ) ;
#74269=DIRECTION ( 'NONE',  ( -1.000000000000000000, -1.224606353822377258E-16, -0.000000000000000000 ) ) ;
#74300=EDGE_CURVE ( 'NONE', #32770, #2944, #84719, .T. ) ;
#74308=CARTESIAN_POINT ( 'NONE',  ( 0.000000000000000000, 6.123233995736767268E-16, -5.000000000000000888 ) ) ;
#74318=CARTESIAN_POINT ( 'NONE',  ( 104.0908829527487711, 6.123233995736568081E-16, -5.000000000000011546 ) ) ;
#74343=ORIENTED_EDGE ( 'NONE', *, *, #85309, .T. ) ;
#74416=DIRECTION ( 'NONE',  ( -1.000000000000000000, -1.224606353822377258E-16, -0.000000000000000000 ) ) ;
#74466=VERTEX_POINT ( 'NONE', #14735 ) ;
#74467=ORIENTED_EDGE ( 'NONE', *, *, #5337, .F. ) ;
#74476=CARTESIAN_POINT ( 'NONE',  ( 98.31310517497099966, 6.123233995736568081E-16, -5.000000000000011546 ) ) ;
#74477=CARTESIAN_POINT ( 'NONE',  ( 95.42421628608209971, 1.030564683017419500E-14, 0.000000000000000000 ) ) ;
#74534=ORIENTED_EDGE ( 'NONE', *, *, #48102, .F. ) ;
#74549=ORIENTED_EDGE ( 'NONE', *, *, #24497, .F. ) ;
#74567=LINE ( 'NONE', #96741, #65104 ) ;
#74572=LINE ( 'NONE', #100981, #51705 ) ;
#74576=VERTEX_POINT ( 'NONE', #76432 ) ;
#74598=CONICAL_SURFACE ( 'NONE', #57345, 5.000000000000010658, 0.9599310885968697082 ) ;
#74621=DIRECTION ( 'NONE',  ( 0.000000000000000000, -1.000000000000000000, 0.000000000000000000 ) ) ;
#74622=CIRCLE ( 'NONE', #33553, 8.000000000000000000 ) ;
#74631=( GEOMETRIC_REPRESENTATION_CONTEXT ( 3 ) GLOBAL_UNCERTAINTY_ASSIGNED_CONTEXT ( ( #48886 ) ) GLOBAL_UNIT_ASSIGNED_CONTEXT ( ( #114, #24987, #36814 ) ) REPRESENTATION_CONTEXT ( 'NONE', 'WORKASPACE' ) );
#74636=DIRECTION ( 'NONE',  ( -1.000000000000000000, -1.224606353822377258E-16, -0.000000000000000000 ) ) ;
#74667=VERTEX_POINT ( 'NONE', #17162 ) ;
#74740=AXIS2_PLACEMENT_3D ( 'NONE', #54830, #89347, #103920 ) ;
#74749=ORIENTED_EDGE ( 'NONE', *, *, #106198, .T. ) ;
#74790=CARTESIAN_POINT ( 'NONE',  ( 82.70911704725124025, -2.002967142162725287E-29, 5.000000000000011546 ) ) ;
#74821=DIRECTION ( 'NONE',  ( 0.000000000000000000, -1.000000000000000000, 0.000000000000000000 ) ) ;
#74823=AXIS2_PLACEMENT_3D ( 'NONE', #91781, #32501, #73980 ) ;
#74838=DIRECTION ( 'NONE',  ( 0.000000000000000000, 0.000000000000000000, -1.000000000000000000 ) ) ;
#74883=DIRECTION ( 'NONE',  ( 1.000000000000000000, 1.224606353822377258E-16, 0.000000000000000000 ) ) ;
#74892=CONICAL_SURFACE ( 'NONE', #21592, 4.172000000000009479, 0.9599310885968813656 ) ;
#74949=DIRECTION ( 'NONE',  ( -1.000000000000000000, -0.000000000000000000, -0.000000000000000000 ) ) ;
#74964=CONICAL_SURFACE ( 'NONE', #26845, 4.172000000000009479, 0.9599310885968813656 ) ;
#74976=EDGE_LOOP ( 'NONE', ( #67123, #88450, #37559, #71092, #26931 ) ) ;
#75028=CARTESIAN_POINT ( 'NONE',  ( 0.000000000000000000, 0.000000000000000000, 5.000000000000000888 ) ) ;
#75060=EDGE_CURVE ( 'NONE', #13325, #23629, #95139, .T. ) ;
#75067=DIRECTION ( 'NONE',  ( 0.000000000000000000, -1.000000000000000000, 0.000000000000000000 ) ) ;
#75069=DIRECTION ( 'NONE',  ( -1.000000000000000000, -0.000000000000000000, 0.000000000000000000 ) ) ;
#75084=ORIENTED_EDGE ( 'NONE', *, *, #79774, .T. ) ;
#75085=( NAMED_UNIT ( * ) SI_UNIT ( $, .STERADIAN. ) SOLID_ANGLE_UNIT ( ) );
#75125=EDGE_CURVE ( 'NONE', #77127, #11414, #72590, .T. ) ;
#75128=AXIS2_PLACEMENT_3D ( 'NONE', #35727, #101490, #86390 ) ;
#75149=CIRCLE ( 'NONE', #61407, 5.000000000000011546 ) ;
#75174=CARTESIAN_POINT ( 'NONE',  ( 99.17777777777777715, 4.172000000000019249, 5.109226446042768454E-16 ) ) ;
#75184=ORIENTED_EDGE ( 'NONE', *, *, #84683, .T. ) ;
#75264=AXIS2_PLACEMENT_3D ( 'NONE', #79392, #102072, #85924 ) ;
#75272=ORIENTED_EDGE ( 'NONE', *, *, #85701, .F. ) ;
#75273=CARTESIAN_POINT ( 'NONE',  ( 80.40000000000000568, -4.171999999999998820, 0.000000000000000000 ) ) ;
#75328=DIRECTION ( 'NONE',  ( -1.000000000000000000, -1.224606353822377258E-16, -0.000000000000000000 ) ) ;
#75342=EDGE_CURVE ( 'NONE', #64079, #59238, #93577, .T. ) ;
#75356=CIRCLE ( 'NONE', #101163, 5.000000000000011546 ) ;
#75370=CIRCLE ( 'NONE', #9929, 5.000000000000011546 ) ;
#75394=FACE_OUTER_BOUND ( 'NONE', #7495, .T. ) ;
#75478=CIRCLE ( 'NONE', #8338, 5.000000000000010658 ) ;
#75543=DIRECTION ( 'NONE',  ( -1.000000000000000000, -1.224606353822377258E-16, -0.000000000000000000 ) ) ;
#75544=EDGE_CURVE ( 'NONE', #9203, #37220, #34802, .T. ) ;
#75575=DIRECTION ( 'NONE',  ( 1.000000000000000000, 0.000000000000000000, 0.000000000000000000 ) ) ;
#75586=ORIENTED_EDGE ( 'NONE', *, *, #33515, .T. ) ;
#75603=CARTESIAN_POINT ( 'NONE',  ( 82.42421628608209971, -5.000000000000000000, 6.123233995736778115E-16 ) ) ;
#75624=CARTESIAN_POINT ( 'NONE',  ( 84.73333333333332007, 4.172000000000019249, 0.000000000000000000 ) ) ;
#75636=DIRECTION ( 'NONE',  ( 0.000000000000000000, -1.000000000000000000, 0.000000000000000000 ) ) ;
#75653=DIRECTION ( 'NONE',  ( 0.000000000000000000, -1.000000000000000000, 0.000000000000000000 ) ) ;
#75712=ORIENTED_EDGE ( 'NONE', *, *, #45550, .T. ) ;
#75763=VECTOR ( 'NONE', #68222, 1000.000000000000000 ) ;
#75789=CIRCLE ( 'NONE', #68895, 5.000000000000000888 ) ;
#75851=DIRECTION ( 'NONE',  ( 0.000000000000000000, -1.000000000000000000, 0.000000000000000000 ) ) ;
#75861=DIRECTION ( 'NONE',  ( -0.5735764363510461594, 0.8191520442889916875, 1.003171929053524870E-16 ) ) ;
#75865=ORIENTED_EDGE ( 'NONE', *, *, #77098, .T. ) ;
#75876=DIRECTION ( 'NONE',  ( -1.000000000000000000, -0.000000000000000000, -0.000000000000000000 ) ) ;
#75880=AXIS2_PLACEMENT_3D ( 'NONE', #72107, #105014, #23053 ) ;
#75885=DIRECTION ( 'NONE',  ( -1.000000000000000000, -1.224606353822377258E-16, -0.000000000000000000 ) ) ;
#75891=FACE_OUTER_BOUND ( 'NONE', #45153, .T. ) ;
#75914=LINE ( 'NONE', #67307, #38104 ) ;
#75920=DIRECTION ( 'NONE',  ( 0.000000000000000000, 0.000000000000000000, 1.000000000000000000 ) ) ;
#75948=VERTEX_POINT ( 'NONE', #13564 ) ;
#75958=AXIS2_PLACEMENT_3D ( 'NONE', #46489, #69191, #61639 ) ;
#75966=CIRCLE ( 'NONE', #51864, 5.000000000000011546 ) ;
#75991=ORIENTED_EDGE ( 'NONE', *, *, #3341, .F. ) ;
#76014=AXIS2_PLACEMENT_3D ( 'NONE', #88379, #63580, #97495 ) ;
#76044=LINE ( 'NONE', #10250, #61383 ) ;
#76047=ORIENTED_EDGE ( 'NONE', *, *, #60617, .F. ) ;
#76118=EDGE_LOOP ( 'NONE', ( #35398, #102796, #29431, #38351, #58500 ) ) ;
#76143=ORIENTED_EDGE ( 'NONE', *, *, #3202, .F. ) ;
#76180=ORIENTED_EDGE ( 'NONE', *, *, #5735, .T. ) ;
#76241=EDGE_CURVE ( 'NONE', #33098, #39859, #75478, .T. ) ;
#76272=ORIENTED_EDGE ( 'NONE', *, *, #23809, .F. ) ;
#76298=CARTESIAN_POINT ( 'NONE',  ( 0.000000000000000000, 6.123233995736767268E-16, -5.000000000000000888 ) ) ;
#76325=CARTESIAN_POINT ( 'NONE',  ( 99.17777777777777715, -4.171999999999998820, 5.616230220889773285E-16 ) ) ;
#76387=ORIENTED_EDGE ( 'NONE', *, *, #10963, .F. ) ;
#76405=CARTESIAN_POINT ( 'NONE',  ( 99.17777777777777715, 1.023464760207051730E-14, 0.000000000000000000 ) ) ;
#76411=EDGE_LOOP ( 'NONE', ( #14580, #50498, #67780 ) ) ;
#76417=DIRECTION ( 'NONE',  ( 0.000000000000000000, 0.000000000000000000, 1.000000000000000000 ) ) ;
#76421=DIRECTION ( 'NONE',  ( -1.000000000000000000, -1.224606353822377258E-16, -0.000000000000000000 ) ) ;
#76432=CARTESIAN_POINT ( 'NONE',  ( 104.3757837139179117, -5.000000000000000000, 0.000000000000000000 ) ) ;
#76435=DIRECTION ( 'NONE',  ( -1.000000000000000000, -0.000000000000000000, -0.000000000000000000 ) ) ;
#76457=ORIENTED_EDGE ( 'NONE', *, *, #82938, .T. ) ;
#76459=ADVANCED_FACE ( 'NONE', ( #15970 ), #41834, .T. ) ;
#76462=ORIENTED_EDGE ( 'NONE', *, *, #50059, .F. ) ;
#76468=VERTEX_POINT ( 'NONE', #9454 ) ;
#76580=VERTEX_POINT ( 'NONE', #58923 ) ;
#76583=CARTESIAN_POINT ( 'NONE',  ( 84.73333333333332007, 1.023464760207051730E-14, 0.000000000000000000 ) ) ;
#76585=AXIS2_PLACEMENT_3D ( 'NONE', #1645, #17335, #41061 ) ;
#76604=ORIENTED_EDGE ( 'NONE', *, *, #54631, .F. ) ;
#76608=CARTESIAN_POINT ( 'NONE',  ( 0.01688885742776732868, 7.321065037175427115, 3.319543390096037605 ) ) ;
#76611=DIRECTION ( 'NONE',  ( -1.000000000000000000, -1.224606353822377258E-16, -0.000000000000000000 ) ) ;
#76616=ORIENTED_EDGE ( 'NONE', *, *, #47791, .T. ) ;
#76618=VERTEX_POINT ( 'NONE', #40072 ) ;
#76641=DIRECTION ( 'NONE',  ( 0.000000000000000000, -1.000000000000000000, 0.000000000000000000 ) ) ;
#76685=DIRECTION ( 'NONE',  ( 0.000000000000000000, 1.000000000000000000, 0.000000000000000000 ) ) ;
#76703=ORIENTED_EDGE ( 'NONE', *, *, #18279, .T. ) ;
#76725=DIRECTION ( 'NONE',  ( 1.000000000000000000, 1.224606353822377258E-16, 0.000000000000000000 ) ) ;
#76804=EDGE_CURVE ( 'NONE', #57410, #49495, #92330, .T. ) ;
#76810=EDGE_CURVE ( 'NONE', #64587, #6669, #10111, .T. ) ;
#76816=EDGE_CURVE ( 'NONE', #55657, #17355, #73854, .T. ) ;
#76820=CONICAL_SURFACE ( 'NONE', #44111, 5.000000000000010658, 0.9599310885968697082 ) ;
#76826=AXIS2_PLACEMENT_3D ( 'NONE', #38865, #64210, #71731 ) ;
#76901=PRODUCT_DEFINITION_CONTEXT ( 'detailed design', #45249, 'design' ) ;
#76923=CONICAL_SURFACE ( 'NONE', #70071, 4.172000000000009479, 0.9599310885968813656 ) ;
#76943=CIRCLE ( 'NONE', #82087, 5.000000000000010658 ) ;
#76998=DIRECTION ( 'NONE',  ( -1.000000000000000000, -1.224606353822377258E-16, -0.000000000000000000 ) ) ;
#77003=EDGE_LOOP ( 'NONE', ( #49425, #13451, #44237 ) ) ;
#77024=CARTESIAN_POINT ( 'NONE',  ( 97.15356149169568312, 1.016364837396684119E-14, 0.000000000000000000 ) ) ;
#77040=DIRECTION ( 'NONE',  ( -1.000000000000000000, -1.224606353822377258E-16, -0.000000000000000000 ) ) ;
#77081=DIRECTION ( 'NONE',  ( -1.000000000000000000, -1.224606353822377258E-16, -0.000000000000000000 ) ) ;
#77098=EDGE_CURVE ( 'NONE', #16922, #21366, #53316, .T. ) ;
#77124=CARTESIAN_POINT ( 'NONE',  ( 0.000000000000000000, 0.000000000000000000, 0.000000000000000000 ) ) ;
#77127=VERTEX_POINT ( 'NONE', #52813 ) ;
#77148=CARTESIAN_POINT ( 'NONE',  ( 80.40000000000000568, 1.023464760207051730E-14, 0.000000000000000000 ) ) ;
#77174=CARTESIAN_POINT ( 'NONE',  ( 93.97977184163765685, -5.000000000000000888, 6.123233995736779101E-16 ) ) ;
#77180=CYLINDRICAL_SURFACE ( 'NONE', #55503, 5.000000000000000888 ) ;
#77213=FACE_OUTER_BOUND ( 'NONE', #106037, .T. ) ;
#77225=VERTEX_POINT ( 'NONE', #91692 ) ;
#77229=CARTESIAN_POINT ( 'NONE',  ( 5.799999999999999822, 6.928203230275505220, -4.000000000000006217 ) ) ;
#77300=DIRECTION ( 'NONE',  ( 0.000000000000000000, -1.000000000000000000, 0.000000000000000000 ) ) ;
#77323=DIRECTION ( 'NONE',  ( -1.000000000000000000, -1.224606353822377258E-16, -0.000000000000000000 ) ) ;
#77326=CYLINDRICAL_SURFACE ( 'NONE', #56901, 5.000000000000000888 ) ;
#77358=ORIENTED_EDGE ( 'NONE', *, *, #90893, .F. ) ;
#77377=ORIENTED_EDGE ( 'NONE', *, *, #96603, .T. ) ;
#77410=ORIENTED_EDGE ( 'NONE', *, *, #76241, .T. ) ;
#77430=DIRECTION ( 'NONE',  ( 0.000000000000000000, 0.000000000000000000, 1.000000000000000000 ) ) ;
#77432=EDGE_LOOP ( 'NONE', ( #10667, #94911, #24686, #66906, #14124 ) ) ;
#77444=MECHANICAL_DESIGN_GEOMETRIC_PRESENTATION_REPRESENTATION('',(#60224),#63673);
#77463=DIRECTION ( 'NONE',  ( 0.000000000000000000, -1.000000000000000000, 0.000000000000000000 ) ) ;
#77519=EDGE_CURVE ( 'NONE', #54088, #10153, #86055, .T. ) ;
#77523=DIRECTION ( 'NONE',  ( 0.000000000000000000, 0.000000000000000000, 1.000000000000000000 ) ) ;
#77541=EDGE_CURVE ( 'NONE', #93631, #44057, #39546, .T. ) ;
#77624=FACE_OUTER_BOUND ( 'NONE', #33344, .T. ) ;
#77725=VERTEX_POINT ( 'NONE', #85464 ) ;
#77806=ORIENTED_EDGE ( 'NONE', *, *, #2365, .T. ) ;
#77810=AXIS2_PLACEMENT_3D ( 'NONE', #1101, #19501, #9739 ) ;
#77816=DIRECTION ( 'NONE',  ( -1.000000000000000000, -0.000000000000000000, -0.000000000000000000 ) ) ;
#77927=FACE_OUTER_BOUND ( 'NONE', #68820, .T. ) ;
#77939=ORIENTED_EDGE ( 'NONE', *, *, #83334, .F. ) ;
#77958=CYLINDRICAL_SURFACE ( 'NONE', #97793, 5.000000000000000888 ) ;
#77996=ORIENTED_EDGE ( 'NONE', *, *, #74300, .T. ) ;
#78017=CARTESIAN_POINT ( 'NONE',  ( 0.000000000000000000, 0.000000000000000000, 5.000000000000000888 ) ) ;
#78038=VECTOR ( 'NONE', #51453, 999.9999999999998863 ) ;
#78057=EDGE_CURVE ( 'NONE', #70018, #24844, #22390, .T. ) ;
#78072=LINE ( 'NONE', #4187, #106227 ) ;
#78078=ORIENTED_EDGE ( 'NONE', *, *, #69088, .T. ) ;
#78169=DIRECTION ( 'NONE',  ( -1.000000000000000000, -1.224606353822377258E-16, -0.000000000000000000 ) ) ;
#78215=CARTESIAN_POINT ( 'NONE',  ( 6.800000000000000711, 0.000000000000000000, 0.000000000000000000 ) ) ;
#78236=CARTESIAN_POINT ( 'NONE',  ( 84.15356149169568312, 6.123233995736582872E-16, -5.000000000000011546 ) ) ;
#78248=ORIENTED_EDGE ( 'NONE', *, *, #37501, .F. ) ;
#78281=FACE_OUTER_BOUND ( 'NONE', #45638, .T. ) ;
#78304=EDGE_CURVE ( 'NONE', #79234, #82760, #70629, .T. ) ;
#78305=EDGE_LOOP ( 'NONE', ( #86822, #95252, #12296 ) ) ;
#78312=CARTESIAN_POINT ( 'NONE',  ( 93.97977184163765685, 5.000000000000021316, 0.000000000000000000 ) ) ;
#78324=ORIENTED_EDGE ( 'NONE', *, *, #53888, .F. ) ;
#78426=EDGE_LOOP ( 'NONE', ( #13057, #7250, #55743, #53566, #24508 ) ) ;
#78443=DIRECTION ( 'NONE',  ( 0.000000000000000000, -0.5000000000000008882, -0.8660254037844381525 ) ) ;
#78449=CARTESIAN_POINT ( 'NONE',  ( 93.39999999999999147, 1.023464760207051730E-14, 0.000000000000000000 ) ) ;
#78456=LINE ( 'NONE', #87100, #16089 ) ;
#78511=VERTEX_POINT ( 'NONE', #61474 ) ;
#78585=FACE_OUTER_BOUND ( 'NONE', #94123, .T. ) ;
#78592=CARTESIAN_POINT ( 'NONE',  ( 99.17777777777777715, 4.172000000000019249, 0.000000000000000000 ) ) ;
#78662=CARTESIAN_POINT ( 'NONE',  ( 96.28888888888889142, -4.171999999999998820, 5.616230220889773285E-16 ) ) ;
#78783=CARTESIAN_POINT ( 'NONE',  ( 94.26467260280679739, 1.016364837396684119E-14, 0.000000000000000000 ) ) ;
#78793=ADVANCED_FACE ( 'NONE', ( #98587 ), #22542, .T. ) ;
#78820=CIRCLE ( 'NONE', #32350, 5.000000000000011546 ) ;
#78827=DIRECTION ( 'NONE',  ( -1.000000000000000000, -1.224606353822377258E-16, -0.000000000000000000 ) ) ;
#78834=AXIS2_PLACEMENT_3D ( 'NONE', #32962, #25411, #65832 ) ;
#78876=CONICAL_SURFACE ( 'NONE', #6570, 4.172000000000009479, 0.9599310885968813656 ) ;
#78889=EDGE_CURVE ( 'NONE', #32770, #70163, #75914, .T. ) ;
#78934=AXIS2_PLACEMENT_3D ( 'NONE', #96033, #29734, #46417 ) ;
#78984=ORIENTED_EDGE ( 'NONE', *, *, #592, .F. ) ;
#79035=ORIENTED_EDGE ( 'NONE', *, *, #39083, .F. ) ;
#79039=CARTESIAN_POINT ( 'NONE',  ( 93.39999999999999147, 1.023464760207051730E-14, 0.000000000000000000 ) ) ;
#79045=AXIS2_PLACEMENT_3D ( 'NONE', #102722, #28885, #95690 ) ;
#79051=DIRECTION ( 'NONE',  ( 0.5735764363510554853, 0.8191520442889852482, 0.000000000000000000 ) ) ;
#79081=CARTESIAN_POINT ( 'NONE',  ( 101.2019940638598854, -2.002967142162725287E-29, 5.000000000000011546 ) ) ;
#79104=VECTOR ( 'NONE', #29844, 1000.000000000000000 ) ;
#79108=CARTESIAN_POINT ( 'NONE',  ( 93.97977184163765685, -2.002967142162725287E-29, 5.000000000000011546 ) ) ;
#79151=AXIS2_PLACEMENT_3D ( 'NONE', #17915, #84760, #43761 ) ;
#79169=ORIENTED_EDGE ( 'NONE', *, *, #10963, .T. ) ;
#79234=VERTEX_POINT ( 'NONE', #4961 ) ;
#79237=DIRECTION ( 'NONE',  ( 0.5735764363510557073, -0.8191520442889850262, 1.003171929053516612E-16 ) ) ;
#79318=CONICAL_SURFACE ( 'NONE', #32840, 5.000000000000010658, 0.9599310885968697082 ) ;
#79344=DIRECTION ( 'NONE',  ( 0.000000000000000000, -1.000000000000000000, 0.000000000000000000 ) ) ;
#79346=CYLINDRICAL_SURFACE ( 'NONE', #19927, 5.000000000000000888 ) ;
#79367=ORIENTED_EDGE ( 'NONE', *, *, #30121, .T. ) ;
#79378=CARTESIAN_POINT ( 'NONE',  ( 0.4969600502617488313, -8.860760056385739603, -0.6527133886630315240 ) ) ;
#79384=AXIS2_PLACEMENT_3D ( 'NONE', #23424, #45569, #78443 ) ;
#79392=CARTESIAN_POINT ( 'NONE',  ( 84.73333333333332007, 1.023464760207051730E-14, 0.000000000000000000 ) ) ;
#79424=VECTOR ( 'NONE', #49934, 1000.000000000000000 ) ;
#79476=EDGE_CURVE ( 'NONE', #17856, #15530, #48358, .T. ) ;
#79503=CARTESIAN_POINT ( 'NONE',  ( 5.086432848262074522E-16, 0.3912769055735421664, -8.000000000000001776 ) ) ;
#79569=ORIENTED_EDGE ( 'NONE', *, *, #97741, .F. ) ;
#79571=LINE ( 'NONE', #5684, #58427 ) ;
#79575=DIRECTION ( 'NONE',  ( -0.7071067811865390240, 0.000000000000000000, 0.7071067811865561215 ) ) ;
#79587=CARTESIAN_POINT ( 'NONE',  ( 91.09088295274877112, 1.030564683017419500E-14, 0.000000000000000000 ) ) ;
#79695=CARTESIAN_POINT ( 'NONE',  ( 0.3157512944461039472, -3.097794232780329171, -8.000000000000000000 ) ) ;
#79701=ADVANCED_FACE ( 'NONE', ( #54406 ), #82865, .T. ) ;
#79726=ADVANCED_FACE ( 'NONE', ( #104572 ), #46682, .T. ) ;
#79731=DIRECTION ( 'NONE',  ( -1.000000000000000000, -1.224606353822377258E-16, -0.000000000000000000 ) ) ;
#79739=PLANE ( 'NONE',  #76014 ) ;
#79755=CARTESIAN_POINT ( 'NONE',  ( 80.97977184163765685, 6.123233995736568081E-16, -5.000000000000011546 ) ) ;
#79774=EDGE_CURVE ( 'NONE', #105973, #39859, #81872, .T. ) ;
#79797=CIRCLE ( 'NONE', #95367, 5.000000000000010658 ) ;
#79821=DIRECTION ( 'NONE',  ( 0.000000000000000000, 0.000000000000000000, 1.000000000000000000 ) ) ;
#79822=DIRECTION ( 'NONE',  ( -1.000000000000000000, -1.224606353822377258E-16, -0.000000000000000000 ) ) ;
#79844=CARTESIAN_POINT ( 'NONE',  ( 82.42421628608209971, -5.000000000000000888, 6.123233995736779101E-16 ) ) ;
#79871=( GEOMETRIC_REPRESENTATION_CONTEXT ( 3 ) GLOBAL_UNCERTAINTY_ASSIGNED_CONTEXT ( ( #41344 ) ) GLOBAL_UNIT_ASSIGNED_CONTEXT ( ( #34687, #8770, #75085 ) ) REPRESENTATION_CONTEXT ( 'NONE', 'WORKASPACE' ) );
#79883=ORIENTED_EDGE ( 'NONE', *, *, #85485, .F. ) ;
#79909=ADVANCED_FACE ( 'NONE', ( #75394 ), #84645, .T. ) ;
#79975=CARTESIAN_POINT ( 'NONE',  ( 102.9313392694734688, 6.123233995736582872E-16, -5.000000000000011546 ) ) ;
#79982=CARTESIAN_POINT ( 'NONE',  ( 5.799999999999999822, 4.618802153517003184, -8.000000000000000000 ) ) ;
#80000=ORIENTED_EDGE ( 'NONE', *, *, #25553, .T. ) ;
#80003=LINE ( 'NONE', #32014, #52666 ) ;
#80031=DIRECTION ( 'NONE',  ( 0.000000000000000000, -1.000000000000000000, 0.000000000000000000 ) ) ;
#80043=DIRECTION ( 'NONE',  ( 0.000000000000000000, -1.000000000000000000, 0.000000000000000000 ) ) ;
#80063=ORIENTED_EDGE ( 'NONE', *, *, #102731, .F. ) ;
#80074=DIRECTION ( 'NONE',  ( 0.000000000000000000, -1.000000000000000000, 0.000000000000000000 ) ) ;
#80082=EDGE_CURVE ( 'NONE', #63169, #72949, #13837, .T. ) ;
#80091=ORIENTED_EDGE ( 'NONE', *, *, #103398, .T. ) ;
#80101=ORIENTED_EDGE ( 'NONE', *, *, #33515, .F. ) ;
#80134=AXIS2_PLACEMENT_3D ( 'NONE', #89788, #81661, #63412 ) ;
#80139=CARTESIAN_POINT ( 'NONE',  ( 85.31310517497098544, -5.000000000000000000, 6.123233995736778115E-16 ) ) ;
#80161=DIRECTION ( 'NONE',  ( 0.000000000000000000, 0.000000000000000000, 1.000000000000000000 ) ) ;
#80172=EDGE_CURVE ( 'NONE', #24268, #55179, #65463, .T. ) ;
#80255=EDGE_LOOP ( 'NONE', ( #88277, #68981, #7268, #83408, #68745 ) ) ;
#80260=VERTEX_POINT ( 'NONE', #76325 ) ;
#80304=ORIENTED_EDGE ( 'NONE', *, *, #67138, .F. ) ;
#80328=EDGE_LOOP ( 'NONE', ( #25549, #25991, #97203, #38882, #43462 ) ) ;
#80345=ORIENTED_EDGE ( 'NONE', *, *, #65477, .T. ) ;
#80412=DIRECTION ( 'NONE',  ( 0.000000000000000000, -1.000000000000000000, 0.000000000000000000 ) ) ;
#80422=CARTESIAN_POINT ( 'NONE',  ( 93.39999999999999147, 4.172000000000019249, 0.000000000000000000 ) ) ;
#80494=CARTESIAN_POINT ( 'NONE',  ( 93.97977184163765685, 1.030564683017419500E-14, 0.000000000000000000 ) ) ;
#80509=ORIENTED_EDGE ( 'NONE', *, *, #73191, .T. ) ;
#80527=ORIENTED_EDGE ( 'NONE', *, *, #29003, .T. ) ;
#80559=CARTESIAN_POINT ( 'NONE',  ( 6.400000000000000355, -9.237604307034013473, 7.924929828396943928E-16 ) ) ;
#80626=ORIENTED_EDGE ( 'NONE', *, *, #105076, .T. ) ;
#80628=EDGE_LOOP ( 'NONE', ( #105965, #54338, #60201, #39948, #7283 ) ) ;
#80667=DIRECTION ( 'NONE',  ( 0.000000000000000000, -1.000000000000000000, 0.000000000000000000 ) ) ;
#80679=EDGE_CURVE ( 'NONE', #49541, #54088, #69388, .T. ) ;
#80686=CIRCLE ( 'NONE', #103119, 5.000000000000011546 ) ;
#80705=ORIENTED_EDGE ( 'NONE', *, *, #3134, .F. ) ;
#80798=ORIENTED_EDGE ( 'NONE', *, *, #52759, .F. ) ;
#80820=ORIENTED_EDGE ( 'NONE', *, *, #27054, .T. ) ;
#80855=LINE ( 'NONE', #32873, #102863 ) ;
#80880=CARTESIAN_POINT ( 'NONE',  ( 98.31310517497099966, 1.030564683017419500E-14, 0.000000000000000000 ) ) ;
#80982=CARTESIAN_POINT ( 'NONE',  ( 0.4964154566687934422, 8.859816792613651515, -0.6543471694412386075 ) ) ;
#80989=ORIENTED_EDGE ( 'NONE', *, *, #43514, .F. ) ;
#81015=DIRECTION ( 'NONE',  ( 0.5735764363510554853, 0.8191520442889852482, 0.000000000000000000 ) ) ;
#81037=CONICAL_SURFACE ( 'NONE', #29516, 4.172000000000009479, 0.9599310885968813656 ) ;
#81040=EDGE_CURVE ( 'NONE', #55434, #5546, #87956, .T. ) ;
#81192=EDGE_CURVE ( 'NONE', #55214, #67654, #23915, .T. ) ;
#81226=CYLINDRICAL_SURFACE ( 'NONE', #63978, 5.000000000000000888 ) ;
#81227=EDGE_CURVE ( 'NONE', #8974, #49616, #74219, .T. ) ;
#81228=AXIS2_PLACEMENT_3D ( 'NONE', #42335, #34283, #58538 ) ;
#81246=ORIENTED_EDGE ( 'NONE', *, *, #17436, .T. ) ;
#81314=ORIENTED_EDGE ( 'NONE', *, *, #25553, .F. ) ;
#81324=ADVANCED_FACE ( 'NONE', ( #102009 ), #70771, .F. ) ;
#81336=PLANE ( 'NONE',  #44272 ) ;
#81340=EDGE_LOOP ( 'NONE', ( #72460, #16150, #36588, #3956, #19196 ) ) ;
#81347=ORIENTED_EDGE ( 'NONE', *, *, #5226, .T. ) ;
#81442=AXIS2_PLACEMENT_3D ( 'NONE', #67821, #57574, #50546 ) ;
#81443=DIRECTION ( 'NONE',  ( 0.000000000000000000, 0.000000000000000000, 1.000000000000000000 ) ) ;
#81463=FACE_OUTER_BOUND ( 'NONE', #8781, .T. ) ;
#81496=ORIENTED_EDGE ( 'NONE', *, *, #67340, .T. ) ;
#81502=AXIS2_PLACEMENT_3D ( 'NONE', #25752, #12556, #67758 ) ;
#81528=CARTESIAN_POINT ( 'NONE',  ( 92.53532739719321398, 5.000000000000021316, 0.000000000000000000 ) ) ;
#81548=DIRECTION ( 'NONE',  ( -1.000000000000000000, -1.224606353822377258E-16, -0.000000000000000000 ) ) ;
#81555=FACE_OUTER_BOUND ( 'NONE', #59700, .T. ) ;
#81595=CARTESIAN_POINT ( 'NONE',  ( 92.53532739719321398, 1.030564683017419500E-14, 0.000000000000000000 ) ) ;
#81641=CARTESIAN_POINT ( 'NONE',  ( 0.000000000000000000, 0.000000000000000000, 0.000000000000000000 ) ) ;
#81649=AXIS2_PLACEMENT_3D ( 'NONE', #41101, #65901, #99312 ) ;
#81659=CARTESIAN_POINT ( 'NONE',  ( 89.93133926947346879, 1.016364837396684119E-14, 0.000000000000000000 ) ) ;
#81661=DIRECTION ( 'NONE',  ( -1.000000000000000000, -1.224606353822377258E-16, -0.000000000000000000 ) ) ;
#81664=ADVANCED_FACE ( 'NONE', ( #8089 ), #20936, .T. ) ;
#81750=FACE_OUTER_BOUND ( 'NONE', #46684, .T. ) ;
#81758=CARTESIAN_POINT ( 'NONE',  ( 0.08224679563970911655, -6.145890662064644516, 5.355005115540896199 ) ) ;
#81761=LINE ( 'NONE', #89360, #63222 ) ;
#81786=ORIENTED_EDGE ( 'NONE', *, *, #106008, .F. ) ;
#81833=EDGE_CURVE ( 'NONE', #44644, #58313, #94882, .T. ) ;
#81836=DIRECTION ( 'NONE',  ( 0.000000000000000000, -1.000000000000000000, 0.000000000000000000 ) ) ;
#81866=VECTOR ( 'NONE', #103250, 999.9999999999998863 ) ;
#81872=LINE ( 'NONE', #7998, #24379 ) ;
#81879=VECTOR ( 'NONE', #10577, 1000.000000000000000 ) ;
#81892=AXIS2_PLACEMENT_3D ( 'NONE', #62435, #75543, #13319 ) ;
#81919=EDGE_CURVE ( 'NONE', #10644, #8974, #67467, .T. ) ;
#81964=CARTESIAN_POINT ( 'NONE',  ( 84.73333333333332007, 1.023464760207051730E-14, 0.000000000000000000 ) ) ;
#81970=CARTESIAN_POINT ( 'NONE',  ( 91.95555555555554861, 4.172000000000019249, 5.109226446042768454E-16 ) ) ;
#81995=DIRECTION ( 'NONE',  ( 0.5735764363510554853, 0.8191520442889852482, 0.000000000000000000 ) ) ;
#81999=FACE_OUTER_BOUND ( 'NONE', #96211, .T. ) ;
#82024=ORIENTED_EDGE ( 'NONE', *, *, #68947, .T. ) ;
#82027=CIRCLE ( 'NONE', #71717, 4.172000000000009479 ) ;
#82030=ORIENTED_EDGE ( 'NONE', *, *, #36601, .T. ) ;
#82035=DIRECTION ( 'NONE',  ( 0.000000000000000000, -1.000000000000000000, 0.000000000000000000 ) ) ;
#82061=VECTOR ( 'NONE', #35508, 1000.000000000000000 ) ;
#82074=ORIENTED_EDGE ( 'NONE', *, *, #404, .T. ) ;
#82087=AXIS2_PLACEMENT_3D ( 'NONE', #9886, #17480, #91366 ) ;
#82090=AXIS2_PLACEMENT_3D ( 'NONE', #85682, #77040, #44694 ) ;
#82101=CARTESIAN_POINT ( 'NONE',  ( 83.28888888888889142, 1.023464760207051730E-14, 0.000000000000000000 ) ) ;
#82106=ORIENTED_EDGE ( 'NONE', *, *, #33785, .F. ) ;
#82145=ORIENTED_EDGE ( 'NONE', *, *, #49824, .T. ) ;
#82157=VECTOR ( 'NONE', #91763, 1000.000000000000000 ) ;
#82161=ORIENTED_EDGE ( 'NONE', *, *, #88764, .T. ) ;
#82168=ORIENTED_EDGE ( 'NONE', *, *, #73474, .T. ) ;
#82194=VERTEX_POINT ( 'NONE', #99629 ) ;
#82204=DIRECTION ( 'NONE',  ( 0.000000000000000000, -1.000000000000000000, 0.000000000000000000 ) ) ;
#82212=CARTESIAN_POINT ( 'NONE',  ( 98.31310517497099966, 1.030564683017419500E-14, 0.000000000000000000 ) ) ;
#82250=B_SPLINE_CURVE_WITH_KNOTS ( 'NONE', 3,
 ( #57757, #22787, #31415, #65870, #30883, #98749, #105791, #14641 ),
 .UNSPECIFIED., .F., .F.,
 ( 4, 2, 2, 4 ),
 ( 0.004673709593152167857, 0.005837709341827654677, 0.007001709090503141497, 0.009329708587854115137 ),
 .UNSPECIFIED. ) ;
#82268=CARTESIAN_POINT ( 'NONE',  ( 85.31310517497098544, 5.000000000000020428, 0.000000000000000000 ) ) ;
#82311=CARTESIAN_POINT ( 'NONE',  ( 0.7145311798163195283, -4.618802153516994302, 8.000000000000000000 ) ) ;
#82371=DIRECTION ( 'NONE',  ( -1.000000000000000000, -1.224606353822377258E-16, -0.000000000000000000 ) ) ;
#82398=EDGE_CURVE ( 'NONE', #74466, #10334, #50644, .T. ) ;
#82472=DIRECTION ( 'NONE',  ( 0.000000000000000000, -1.000000000000000000, 0.000000000000000000 ) ) ;
#82516=DIRECTION ( 'NONE',  ( 1.000000000000000000, 1.224606353822377258E-16, 0.000000000000000000 ) ) ;
#82520=CIRCLE ( 'NONE', #17086, 8.000000000000000000 ) ;
#82523=CIRCLE ( 'NONE', #89461, 5.000000000000011546 ) ;
#82524=CARTESIAN_POINT ( 'NONE',  ( 88.20199406385988539, 1.030564683017419500E-14, 0.000000000000000000 ) ) ;
#82545=CARTESIAN_POINT ( 'NONE',  ( 92.53532739719321398, 5.000000000000020428, 0.000000000000000000 ) ) ;
#82581=DIRECTION ( 'NONE',  ( -1.000000000000000000, -0.000000000000000000, -0.000000000000000000 ) ) ;
#82618=CIRCLE ( 'NONE', #39598, 5.000000000000010658 ) ;
#82631=EDGE_CURVE ( 'NONE', #104741, #60462, #101941, .T. ) ;
#82694=DIRECTION ( 'NONE',  ( -1.000000000000000000, -1.224606353822377258E-16, -0.000000000000000000 ) ) ;
#82725=DIRECTION ( 'NONE',  ( 0.000000000000000000, -1.000000000000000000, 0.000000000000000000 ) ) ;
#82743=EDGE_CURVE ( 'NONE', #3401, #55657, #83010, .T. ) ;
#82748=CARTESIAN_POINT ( 'NONE',  ( 103.5111111111111057, 4.172000000000019249, 0.000000000000000000 ) ) ;
#82760=VERTEX_POINT ( 'NONE', #77229 ) ;
#82770=CARTESIAN_POINT ( 'NONE',  ( 80.97977184163765685, 1.030564683017419500E-14, 0.000000000000000000 ) ) ;
#82785=ORIENTED_EDGE ( 'NONE', *, *, #24497, .T. ) ;
#82791=ADVANCED_FACE ( 'NONE', ( #53487 ), #93417, .T. ) ;
#82835=ORIENTED_EDGE ( 'NONE', *, *, #11335, .F. ) ;
#82852=VERTEX_POINT ( 'NONE', #85878 ) ;
#82854=AXIS2_PLACEMENT_3D ( 'NONE', #55735, #14756, #97276 ) ;
#82855=AXIS2_PLACEMENT_3D ( 'NONE', #48663, #81548, #92 ) ;
#82856=DIRECTION ( 'NONE',  ( 0.000000000000000000, 0.000000000000000000, -1.000000000000000000 ) ) ;
#82865=CONICAL_SURFACE ( 'NONE', #38171, 4.172000000000009479, 0.9599310885968813656 ) ;
#82875=CIRCLE ( 'NONE', #50147, 5.000000000000011546 ) ;
#82877=ORIENTED_EDGE ( 'NONE', *, *, #89783, .F. ) ;
#82890=DIRECTION ( 'NONE',  ( -1.000000000000000000, -1.224606353822377258E-16, -0.000000000000000000 ) ) ;
#82935=DIRECTION ( 'NONE',  ( 0.000000000000000000, -1.000000000000000000, 0.000000000000000000 ) ) ;
#82938=EDGE_CURVE ( 'NONE', #22959, #6669, #97116, .T. ) ;
#82986=EDGE_CURVE ( 'NONE', #85106, #1566, #2140, .T. ) ;
#83010=CIRCLE ( 'NONE', #24463, 5.000000000000010658 ) ;
#83084=DIRECTION ( 'NONE',  ( 0.000000000000000000, -1.000000000000000000, 0.000000000000000000 ) ) ;
#83110=FACE_OUTER_BOUND ( 'NONE', #41260, .T. ) ;
#83161=AXIS2_PLACEMENT_3D ( 'NONE', #51146, #74883, #50094 ) ;
#83215=CARTESIAN_POINT ( 'NONE',  ( 88.48689482502902592, -5.000000000000000000, 0.000000000000000000 ) ) ;
#83224=CARTESIAN_POINT ( 'NONE',  ( 92.53532739719321398, 1.030564683017419500E-14, 0.000000000000000000 ) ) ;
#83242=DIRECTION ( 'NONE',  ( 0.000000000000000000, 0.4999999999999996114, -0.8660254037844388186 ) ) ;
#83283=ORIENTED_EDGE ( 'NONE', *, *, #16924, .F. ) ;
#83289=ADVANCED_FACE ( 'NONE', ( #32817 ), #17681, .T. ) ;
#83294=EDGE_LOOP ( 'NONE', ( #95214, #51797, #30547, #102233 ) ) ;
#83302=FACE_OUTER_BOUND ( 'NONE', #38308, .T. ) ;
#83318=ORIENTED_EDGE ( 'NONE', *, *, #68349, .T. ) ;
#83334=EDGE_CURVE ( 'NONE', #41772, #49495, #64239, .T. ) ;
#83399=DIRECTION ( 'NONE',  ( 1.000000000000000000, 1.224606353822377258E-16, 0.000000000000000000 ) ) ;
#83408=ORIENTED_EDGE ( 'NONE', *, *, #73816, .F. ) ;
#83413=AXIS2_PLACEMENT_3D ( 'NONE', #58121, #24725, #32284 ) ;
#83430=ORIENTED_EDGE ( 'NONE', *, *, #55043, .T. ) ;
#83473=DIRECTION ( 'NONE',  ( 0.5735764363510554853, 0.8191520442889852482, 0.000000000000000000 ) ) ;
#83477=CARTESIAN_POINT ( 'NONE',  ( 96.86866073052655679, 1.030564683017419500E-14, 0.000000000000000000 ) ) ;
#83484=CARTESIAN_POINT ( 'NONE',  ( 89.06666666666666288, 1.023464760207051730E-14, 0.000000000000000000 ) ) ;
#83493=ADVANCED_FACE ( 'NONE', ( #36029 ), #105563, .T. ) ;
#83507=EDGE_CURVE ( 'NONE', #78511, #72914, #43547, .T. ) ;
#83512=DIRECTION ( 'NONE',  ( -1.000000000000000000, -1.224606353822377258E-16, -0.000000000000000000 ) ) ;
#83532=AXIS2_PLACEMENT_3D ( 'NONE', #37340, #13004, #96074 ) ;
#83534=B_SPLINE_CURVE_WITH_KNOTS ( 'NONE', 3,
 ( #86336, #29188, #76608, #2722, #28641, #43718, #37797, #69078 ),
 .UNSPECIFIED., .F., .F.,
 ( 4, 2, 2, 4 ),
 ( 0.004673709593152147040, 0.005837709341827638197, 0.007001709090503129354, 0.009329708587854111668 ),
 .UNSPECIFIED. ) ;
#83539=ORIENTED_EDGE ( 'NONE', *, *, #59716, .T. ) ;
#83593=CONICAL_SURFACE ( 'NONE', #80134, 4.172000000000009479, 0.9599310885968813656 ) ;
#83594=AXIS2_PLACEMENT_3D ( 'NONE', #7892, #14922, #57502 ) ;
#83596=CONICAL_SURFACE ( 'NONE', #105997, 5.000000000000010658, 0.9599310885968697082 ) ;
#83626=ORIENTED_EDGE ( 'NONE', *, *, #65477, .F. ) ;
#83650=FACE_OUTER_BOUND ( 'NONE', #26255, .T. ) ;
#83659=LINE ( 'NONE', #59, #48257 ) ;
#83677=AXIS2_PLACEMENT_3D ( 'NONE', #38449, #86997, #31430 ) ;
#83704=ORIENTED_EDGE ( 'NONE', *, *, #22824, .T. ) ;
#83712=DIRECTION ( 'NONE',  ( 0.000000000000000000, -1.000000000000000000, 0.000000000000000000 ) ) ;
#83720=CARTESIAN_POINT ( 'NONE',  ( 94.84444444444443434, 1.023464760207051730E-14, 0.000000000000000000 ) ) ;
#83765=CARTESIAN_POINT ( 'NONE',  ( 5.799999999999999822, -4.618802153517009401, -8.000000000000001776 ) ) ;
#83775=CARTESIAN_POINT ( 'NONE',  ( 0.000000000000000000, 0.000000000000000000, 0.000000000000000000 ) ) ;
#83793=CARTESIAN_POINT ( 'NONE',  ( 90.51111111111110574, 1.023464760207051730E-14, 0.000000000000000000 ) ) ;
#83859=CARTESIAN_POINT ( 'NONE',  ( 83.86866073052654258, 1.030564683017419500E-14, 0.000000000000000000 ) ) ;
#83866=CARTESIAN_POINT ( 'NONE',  ( 82.42421628608209971, 5.000000000000021316, 0.000000000000000000 ) ) ;
#83893=ORIENTED_EDGE ( 'NONE', *, *, #30394, .F. ) ;
#83933=CIRCLE ( 'NONE', #18514, 5.000000000000011546 ) ;
#83977=CARTESIAN_POINT ( 'NONE',  ( 89.64643850830432825, 1.030564683017419500E-14, 0.000000000000000000 ) ) ;
#83990=AXIS2_PLACEMENT_3D ( 'NONE', #91848, #42762, #75653 ) ;
#84003=EDGE_CURVE ( 'NONE', #66540, #82760, #32026, .T. ) ;
#84011=CARTESIAN_POINT ( 'NONE',  ( 99.75754961941544252, -5.000000000000000000, 6.123233995736778115E-16 ) ) ;
#84018=CIRCLE ( 'NONE', #94354, 5.000000000000011546 ) ;
#84021=ORIENTED_EDGE ( 'NONE', *, *, #85655, .T. ) ;
#84026=EDGE_CURVE ( 'NONE', #9728, #4234, #25548, .T. ) ;
#84056=AXIS2_PLACEMENT_3D ( 'NONE', #101822, #3135, #86205 ) ;
#84073=LINE ( 'NONE', #10173, #43966 ) ;
#84081=ORIENTED_EDGE ( 'NONE', *, *, #14617, .F. ) ;
#84085=ADVANCED_FACE ( 'NONE', ( #103910 ), #47264, .T. ) ;
#84176=EDGE_CURVE ( 'NONE', #10644, #45933, #78456, .T. ) ;
#84218=AXIS2_PLACEMENT_3D ( 'NONE', #91031, #10611, #9544 ) ;
#84246=CONICAL_SURFACE ( 'NONE', #13548, 4.172000000000009479, 0.9599310885968813656 ) ;
#84264=CARTESIAN_POINT ( 'NONE',  ( 90.51111111111110574, 1.023464760207051730E-14, 0.000000000000000000 ) ) ;
#84265=VECTOR ( 'NONE', #50852, 1000.000000000000000 ) ;
#84285=AXIS2_PLACEMENT_3D ( 'NONE', #94209, #12210, #39168 ) ;
#84356=DIRECTION ( 'NONE',  ( -0.5735764363510461594, 0.8191520442889916875, 1.003171929053524870E-16 ) ) ;
#84411=LINE ( 'NONE', #83866, #9177 ) ;
#84452=DIRECTION ( 'NONE',  ( -1.000000000000000000, -1.224606353822377258E-16, -0.000000000000000000 ) ) ;
#84475=AXIS2_PLACEMENT_3D ( 'NONE', #22895, #47128, #46609 ) ;
#84484=CARTESIAN_POINT ( 'NONE',  ( 6.400000000000000355, 9.237604307034018802, 0.000000000000000000 ) ) ;
#84531=PLANE ( 'NONE',  #84959 ) ;
#84541=EDGE_LOOP ( 'NONE', ( #6282, #91559, #42133, #30141, #28495 ) ) ;
#84609=DIRECTION ( 'NONE',  ( -1.000000000000000000, -0.000000000000000000, -0.000000000000000000 ) ) ;
#84618=FACE_OUTER_BOUND ( 'NONE', #46541, .T. ) ;
#84635=DIRECTION ( 'NONE',  ( 0.000000000000000000, -1.000000000000000000, 0.000000000000000000 ) ) ;
#84645=CONICAL_SURFACE ( 'NONE', #91502, 4.172000000000009479, 0.9599310885968813656 ) ;
#84683=EDGE_CURVE ( 'NONE', #22906, #82852, #104012, .T. ) ;
#84685=ORIENTED_EDGE ( 'NONE', *, *, #55535, .T. ) ;
#84719=CIRCLE ( 'NONE', #81228, 4.171999999999999709 ) ;
#84760=DIRECTION ( 'NONE',  ( -1.000000000000000000, -1.224606353822377258E-16, -0.000000000000000000 ) ) ;
#84787=AXIS2_PLACEMENT_3D ( 'NONE', #86412, #37338, #62136 ) ;
#84922=CARTESIAN_POINT ( 'NONE',  ( 104.9555555555555486, 1.023464760207051730E-14, 0.000000000000000000 ) ) ;
#84959=AXIS2_PLACEMENT_3D ( 'NONE', #34415, #60279, #17142 ) ;
#84982=CARTESIAN_POINT ( 'NONE',  ( 85.31310517497098544, 1.030564683017419500E-14, 0.000000000000000000 ) ) ;
#85007=ORIENTED_EDGE ( 'NONE', *, *, #9184, .F. ) ;
#85028=ORIENTED_EDGE ( 'NONE', *, *, #38768, .F. ) ;
#85048=ORIENTED_EDGE ( 'NONE', *, *, #93560, .F. ) ;
#85106=VERTEX_POINT ( 'NONE', #32736 ) ;
#85221=DIRECTION ( 'NONE',  ( -1.000000000000000000, -1.224606353822377258E-16, -0.000000000000000000 ) ) ;
#85247=CARTESIAN_POINT ( 'NONE',  ( 0.000000000000000000, 0.000000000000000000, 5.000000000000000888 ) ) ;
#85271=FACE_OUTER_BOUND ( 'NONE', #72103, .T. ) ;
#85301=ORIENTED_EDGE ( 'NONE', *, *, #18794, .T. ) ;
#85309=EDGE_CURVE ( 'NONE', #87052, #73379, #15348, .T. ) ;
#85413=ORIENTED_EDGE ( 'NONE', *, *, #18875, .F. ) ;
#85441=CYLINDRICAL_SURFACE ( 'NONE', #65695, 5.000000000000000888 ) ;
#85459=ORIENTED_EDGE ( 'NONE', *, *, #53888, .T. ) ;
#85464=CARTESIAN_POINT ( 'NONE',  ( 95.42421628608209971, -5.000000000000000888, 6.123233995736779101E-16 ) ) ;
#85468=CONICAL_SURFACE ( 'NONE', #76826, 4.172000000000009479, 0.9599310885968813656 ) ;
#85485=EDGE_CURVE ( 'NONE', #28024, #104209, #61076, .T. ) ;
#85495=PRODUCT_DEFINITION_SHAPE ( 'NONE', 'NONE',  #105582 ) ;
#85498=CIRCLE ( 'NONE', #35556, 4.172000000000009479 ) ;
#85503=AXIS2_PLACEMENT_3D ( 'NONE', #9348, #90290, #74621 ) ;
#85533=CYLINDRICAL_SURFACE ( 'NONE', #43256, 5.000000000000000888 ) ;
#85551=ORIENTED_EDGE ( 'NONE', *, *, #78889, .F. ) ;
#85553=DIRECTION ( 'NONE',  ( -1.000000000000000000, -1.224606353822377258E-16, -0.000000000000000000 ) ) ;
#85563=FACE_OUTER_BOUND ( 'NONE', #361, .T. ) ;
#85588=CARTESIAN_POINT ( 'NONE',  ( 6.400000000000000355, 4.618802153517003184, -8.000000000000000000 ) ) ;
#85594=CARTESIAN_POINT ( 'NONE',  ( 104.0908829527487711, -5.000000000000000888, 6.123233995736779101E-16 ) ) ;
#85640=ADVANCED_FACE ( 'NONE', ( #34106 ), #45605, .T. ) ;
#85642=DIRECTION ( 'NONE',  ( 0.000000000000000000, -1.000000000000000000, 0.000000000000000000 ) ) ;
#85648=VERTEX_POINT ( 'NONE', #16826 ) ;
#85655=EDGE_CURVE ( 'NONE', #9366, #6102, #42107, .T. ) ;
#85678=AXIS2_PLACEMENT_3D ( 'NONE', #67831, #65709, #74838 ) ;
#85682=CARTESIAN_POINT ( 'NONE',  ( 97.73333333333333428, 1.023464760207051730E-14, 0.000000000000000000 ) ) ;
#85701=EDGE_CURVE ( 'NONE', #38733, #42532, #102412, .T. ) ;
#85726=DIRECTION ( 'NONE',  ( -1.000000000000000000, -1.224606353822377258E-16, -0.000000000000000000 ) ) ;
#85803=CARTESIAN_POINT ( 'NONE',  ( 5.799999999999999822, 4.618802153517005848, 7.999999999999996447 ) ) ;
#85848=CONICAL_SURFACE ( 'NONE', #72040, 5.000000000000010658, 0.9599310885968697082 ) ;
#85866=AXIS2_PLACEMENT_3D ( 'NONE', #78783, #4374, #53969 ) ;
#85869=EDGE_LOOP ( 'NONE', ( #82877, #25592, #97098, #10423 ) ) ;
#85878=CARTESIAN_POINT ( 'NONE',  ( 82.42421628608209971, 6.123233995736568081E-16, -5.000000000000011546 ) ) ;
#85899=DIRECTION ( 'NONE',  ( -1.000000000000000000, -1.224606353822377258E-16, -0.000000000000000000 ) ) ;
#85913=AXIS2_PLACEMENT_3D ( 'NONE', #90553, #16662, #66813 ) ;
#85924=DIRECTION ( 'NONE',  ( 0.000000000000000000, -1.000000000000000000, 0.000000000000000000 ) ) ;
#85930=AXIS2_PLACEMENT_3D ( 'NONE', #83977, #75885, #889 ) ;
#85957=CARTESIAN_POINT ( 'NONE',  ( 0.000000000000000000, 0.000000000000000000, 0.000000000000000000 ) ) ;
#85971=DIRECTION ( 'NONE',  ( -1.000000000000000000, -1.224606353822377258E-16, -0.000000000000000000 ) ) ;
#86005=AXIS2_PLACEMENT_3D ( 'NONE', #15683, #7578, #80412 ) ;
#86041=CARTESIAN_POINT ( 'NONE',  ( 87.04245038058458306, 6.123233995736582872E-16, -5.000000000000011546 ) ) ;
#86055=CIRCLE ( 'NONE', #99798, 5.000000000000011546 ) ;
#86060=EDGE_CURVE ( 'NONE', #46987, #49140, #56541, .T. ) ;
#86102=CARTESIAN_POINT ( 'NONE',  ( 81.84444444444444855, 1.023464760207051730E-14, 0.000000000000000000 ) ) ;
#86110=LINE ( 'NONE', #69904, #93238 ) ;
#86113=EDGE_CURVE ( 'NONE', #6669, #51522, #11225, .T. ) ;
#86123=AXIS2_PLACEMENT_3D ( 'NONE', #54810, #15420, #62934 ) ;
#86159=CARTESIAN_POINT ( 'NONE',  ( 89.64643850830432825, -5.000000000000000000, 6.123233995736778115E-16 ) ) ;
#86188=CARTESIAN_POINT ( 'NONE',  ( 85.31310517497098544, 1.030564683017419500E-14, 0.000000000000000000 ) ) ;
#86197=ORIENTED_EDGE ( 'NONE', *, *, #48450, .F. ) ;
#86205=DIRECTION ( 'NONE',  ( 0.000000000000000000, -1.000000000000000000, 0.000000000000000000 ) ) ;
#86253=DIRECTION ( 'NONE',  ( 0.000000000000000000, 0.000000000000000000, 1.000000000000000000 ) ) ;
#86311=EDGE_CURVE ( 'NONE', #102376, #63754, #799, .T. ) ;
#86330=EDGE_CURVE ( 'NONE', #49122, #72914, #99076, .T. ) ;
#86333=CARTESIAN_POINT ( 'NONE',  ( 87.04245038058458306, -5.000000000000000000, 0.000000000000000000 ) ) ;
#86336=CARTESIAN_POINT ( 'NONE',  ( 0.000000000000000000, 6.928203230275505220, 4.000000000000006217 ) ) ;
#86353=CIRCLE ( 'NONE', #82854, 5.000000000000011546 ) ;
#86390=DIRECTION ( 'NONE',  ( 0.000000000000000000, -1.000000000000000000, 0.000000000000000000 ) ) ;
#86397=EDGE_CURVE ( 'NONE', #92683, #79234, #84073, .T. ) ;
#86398=ADVANCED_FACE ( 'NONE', ( #68974 ), #74892, .T. ) ;
#86412=CARTESIAN_POINT ( 'NONE',  ( 0.000000000000000000, 0.000000000000000000, 0.000000000000000000 ) ) ;
#86457=EDGE_CURVE ( 'NONE', #27178, #9659, #62998, .T. ) ;
#86532=ADVANCED_FACE ( 'NONE', ( #56469 ), #100618, .T. ) ;
#86566=DIRECTION ( 'NONE',  ( -1.000000000000000000, -0.000000000000000000, -0.000000000000000000 ) ) ;
#86591=CARTESIAN_POINT ( 'NONE',  ( 105.5720000000000312, 6.123233995736768255E-16, -5.000000000000000888 ) ) ;
#86606=EDGE_CURVE ( 'NONE', #9728, #14501, #45741, .T. ) ;
#86607=CARTESIAN_POINT ( 'NONE',  ( 84.73333333333332007, 1.023464760207051730E-14, 0.000000000000000000 ) ) ;
#86608=VERTEX_POINT ( 'NONE', #35438 ) ;
#86609=DIRECTION ( 'NONE',  ( 0.000000000000000000, 0.000000000000000000, 1.000000000000000000 ) ) ;
#86610=DIRECTION ( 'NONE',  ( -1.000000000000000000, -0.000000000000000000, -0.000000000000000000 ) ) ;
#86644=ORIENTED_EDGE ( 'NONE', *, *, #93701, .T. ) ;
#86704=FACE_OUTER_BOUND ( 'NONE', #14324, .T. ) ;
#86714=DIRECTION ( 'NONE',  ( -1.000000000000000000, -0.000000000000000000, -0.000000000000000000 ) ) ;
#86772=DIRECTION ( 'NONE',  ( -0.5735764363510461594, 0.8191520442889916875, 1.003171929053524870E-16 ) ) ;
#86822=ORIENTED_EDGE ( 'NONE', *, *, #86060, .T. ) ;
#86851=EDGE_LOOP ( 'NONE', ( #39418, #21385, #44442, #80527, #84685 ) ) ;
#86867=VERTEX_POINT ( 'NONE', #42990 ) ;
#86997=DIRECTION ( 'NONE',  ( -1.000000000000000000, -1.224606353822377258E-16, -0.000000000000000000 ) ) ;
#87052=VERTEX_POINT ( 'NONE', #63441 ) ;
#87100=CARTESIAN_POINT ( 'NONE',  ( 0.000000000000000000, 6.123233995736767268E-16, -5.000000000000000888 ) ) ;
#87154=DIRECTION ( 'NONE',  ( -1.000000000000000000, -1.224606353822377258E-16, -0.000000000000000000 ) ) ;
#87178=CIRCLE ( 'NONE', #63062, 5.000000000000000888 ) ;
#87183=AXIS2_PLACEMENT_3D ( 'NONE', #43162, #35639, #83084 ) ;
#87190=CARTESIAN_POINT ( 'NONE',  ( 92.53532739719321398, -2.002967142162725287E-29, 5.000000000000011546 ) ) ;
#87253=DIRECTION ( 'NONE',  ( 0.000000000000000000, -1.000000000000000000, 0.000000000000000000 ) ) ;
#87293=CARTESIAN_POINT ( 'NONE',  ( 93.97977184163765685, 1.030564683017419500E-14, 0.000000000000000000 ) ) ;
#87324=AXIS2_PLACEMENT_3D ( 'NONE', #25175, #56961, #64552 ) ;
#87347=ORIENTED_EDGE ( 'NONE', *, *, #39623, .T. ) ;
#87350=CIRCLE ( 'NONE', #70174, 5.000000000000010658 ) ;
#87398=AXIS2_PLACEMENT_3D ( 'NONE', #72867, #53653, #70904 ) ;
#87417=CARTESIAN_POINT ( 'NONE',  ( 105.5353273971932140, 1.030564683017419500E-14, 0.000000000000000000 ) ) ;
#87420=EDGE_CURVE ( 'NONE', #85648, #15028, #11143, .T. ) ;
#87467=ADVANCED_FACE ( 'NONE', ( #83110 ), #34070, .T. ) ;
#87519=ORIENTED_EDGE ( 'NONE', *, *, #71667, .F. ) ;
#87544=VERTEX_POINT ( 'NONE', #74476 ) ;
#87549=AXIS2_PLACEMENT_3D ( 'NONE', #106252, #74949, #81443 ) ;
#87568=CARTESIAN_POINT ( 'NONE',  ( 83.28888888888889142, -4.171999999999998820, 0.000000000000000000 ) ) ;
#87577=ORIENTED_EDGE ( 'NONE', *, *, #54899, .F. ) ;
#87584=EDGE_LOOP ( 'NONE', ( #46683, #64068, #80626, #32478, #80509 ) ) ;
#87618=DIRECTION ( 'NONE',  ( 0.000000000000000000, 0.5000000000000008882, -0.8660254037844381525 ) ) ;
#87628=EDGE_CURVE ( 'NONE', #35844, #76618, #38744, .T. ) ;
#87632=CARTESIAN_POINT ( 'NONE',  ( 99.75754961941544252, 1.030564683017419500E-14, 0.000000000000000000 ) ) ;
#87667=ORIENTED_EDGE ( 'NONE', *, *, #36078, .T. ) ;
#87677=FACE_OUTER_BOUND ( 'NONE', #63247, .T. ) ;
#87720=CIRCLE ( 'NONE', #10239, 8.000000000000000000 ) ;
#87738=AXIS2_PLACEMENT_3D ( 'NONE', #19965, #52270, #10221 ) ;
#87743=VECTOR ( 'NONE', #66016, 1000.000000000000000 ) ;
#87769=AXIS2_PLACEMENT_3D ( 'NONE', #23762, #64721, #54613 ) ;
#87784=AXIS2_PLACEMENT_3D ( 'NONE', #95289, #47241, #63995 ) ;
#87800=ORIENTED_EDGE ( 'NONE', *, *, #42074, .T. ) ;
#87820=LINE ( 'NONE', #105060, #68406 ) ;
#87821=CONICAL_SURFACE ( 'NONE', #10342, 8.000000000000000000, 1.047197551196600296 ) ;
#87883=ADVANCED_FACE ( 'NONE', ( #3788 ), #38805, .T. ) ;
#87907=CARTESIAN_POINT ( 'NONE',  ( 0.3157512944460784676, -3.097794232780207491, 8.000000000000000000 ) ) ;
#87937=ORIENTED_EDGE ( 'NONE', *, *, #37238, .T. ) ;
#87956=CIRCLE ( 'NONE', #56897, 5.000000000000010658 ) ;
#87999=VERTEX_POINT ( 'NONE', #13973 ) ;
#88048=ORIENTED_EDGE ( 'NONE', *, *, #87628, .T. ) ;
#88065=VECTOR ( 'NONE', #67206, 1000.000000000000000 ) ;
#88095=CARTESIAN_POINT ( 'NONE',  ( 0.000000000000000000, 0.000000000000000000, 0.000000000000000000 ) ) ;
#88116=LINE ( 'NONE', #63319, #25257 ) ;
#88133=CARTESIAN_POINT ( 'NONE',  ( 90.51111111111110574, 4.172000000000019249, 0.000000000000000000 ) ) ;
#88150=CARTESIAN_POINT ( 'NONE',  ( 103.5111111111111057, 1.023464760207051730E-14, 0.000000000000000000 ) ) ;
#88211=CARTESIAN_POINT ( 'NONE',  ( 0.000000000000000000, 6.123233995736767268E-16, -5.000000000000000888 ) ) ;
#88229=CONICAL_SURFACE ( 'NONE', #96767, 4.172000000000009479, 0.9599310885968813656 ) ;
#88275=ADVANCED_FACE ( 'NONE', ( #4721 ), #97444, .T. ) ;
#88277=ORIENTED_EDGE ( 'NONE', *, *, #31356, .F. ) ;
#88379=CARTESIAN_POINT ( 'NONE',  ( 5.799999999999999822, 8.000000000000000000, 0.000000000000000000 ) ) ;
#88444=EDGE_CURVE ( 'NONE', #17510, #64937, #40636, .T. ) ;
#88450=ORIENTED_EDGE ( 'NONE', *, *, #88636, .F. ) ;
#88636=EDGE_CURVE ( 'NONE', #64079, #69907, #18342, .T. ) ;
#88677=ADVANCED_FACE ( 'NONE', ( #25896 ), #95851, .T. ) ;
#88742=VERTEX_POINT ( 'NONE', #15964 ) ;
#88764=EDGE_CURVE ( 'NONE', #24268, #92963, #32711, .T. ) ;
#88803=CARTESIAN_POINT ( 'NONE',  ( 99.75754961941544252, 1.030564683017419500E-14, 0.000000000000000000 ) ) ;
#88807=ORIENTED_EDGE ( 'NONE', *, *, #83334, .T. ) ;
#88821=ORIENTED_EDGE ( 'NONE', *, *, #16480, .T. ) ;
#88883=CARTESIAN_POINT ( 'NONE',  ( 95.70911704725124025, -5.000000000000020428, 0.000000000000000000 ) ) ;
#88884=AXIS2_PLACEMENT_3D ( 'NONE', #33900, #67314, #75920 ) ;
#88893=DIRECTION ( 'NONE',  ( -1.000000000000000000, -1.224606353822377258E-16, -0.000000000000000000 ) ) ;
#88903=EDGE_LOOP ( 'NONE', ( #88048, #62243 ) ) ;
#88936=ORIENTED_EDGE ( 'NONE', *, *, #93201, .T. ) ;
#88964=PLANE ( 'NONE',  #43405 ) ;
#88974=CARTESIAN_POINT ( 'NONE',  ( 91.09088295274877112, 1.030564683017419500E-14, 0.000000000000000000 ) ) ;
#88989=ADVANCED_FACE ( 'NONE', ( #104939 ), #42409, .T. ) ;
#88995=AXIS2_PLACEMENT_3D ( 'NONE', #61783, #70384, #29428 ) ;
#89005=VECTOR ( 'NONE', #10337, 1000.000000000000000 ) ;
#89007=VECTOR ( 'NONE', #34657, 1000.000000000000000 ) ;
#89046=EDGE_CURVE ( 'NONE', #100880, #13325, #42784, .T. ) ;
#89071=VECTOR ( 'NONE', #17172, 1000.000000000000000 ) ;
#89092=EDGE_CURVE ( 'NONE', #13329, #28602, #103094, .T. ) ;
#89095=CIRCLE ( 'NONE', #90880, 5.000000000000010658 ) ;
#89125=CARTESIAN_POINT ( 'NONE',  ( 95.70911704725124025, 1.016364837396684119E-14, 0.000000000000000000 ) ) ;
#89133=CARTESIAN_POINT ( 'NONE',  ( 80.97977184163765685, 5.000000000000020428, 0.000000000000000000 ) ) ;
#89169=VERTEX_POINT ( 'NONE', #62113 ) ;
#89200=CIRCLE ( 'NONE', #104733, 5.000000000000011546 ) ;
#89220=VERTEX_POINT ( 'NONE', #25372 ) ;
#89257=ORIENTED_EDGE ( 'NONE', *, *, #36033, .F. ) ;
#89280=CARTESIAN_POINT ( 'NONE',  ( 104.0908829527487711, -5.000000000000000000, 6.123233995736778115E-16 ) ) ;
#89316=DIRECTION ( 'NONE',  ( -1.000000000000000000, -1.224606353822377258E-16, -0.000000000000000000 ) ) ;
#89322=VECTOR ( 'NONE', #10633, 999.9999999999998863 ) ;
#89347=DIRECTION ( 'NONE',  ( -1.000000000000000000, -1.224606353822377258E-16, -0.000000000000000000 ) ) ;
#89360=CARTESIAN_POINT ( 'NONE',  ( 0.000000000000000000, 0.000000000000000000, 5.000000000000000888 ) ) ;
#89386=DIRECTION ( 'NONE',  ( -1.000000000000000000, -1.224606353822377258E-16, -0.000000000000000000 ) ) ;
#89395=ORIENTED_EDGE ( 'NONE', *, *, #14073, .F. ) ;
#89399=DIRECTION ( 'NONE',  ( 1.000000000000000000, 1.224606353822377258E-16, 0.000000000000000000 ) ) ;
#89415=CONICAL_SURFACE ( 'NONE', #53227, 4.172000000000009479, 0.9599310885968813656 ) ;
#89461=AXIS2_PLACEMENT_3D ( 'NONE', #21904, #87154, #55797 ) ;
#89498=CARTESIAN_POINT ( 'NONE',  ( 83.86866073052654258, 1.030564683017419500E-14, 0.000000000000000000 ) ) ;
#89600=DIRECTION ( 'NONE',  ( 0.000000000000000000, 0.000000000000000000, 1.000000000000000000 ) ) ;
#89617=CIRCLE ( 'NONE', #67302, 5.000000000000010658 ) ;
#89750=CIRCLE ( 'NONE', #75958, 8.000000000000000000 ) ;
#89767=DIRECTION ( 'NONE',  ( 0.000000000000000000, 1.000000000000000000, 0.000000000000000000 ) ) ;
#89783=EDGE_CURVE ( 'NONE', #76580, #45933, #41103, .T. ) ;
#89788=CARTESIAN_POINT ( 'NONE',  ( 86.17777777777776294, 1.023464760207051730E-14, 0.000000000000000000 ) ) ;
#89890=ORIENTED_EDGE ( 'NONE', *, *, #97741, .T. ) ;
#89928=EDGE_CURVE ( 'NONE', #34210, #49122, #103155, .T. ) ;
#89942=CONICAL_SURFACE ( 'NONE', #100255, 4.172000000000009479, 0.9599310885968813656 ) ;
#89954=VECTOR ( 'NONE', #6252, 1000.000000000000000 ) ;
#90013=ORIENTED_EDGE ( 'NONE', *, *, #86397, .F. ) ;
#90104=LINE ( 'NONE', #58818, #29432 ) ;
#90139=DIRECTION ( 'NONE',  ( 0.000000000000000000, -1.000000000000000000, 0.000000000000000000 ) ) ;
#90151=CARTESIAN_POINT ( 'NONE',  ( 0.000000000000000000, 6.928203230275505220, -4.000000000000007105 ) ) ;
#90174=EDGE_CURVE ( 'NONE', #105973, #9396, #54934, .T. ) ;
#90186=DIRECTION ( 'NONE',  ( -1.000000000000000000, -1.224606353822377258E-16, -0.000000000000000000 ) ) ;
#90196=CARTESIAN_POINT ( 'NONE',  ( 87.04245038058458306, 1.016364837396684119E-14, 0.000000000000000000 ) ) ;
#90203=ORIENTED_EDGE ( 'NONE', *, *, #35625, .F. ) ;
#90242=CARTESIAN_POINT ( 'NONE',  ( 5.799999999999999822, 4.618802153517003184, -8.000000000000000000 ) ) ;
#90267=AXIS2_PLACEMENT_3D ( 'NONE', #101237, #93679, #51060 ) ;
#90284=DIRECTION ( 'NONE',  ( -1.000000000000000000, -1.224606353822377258E-16, -0.000000000000000000 ) ) ;
#90290=DIRECTION ( 'NONE',  ( -1.000000000000000000, -1.224606353822377258E-16, -0.000000000000000000 ) ) ;
#90338=DIRECTION ( 'NONE',  ( 1.000000000000000000, 1.224606353822377258E-16, 0.000000000000000000 ) ) ;
#90339=ORIENTED_EDGE ( 'NONE', *, *, #101646, .F. ) ;
#90354=ORIENTED_EDGE ( 'NONE', *, *, #89046, .F. ) ;
#90363=LINE ( 'NONE', #40745, #60251 ) ;
#90378=EDGE_CURVE ( 'NONE', #82760, #20011, #82520, .T. ) ;
#90408=FACE_OUTER_BOUND ( 'NONE', #6196, .T. ) ;
#90445=ORIENTED_EDGE ( 'NONE', *, *, #68960, .T. ) ;
#90473=ADVANCED_FACE ( 'NONE', ( #73766 ), #91044, .T. ) ;
#90502=LINE ( 'NONE', #74308, #3208 ) ;
#90533=CIRCLE ( 'NONE', #25119, 4.172000000000009479 ) ;
#90553=CARTESIAN_POINT ( 'NONE',  ( 80.40000000000000568, 1.023464760207051730E-14, 0.000000000000000000 ) ) ;
#90569=CARTESIAN_POINT ( 'NONE',  ( 89.64643850830432825, 1.030564683017419500E-14, 0.000000000000000000 ) ) ;
#90570=CARTESIAN_POINT ( 'NONE',  ( 81.26467260280679739, 1.016364837396684119E-14, 0.000000000000000000 ) ) ;
#90573=UNCERTAINTY_MEASURE_WITH_UNIT (LENGTH_MEASURE( 1.000000000000000082E-05 ), #100043, 'distance_accuracy_value', 'NONE');
#90601=ORIENTED_EDGE ( 'NONE', *, *, #45674, .F. ) ;
#90611=CARTESIAN_POINT ( 'NONE',  ( 91.09088295274877112, 1.030564683017419500E-14, 0.000000000000000000 ) ) ;
#90612=CARTESIAN_POINT ( 'NONE',  ( 92.53532739719321398, 1.030564683017419500E-14, 0.000000000000000000 ) ) ;
#90621=EDGE_LOOP ( 'NONE', ( #16149, #96849, #35379 ) ) ;
#90647=EDGE_CURVE ( 'NONE', #24844, #70018, #92899, .T. ) ;
#90718=ORIENTED_EDGE ( 'NONE', *, *, #65872, .T. ) ;
#90721=EDGE_LOOP ( 'NONE', ( #25803, #58414, #37029, #8698, #46248, #41122 ) ) ;
#90733=CARTESIAN_POINT ( 'NONE',  ( 0.06809871960542319969, -6.146186931204438153, -5.354491962338079780 ) ) ;
#90740=LINE ( 'NONE', #26057, #89005 ) ;
#90750=ORIENTED_EDGE ( 'NONE', *, *, #75544, .F. ) ;
#90806=ORIENTED_EDGE ( 'NONE', *, *, #81192, .F. ) ;
#90832=LINE ( 'NONE', #16947, #61760 ) ;
#90848=DIRECTION ( 'NONE',  ( -1.000000000000000000, -1.224606353822377258E-16, -0.000000000000000000 ) ) ;
#90852=VECTOR ( 'NONE', #71679, 1000.000000000000000 ) ;
#90876=ORIENTED_EDGE ( 'NONE', *, *, #7508, .T. ) ;
#90880=AXIS2_PLACEMENT_3D ( 'NONE', #18877, #51720, #84635 ) ;
#90893=EDGE_CURVE ( 'NONE', #76468, #51522, #16475, .T. ) ;
#90922=EDGE_CURVE ( 'NONE', #9659, #41772, #43023, .T. ) ;
#90932=VERTEX_POINT ( 'NONE', #43416 ) ;
#90947=MANIFOLD_SOLID_BREP ( 'ThdSchPat', #49764 ) ;
#90953=CARTESIAN_POINT ( 'NONE',  ( 91.09088295274877112, 1.030564683017419500E-14, 0.000000000000000000 ) ) ;
#90962=ORIENTED_EDGE ( 'NONE', *, *, #5169, .T. ) ;
#90963=CARTESIAN_POINT ( 'NONE',  ( 6.800000000000000711, 0.000000000000000000, 0.000000000000000000 ) ) ;
#90990=CIRCLE ( 'NONE', #10056, 5.000000000000011546 ) ;
#91007=AXIS2_PLACEMENT_3D ( 'NONE', #58726, #83512, #961 ) ;
#91018=ORIENTED_EDGE ( 'NONE', *, *, #23480, .T. ) ;
#91031=CARTESIAN_POINT ( 'NONE',  ( 6.800000000000000711, 0.000000000000000000, 0.000000000000000000 ) ) ;
#91044=CYLINDRICAL_SURFACE ( 'NONE', #6758, 5.000000000000000888 ) ;
#91066=AXIS2_PLACEMENT_3D ( 'NONE', #10036, #106055, #97982 ) ;
#91067=CARTESIAN_POINT ( 'NONE',  ( 83.28888888888889142, 1.023464760207051730E-14, 0.000000000000000000 ) ) ;
#91096=ORIENTED_EDGE ( 'NONE', *, *, #73513, .T. ) ;
#91118=ORIENTED_EDGE ( 'NONE', *, *, #75125, .T. ) ;
#91170=DIRECTION ( 'NONE',  ( -1.000000000000000000, -1.224606353822377258E-16, -0.000000000000000000 ) ) ;
#91232=CARTESIAN_POINT ( 'NONE',  ( 5.799999999999999822, -6.928203230275510549, -3.999999999999997335 ) ) ;
#91255=DIRECTION ( 'NONE',  ( -1.000000000000000000, -0.000000000000000000, -0.000000000000000000 ) ) ;
#91337=PLANE ( 'NONE',  #105462 ) ;
#91356=AXIS2_PLACEMENT_3D ( 'NONE', #97868, #24024, #17506 ) ;
#91366=DIRECTION ( 'NONE',  ( 0.000000000000000000, -1.000000000000000000, 0.000000000000000000 ) ) ;
#91387=CARTESIAN_POINT ( 'NONE',  ( 86.75754961941542831, 1.030564683017419500E-14, 0.000000000000000000 ) ) ;
#91395=ORIENTED_EDGE ( 'NONE', *, *, #81040, .F. ) ;
#91402=EDGE_CURVE ( 'NONE', #19034, #1527, #74572, .T. ) ;
#91418=ORIENTED_EDGE ( 'NONE', *, *, #67, .F. ) ;
#91437=CIRCLE ( 'NONE', #105209, 5.000000000000011546 ) ;
#91442=( NAMED_UNIT ( * ) PLANE_ANGLE_UNIT ( ) SI_UNIT ( $, .RADIAN. ) );
#91471=CARTESIAN_POINT ( 'NONE',  ( 93.39999999999999147, 1.023464760207051730E-14, 0.000000000000000000 ) ) ;
#91479=DIRECTION ( 'NONE',  ( -1.000000000000000000, -0.000000000000000000, -0.000000000000000000 ) ) ;
#91486=DIRECTION ( 'NONE',  ( -1.000000000000000000, -1.224606353822377258E-16, -0.000000000000000000 ) ) ;
#91498=ORIENTED_EDGE ( 'NONE', *, *, #11221, .F. ) ;
#91502=AXIS2_PLACEMENT_3D ( 'NONE', #402, #48451, #7456 ) ;
#91557=CIRCLE ( 'NONE', #55335, 4.172000000000009479 ) ;
#91559=ORIENTED_EDGE ( 'NONE', *, *, #76804, .T. ) ;
#91564=CARTESIAN_POINT ( 'NONE',  ( 89.93133926947346879, -2.002967142162725287E-29, 5.000000000000011546 ) ) ;
#91575=CARTESIAN_POINT ( 'NONE',  ( 86.75754961941542831, 1.030564683017419500E-14, 0.000000000000000000 ) ) ;
#91608=AXIS2_PLACEMENT_3D ( 'NONE', #103908, #96377, #103390 ) ;
#91692=CARTESIAN_POINT ( 'NONE',  ( 99.75754961941544252, 6.123233995736568081E-16, -5.000000000000011546 ) ) ;
#91763=DIRECTION ( 'NONE',  ( 0.000000000000000000, -0.5000000000000009992, -0.8660254037844380415 ) ) ;
#91781=CARTESIAN_POINT ( 'NONE',  ( 0.000000000000000000, 0.000000000000000000, 0.000000000000000000 ) ) ;
#91791=DIRECTION ( 'NONE',  ( -1.000000000000000000, -0.000000000000000000, -0.000000000000000000 ) ) ;
#91795=VECTOR ( 'NONE', #100766, 1000.000000000000000 ) ;
#91816=ORIENTED_EDGE ( 'NONE', *, *, #20482, .F. ) ;
#91848=CARTESIAN_POINT ( 'NONE',  ( 99.75754961941544252, 1.030564683017419500E-14, 0.000000000000000000 ) ) ;
#91852=DIRECTION ( 'NONE',  ( 0.000000000000000000, 0.000000000000000000, -1.000000000000000000 ) ) ;
#91896=ORIENTED_EDGE ( 'NONE', *, *, #53461, .T. ) ;
#91949=EDGE_CURVE ( 'NONE', #20613, #33098, #90104, .T. ) ;
#91956=SURFACE_STYLE_FILL_AREA ( #42874 ) ;
#92048=VERTEX_POINT ( 'NONE', #82545 ) ;
#92084=EDGE_CURVE ( 'NONE', #11414, #64162, #101686, .T. ) ;
#92102=ORIENTED_EDGE ( 'NONE', *, *, #76810, .T. ) ;
#92175=CARTESIAN_POINT ( 'NONE',  ( 97.15356149169568312, -2.002967142162725287E-29, 5.000000000000011546 ) ) ;
#92190=ADVANCED_FACE ( 'NONE', ( #19988 ), #81037, .T. ) ;
#92267=ADVANCED_FACE ( 'NONE', ( #98494 ), #1881, .F. ) ;
#92304=DIRECTION ( 'NONE',  ( -1.000000000000000000, -1.224606353822377258E-16, -0.000000000000000000 ) ) ;
#92330=LINE ( 'NONE', #19566, #42838 ) ;
#92332=CARTESIAN_POINT ( 'NONE',  ( 82.70911704725124025, 6.123233995736582872E-16, -5.000000000000011546 ) ) ;
#92333=ADVANCED_FACE ( 'NONE', ( #11073 ), #27866, .T. ) ;
#92335=ADVANCED_FACE ( 'NONE', ( #1923 ), #85533, .T. ) ;
#92360=CIRCLE ( 'NONE', #83990, 5.000000000000010658 ) ;
#92371=AXIS2_PLACEMENT_3D ( 'NONE', #58307, #57226, #82035 ) ;
#92383=VECTOR ( 'NONE', #33578, 1000.000000000000000 ) ;
#92384=CARTESIAN_POINT ( 'NONE',  ( 85.59800593614014019, 1.016364837396684119E-14, 0.000000000000000000 ) ) ;
#92425=DIRECTION ( 'NONE',  ( -1.000000000000000000, -1.224606353822377258E-16, -0.000000000000000000 ) ) ;
#92455=CONICAL_SURFACE ( 'NONE', #42563, 5.000000000000010658, 0.9599310885968697082 ) ;
#92526=ORIENTED_EDGE ( 'NONE', *, *, #64566, .T. ) ;
#92527=DIRECTION ( 'NONE',  ( -0.5735764363510459374, -0.8191520442889919096, 0.000000000000000000 ) ) ;
#92560=DIRECTION ( 'NONE',  ( 0.000000000000000000, 0.000000000000000000, 1.000000000000000000 ) ) ;
#92576=EDGE_LOOP ( 'NONE', ( #57772, #56310, #72998, #79883, #53426 ) ) ;
#92586=VERTEX_POINT ( 'NONE', #48747 ) ;
#92599=ADVANCED_FACE ( 'NONE', ( #99971 ), #64954, .T. ) ;
#92607=CARTESIAN_POINT ( 'NONE',  ( 106.4000000000000057, 0.000000000000000000, 0.000000000000000000 ) ) ;
#92663=ORIENTED_EDGE ( 'NONE', *, *, #28315, .F. ) ;
#92683=VERTEX_POINT ( 'NONE', #57375 ) ;
#92685=CIRCLE ( 'NONE', #25420, 4.172000000000009479 ) ;
#92704=ORIENTED_EDGE ( 'NONE', *, *, #7213, .F. ) ;
#92721=ADVANCED_FACE ( 'NONE', ( #10944 ), #55237, .T. ) ;
#92846=CARTESIAN_POINT ( 'NONE',  ( 6.400000000000000355, 4.618802153517005848, 7.999999999999996447 ) ) ;
#92853=CARTESIAN_POINT ( 'NONE',  ( 0.000000000000000000, 0.000000000000000000, 5.000000000000000888 ) ) ;
#92870=DIRECTION ( 'NONE',  ( -1.000000000000000000, -1.224606353822377258E-16, -0.000000000000000000 ) ) ;
#92888=CIRCLE ( 'NONE', #6740, 5.000000000000010658 ) ;
#92899=CIRCLE ( 'NONE', #22345, 4.172000000000009479 ) ;
#92952=DIRECTION ( 'NONE',  ( -1.000000000000000000, -0.000000000000000000, -0.000000000000000000 ) ) ;
#92963=VERTEX_POINT ( 'NONE', #77174 ) ;
#92985=ORIENTED_EDGE ( 'NONE', *, *, #55610, .F. ) ;
#93085=AXIS2_PLACEMENT_3D ( 'NONE', #55002, #79822, #29215 ) ;
#93099=FACE_OUTER_BOUND ( 'NONE', #95119, .T. ) ;
#93116=ORIENTED_EDGE ( 'NONE', *, *, #37501, .T. ) ;
#93127=CIRCLE ( 'NONE', #43232, 5.000000000000010658 ) ;
#93191=AXIS2_PLACEMENT_3D ( 'NONE', #77148, #3264, #36205 ) ;
#93192=VECTOR ( 'NONE', #71633, 1000.000000000000000 ) ;
#93201=EDGE_CURVE ( 'NONE', #69907, #40083, #106195, .T. ) ;
#93223=DIRECTION ( 'NONE',  ( 1.000000000000000000, 1.224606353822377258E-16, 0.000000000000000000 ) ) ;
#93238=VECTOR ( 'NONE', #79575, 1000.000000000000000 ) ;
#93244=ORIENTED_EDGE ( 'NONE', *, *, #11335, .T. ) ;
#93260=ORIENTED_EDGE ( 'NONE', *, *, #42170, .T. ) ;
#93268=DIRECTION ( 'NONE',  ( 0.000000000000000000, -1.000000000000000000, 0.000000000000000000 ) ) ;
#93274=AXIS2_PLACEMENT_3D ( 'NONE', #102895, #27453, #46252 ) ;
#93380=AXIS2_PLACEMENT_3D ( 'NONE', #91387, #90848, #9367 ) ;
#93406=CARTESIAN_POINT ( 'NONE',  ( 93.39999999999999147, -4.171999999999998820, 5.616230220889773285E-16 ) ) ;
#93407=DIRECTION ( 'NONE',  ( 0.000000000000000000, 0.000000000000000000, -1.000000000000000000 ) ) ;
#93417=CONICAL_SURFACE ( 'NONE', #84787, 8.000000000000000000, 1.047197551196600296 ) ;
#93453=CIRCLE ( 'NONE', #40004, 5.000000000000011546 ) ;
#93462=DIRECTION ( 'NONE',  ( 1.000000000000000000, 0.000000000000000000, 0.000000000000000000 ) ) ;
#93472=FACE_OUTER_BOUND ( 'NONE', #8868, .T. ) ;
#93524=CARTESIAN_POINT ( 'NONE',  ( 86.17777777777776294, 4.172000000000019249, 5.109226446042768454E-16 ) ) ;
#93560=EDGE_CURVE ( 'NONE', #65774, #59097, #52013, .T. ) ;
#93577=LINE ( 'NONE', #54145, #4811 ) ;
#93599=DIRECTION ( 'NONE',  ( 1.000000000000000000, 0.000000000000000000, -0.000000000000000000 ) ) ;
#93610=ORIENTED_EDGE ( 'NONE', *, *, #91949, .T. ) ;
#93631=VERTEX_POINT ( 'NONE', #82748 ) ;
#93636=EDGE_CURVE ( 'NONE', #49140, #33725, #35069, .T. ) ;
#93679=DIRECTION ( 'NONE',  ( -1.000000000000000000, -1.224606353822377258E-16, -0.000000000000000000 ) ) ;
#93697=DIRECTION ( 'NONE',  ( 1.000000000000000000, 1.224606353822377258E-16, 0.000000000000000000 ) ) ;
#93701=EDGE_CURVE ( 'NONE', #28602, #101881, #53782, .T. ) ;
#93727=CARTESIAN_POINT ( 'NONE',  ( 6.400000000000000355, 4.618802153517005848, 7.999999999999996447 ) ) ;
#93739=AXIS2_PLACEMENT_3D ( 'NONE', #53335, #6347, #86253 ) ;
#93787=AXIS2_PLACEMENT_3D ( 'NONE', #105165, #72778, #56049 ) ;
#93803=CARTESIAN_POINT ( 'NONE',  ( 0.000000000000000000, 0.000000000000000000, 5.000000000000000888 ) ) ;
#93844=DIRECTION ( 'NONE',  ( -1.000000000000000000, -1.224606353822377258E-16, -0.000000000000000000 ) ) ;
#93932=CARTESIAN_POINT ( 'NONE',  ( 6.800000000000000711, 0.000000000000000000, 0.000000000000000000 ) ) ;
#93942=VERTEX_POINT ( 'NONE', #70295 ) ;
#93961=CARTESIAN_POINT ( 'NONE',  ( 94.84444444444443434, 1.023464760207051730E-14, 0.000000000000000000 ) ) ;
#94051=ORIENTED_EDGE ( 'NONE', *, *, #55535, .F. ) ;
#94074=EDGE_CURVE ( 'NONE', #28693, #13329, #93453, .T. ) ;
#94086=DIRECTION ( 'NONE',  ( 0.000000000000000000, -1.000000000000000000, 0.000000000000000000 ) ) ;
#94104=CARTESIAN_POINT ( 'NONE',  ( 104.3757837139179117, 1.016364837396684119E-14, 0.000000000000000000 ) ) ;
#94107=CYLINDRICAL_SURFACE ( 'NONE', #15830, 5.000000000000000888 ) ;
#94120=CARTESIAN_POINT ( 'NONE',  ( 6.400000000000000355, 0.000000000000000000, 0.000000000000000000 ) ) ;
#94123=EDGE_LOOP ( 'NONE', ( #77358, #72677, #77377, #92102, #103171 ) ) ;
#94125=LINE ( 'NONE', #20293, #88065 ) ;
#94138=CARTESIAN_POINT ( 'NONE',  ( 89.93133926947346879, 5.000000000000023093, 6.123233995736781074E-16 ) ) ;
#94156=VECTOR ( 'NONE', #43300, 1000.000000000000000 ) ;
#94168=AXIS2_PLACEMENT_3D ( 'NONE', #90196, #8738, #25502 ) ;
#94209=CARTESIAN_POINT ( 'NONE',  ( 81.26467260280679739, 1.016364837396684119E-14, 0.000000000000000000 ) ) ;
#94215=CARTESIAN_POINT ( 'NONE',  ( 105.5353273971932140, 6.123233995736568081E-16, -5.000000000000011546 ) ) ;
#94228=CARTESIAN_POINT ( 'NONE',  ( 83.86866073052654258, 1.030564683017419500E-14, 0.000000000000000000 ) ) ;
#94233=AXIS2_PLACEMENT_3D ( 'NONE', #86188, #12260, #45191 ) ;
#94246=VECTOR ( 'NONE', #62577, 999.9999999999998863 ) ;
#94354=AXIS2_PLACEMENT_3D ( 'NONE', #5284, #13346, #37688 ) ;
#94407=ORIENTED_EDGE ( 'NONE', *, *, #91402, .T. ) ;
#94417=EDGE_CURVE ( 'NONE', #66540, #9203, #62376, .T. ) ;
#94428=EDGE_LOOP ( 'NONE', ( #60364, #87667, #9078, #38050, #78984, #10202 ) ) ;
#94467=DIRECTION ( 'NONE',  ( -1.000000000000000000, -1.224606353822377258E-16, -0.000000000000000000 ) ) ;
#94498=ORIENTED_EDGE ( 'NONE', *, *, #89783, .T. ) ;
#94565=CARTESIAN_POINT ( 'NONE',  ( 91.95555555555554861, 1.023464760207051730E-14, 0.000000000000000000 ) ) ;
#94570=CARTESIAN_POINT ( 'NONE',  ( 96.86866073052655679, -5.000000000000000000, 6.123233995736778115E-16 ) ) ;
#94596=AXIS2_PLACEMENT_3D ( 'NONE', #28935, #37544, #39110 ) ;
#94597=ORIENTED_EDGE ( 'NONE', *, *, #39083, .T. ) ;
#94654=FACE_OUTER_BOUND ( 'NONE', #34643, .T. ) ;
#94756=AXIS2_PLACEMENT_3D ( 'NONE', #46796, #73168, #21489 ) ;
#94797=CARTESIAN_POINT ( 'NONE',  ( 102.6464385083043283, -5.000000000000000000, 6.123233995736778115E-16 ) ) ;
#94817=CIRCLE ( 'NONE', #48282, 5.000000000000010658 ) ;
#94882=LINE ( 'NONE', #93803, #208 ) ;
#94911=ORIENTED_EDGE ( 'NONE', *, *, #22824, .F. ) ;
#94971=VECTOR ( 'NONE', #15781, 999.9999999999998863 ) ;
#95069=AXIS2_PLACEMENT_3D ( 'NONE', #78215, #62578, #21608 ) ;
#95119=EDGE_LOOP ( 'NONE', ( #64579, #20173, #93260, #31136, #34510, #101525 ) ) ;
#95139=CIRCLE ( 'NONE', #15887, 5.000000000000011546 ) ;
#95196=AXIS2_PLACEMENT_3D ( 'NONE', #73868, #106763, #33439 ) ;
#95214=ORIENTED_EDGE ( 'NONE', *, *, #5535, .F. ) ;
#95215=CARTESIAN_POINT ( 'NONE',  ( 0.000000000000000000, 0.000000000000000000, 0.000000000000000000 ) ) ;
#95235=DIRECTION ( 'NONE',  ( 0.000000000000000000, -1.000000000000000000, 0.000000000000000000 ) ) ;
#95252=ORIENTED_EDGE ( 'NONE', *, *, #29002, .T. ) ;
#95289=CARTESIAN_POINT ( 'NONE',  ( 81.26467260280679739, 1.016364837396684119E-14, 0.000000000000000000 ) ) ;
#95307=DIRECTION ( 'NONE',  ( -1.000000000000000000, -1.224606353822377258E-16, -0.000000000000000000 ) ) ;
#95311=DIRECTION ( 'NONE',  ( 0.000000000000000000, 1.000000000000000000, 0.000000000000000000 ) ) ;
#95320=CARTESIAN_POINT ( 'NONE',  ( 0.000000000000000000, 6.123233995736767268E-16, -5.000000000000000888 ) ) ;
#95333=FACE_OUTER_BOUND ( 'NONE', #13596, .T. ) ;
#95336=CARTESIAN_POINT ( 'NONE',  ( 89.06666666666666288, 1.023464760207051730E-14, 0.000000000000000000 ) ) ;
#95353=ORIENTED_EDGE ( 'NONE', *, *, #32843, .T. ) ;
#95363=EDGE_CURVE ( 'NONE', #37934, #45434, #105860, .T. ) ;
#95367=AXIS2_PLACEMENT_3D ( 'NONE', #19189, #33217, #9425 ) ;
#95373=ORIENTED_EDGE ( 'NONE', *, *, #76816, .F. ) ;
#95447=ORIENTED_EDGE ( 'NONE', *, *, #7508, .F. ) ;
#95448=EDGE_LOOP ( 'NONE', ( #29672, #6748, #2928, #97370, #32904 ) ) ;
#95508=CIRCLE ( 'NONE', #48975, 5.000000000000011546 ) ;
#95514=CIRCLE ( 'NONE', #38705, 5.000000000000010658 ) ;
#95537=CONICAL_SURFACE ( 'NONE', #16536, 4.172000000000009479, 0.9599310885968813656 ) ;
#95543=CARTESIAN_POINT ( 'NONE',  ( 80.97977184163765685, -2.002967142162725287E-29, 5.000000000000011546 ) ) ;
#95575=CARTESIAN_POINT ( 'NONE',  ( 94.26467260280679739, -2.002967142162725287E-29, 5.000000000000011546 ) ) ;
#95599=ORIENTED_EDGE ( 'NONE', *, *, #4590, .F. ) ;
#95600=DIRECTION ( 'NONE',  ( -0.5735764363510459374, -0.8191520442889919096, 0.000000000000000000 ) ) ;
#95642=AXIS2_PLACEMENT_3D ( 'NONE', #38333, #23205, #71194 ) ;
#95656=LINE ( 'NONE', #87568, #17435 ) ;
#95669=CARTESIAN_POINT ( 'NONE',  ( 85.31310517497098544, -5.000000000000000888, 6.123233995736779101E-16 ) ) ;
#95690=DIRECTION ( 'NONE',  ( 0.000000000000000000, -1.000000000000000000, 0.000000000000000000 ) ) ;
#95693=DIRECTION ( 'NONE',  ( -0.5735764363510461594, 0.8191520442889916875, 1.003171929053524870E-16 ) ) ;
#95708=EDGE_CURVE ( 'NONE', #39859, #55434, #64358, .T. ) ;
#95742=AXIS2_PLACEMENT_3D ( 'NONE', #65170, #96490, #63058 ) ;
#95770=DIRECTION ( 'NONE',  ( -1.000000000000000000, -0.000000000000000000, -0.000000000000000000 ) ) ;
#95778=ORIENTED_EDGE ( 'NONE', *, *, #15458, .T. ) ;
#95810=AXIS2_PLACEMENT_3D ( 'NONE', #73339, #38884, #24314 ) ;
#95851=CONICAL_SURFACE ( 'NONE', #21815, 5.000000000000010658, 0.9599310885968697082 ) ;
#95868=FACE_OUTER_BOUND ( 'NONE', #49886, .T. ) ;
#95902=VERTEX_POINT ( 'NONE', #11811 ) ;
#95966=CARTESIAN_POINT ( 'NONE',  ( 104.3757837139179117, 1.016364837396684119E-14, 0.000000000000000000 ) ) ;
#96031=CARTESIAN_POINT ( 'NONE',  ( 0.000000000000000000, -6.928203230275511437, -3.999999999999997335 ) ) ;
#96033=CARTESIAN_POINT ( 'NONE',  ( 101.2019940638598854, 1.030564683017419500E-14, 0.000000000000000000 ) ) ;
#96074=DIRECTION ( 'NONE',  ( 0.000000000000000000, 1.000000000000000000, 0.000000000000000000 ) ) ;
#96152=EDGE_CURVE ( 'NONE', #14501, #39221, #57304, .T. ) ;
#96179=DIRECTION ( 'NONE',  ( 1.000000000000000000, 0.000000000000000000, -0.000000000000000000 ) ) ;
#96196=LINE ( 'NONE', #79982, #101120 ) ;
#96211=EDGE_LOOP ( 'NONE', ( #73943, #22729, #85459, #31708, #94597 ) ) ;
#96222=DIRECTION ( 'NONE',  ( -1.000000000000000000, -1.224606353822377258E-16, -0.000000000000000000 ) ) ;
#96240=CARTESIAN_POINT ( 'NONE',  ( 0.08285530294364995552, 1.570896314703521091, -8.000000000000000000 ) ) ;
#96254=CARTESIAN_POINT ( 'NONE',  ( 93.97977184163765685, 5.000000000000020428, 0.000000000000000000 ) ) ;
#96270=AXIS2_PLACEMENT_3D ( 'NONE', #46546, #12043, #30387 ) ;
#96285=FACE_OUTER_BOUND ( 'NONE', #73726, .T. ) ;
#96303=ORIENTED_EDGE ( 'NONE', *, *, #3212, .F. ) ;
#96310=CONICAL_SURFACE ( 'NONE', #86005, 4.172000000000009479, 0.9599310885968813656 ) ;
#96321=LINE ( 'NONE', #38619, #15923 ) ;
#96377=DIRECTION ( 'NONE',  ( -1.000000000000000000, -1.224606353822377258E-16, -0.000000000000000000 ) ) ;
#96400=EDGE_LOOP ( 'NONE', ( #16851, #20891, #99513, #31777, #55420 ) ) ;
#96403=ORIENTED_EDGE ( 'NONE', *, *, #16924, .T. ) ;
#96490=DIRECTION ( 'NONE',  ( -1.000000000000000000, -1.224606353822377258E-16, -0.000000000000000000 ) ) ;
#96539=CONICAL_SURFACE ( 'NONE', #10443, 5.000000000000010658, 0.9599310885968697082 ) ;
#96550=CARTESIAN_POINT ( 'NONE',  ( 98.31310517497099966, 1.030564683017419500E-14, 0.000000000000000000 ) ) ;
#96552=DIRECTION ( 'NONE',  ( 0.000000000000000000, -1.000000000000000000, 0.000000000000000000 ) ) ;
#96562=FACE_OUTER_BOUND ( 'NONE', #74976, .T. ) ;
#96585=ORIENTED_EDGE ( 'NONE', *, *, #63092, .F. ) ;
#96603=EDGE_CURVE ( 'NONE', #98133, #64587, #50555, .T. ) ;
#96606=CARTESIAN_POINT ( 'NONE',  ( 0.000000000000000000, 6.123233995736767268E-16, -5.000000000000000888 ) ) ;
#96649=CARTESIAN_POINT ( 'NONE',  ( 88.48689482502902592, 5.000000000000023093, 6.123233995736781074E-16 ) ) ;
#96655=ADVANCED_FACE ( 'NONE', ( #101271 ), #36041, .T. ) ;
#96691=ORIENTED_EDGE ( 'NONE', *, *, #14814, .T. ) ;
#96738=CYLINDRICAL_SURFACE ( 'NONE', #40697, 8.000000000000000000 ) ;
#96741=CARTESIAN_POINT ( 'NONE',  ( 86.75754961941542831, -5.000000000000000000, 6.123233995736778115E-16 ) ) ;
#96767=AXIS2_PLACEMENT_3D ( 'NONE', #78449, #29415, #5624 ) ;
#96800=DIRECTION ( 'NONE',  ( 0.000000000000000000, -1.000000000000000000, 0.000000000000000000 ) ) ;
#96824=FACE_OUTER_BOUND ( 'NONE', #96400, .T. ) ;
#96837=EDGE_CURVE ( 'NONE', #55179, #75948, #8336, .T. ) ;
#96849=ORIENTED_EDGE ( 'NONE', *, *, #511, .T. ) ;
#96866=CARTESIAN_POINT ( 'NONE',  ( 85.59800593614014019, 1.016364837396684119E-14, 0.000000000000000000 ) ) ;
#96926=CARTESIAN_POINT ( 'NONE',  ( 106.4000000000000057, 0.000000000000000000, 0.000000000000000000 ) ) ;
#96945=EDGE_LOOP ( 'NONE', ( #3918, #73476, #16366 ) ) ;
#96961=ORIENTED_EDGE ( 'NONE', *, *, #67743, .F. ) ;
#97019=EDGE_LOOP ( 'NONE', ( #26055, #70696, #2894, #80101, #103647 ) ) ;
#97033=VERTEX_POINT ( 'NONE', #64993 ) ;
#97077=EDGE_LOOP ( 'NONE', ( #41457, #62514, #104126, #100097, #30751, #33133 ) ) ;
#97098=ORIENTED_EDGE ( 'NONE', *, *, #50933, .F. ) ;
#97103=DIRECTION ( 'NONE',  ( 0.000000000000000000, -1.000000000000000000, 0.000000000000000000 ) ) ;
#97116=LINE ( 'NONE', #96606, #3874 ) ;
#97139=CARTESIAN_POINT ( 'NONE',  ( 83.28888888888889142, 4.172000000000019249, 5.109226446042768454E-16 ) ) ;
#97200=EDGE_LOOP ( 'NONE', ( #81347, #11427, #82785, #62374, #85048, #101409 ) ) ;
#97203=ORIENTED_EDGE ( 'NONE', *, *, #16762, .F. ) ;
#97241=DIRECTION ( 'NONE',  ( -1.000000000000000000, -1.224606353822377258E-16, -0.000000000000000000 ) ) ;
#97251=DIRECTION ( 'NONE',  ( -1.000000000000000000, -0.000000000000000000, -0.000000000000000000 ) ) ;
#97272=ORIENTED_EDGE ( 'NONE', *, *, #81833, .T. ) ;
#97276=DIRECTION ( 'NONE',  ( 0.000000000000000000, -1.000000000000000000, 0.000000000000000000 ) ) ;
#97323=CARTESIAN_POINT ( 'NONE',  ( 96.28888888888889142, 4.172000000000019249, 5.109226446042768454E-16 ) ) ;
#97328=ORIENTED_EDGE ( 'NONE', *, *, #10775, .T. ) ;
#97357=ORIENTED_EDGE ( 'NONE', *, *, #71551, .T. ) ;
#97370=ORIENTED_EDGE ( 'NONE', *, *, #81227, .F. ) ;
#97423=EDGE_LOOP ( 'NONE', ( #98641, #64757, #57011, #90750, #34464, #3749 ) ) ;
#97426=ORIENTED_EDGE ( 'NONE', *, *, #83507, .T. ) ;
#97429=CARTESIAN_POINT ( 'NONE',  ( 79.82022815836235452, 1.016364837396684119E-14, 0.000000000000000000 ) ) ;
#97444=CONICAL_SURFACE ( 'NONE', #7908, 5.000000000000010658, 0.9599310885968697082 ) ;
#97462=CIRCLE ( 'NONE', #37158, 5.000000000000010658 ) ;
#97495=DIRECTION ( 'NONE',  ( 0.000000000000000000, 0.000000000000000000, -1.000000000000000000 ) ) ;
#97523=AXIS2_PLACEMENT_3D ( 'NONE', #22267, #37931, #13063 ) ;
#97543=ADVANCED_FACE ( 'NONE', ( #13913 ), #98863, .T. ) ;
#97594=ORIENTED_EDGE ( 'NONE', *, *, #90378, .F. ) ;
#97601=CONICAL_SURFACE ( 'NONE', #35683, 5.000000000000010658, 0.9599310885968697082 ) ;
#97637=AXIS2_PLACEMENT_3D ( 'NONE', #11639, #9506, #3571 ) ;
#97680=EDGE_CURVE ( 'NONE', #43584, #92586, #18208, .T. ) ;
#97685=EDGE_CURVE ( 'NONE', #80260, #4508, #7564, .T. ) ;
#97686=CYLINDRICAL_SURFACE ( 'NONE', #64611, 5.000000000000000888 ) ;
#97726=ORIENTED_EDGE ( 'NONE', *, *, #75342, .F. ) ;
#97741=EDGE_CURVE ( 'NONE', #88742, #74576, #30022, .T. ) ;
#97762=CARTESIAN_POINT ( 'NONE',  ( 0.000000000000000000, 0.000000000000000000, 5.000000000000000888 ) ) ;
#97791=ORIENTED_EDGE ( 'NONE', *, *, #34273, .T. ) ;
#97793=AXIS2_PLACEMENT_3D ( 'NONE', #95215, #27863, #86609 ) ;
#97800=CARTESIAN_POINT ( 'NONE',  ( 0.000000000000000000, 1.502314598737159228E-15, -8.000000000000000000 ) ) ;
#97811=AXIS2_PLACEMENT_3D ( 'NONE', #89498, #14513, #22125 ) ;
#97836=EDGE_LOOP ( 'NONE', ( #105641, #15580, #59013, #88821, #5339 ) ) ;
#97868=CARTESIAN_POINT ( 'NONE',  ( 100.0424503805845831, 1.016364837396684119E-14, 0.000000000000000000 ) ) ;
#97894=DIRECTION ( 'NONE',  ( 0.000000000000000000, 1.000000000000000000, 0.000000000000000000 ) ) ;
#97916=CIRCLE ( 'NONE', #47929, 5.000000000000010658 ) ;
#97943=CARTESIAN_POINT ( 'NONE',  ( 93.97977184163765685, -5.000000000000000000, 6.123233995736778115E-16 ) ) ;
#97951=DIRECTION ( 'NONE',  ( -1.000000000000000000, -1.224606353822377258E-16, -0.000000000000000000 ) ) ;
#97960=DIRECTION ( 'NONE',  ( 0.000000000000000000, 0.000000000000000000, 1.000000000000000000 ) ) ;
#97967=AXIS2_PLACEMENT_3D ( 'NONE', #10971, #92425, #50898 ) ;
#97982=DIRECTION ( 'NONE',  ( 0.000000000000000000, -1.000000000000000000, 0.000000000000000000 ) ) ;
#98042=DIRECTION ( 'NONE',  ( -1.000000000000000000, -1.224606353822377258E-16, -0.000000000000000000 ) ) ;
#98048=CARTESIAN_POINT ( 'NONE',  ( 0.000000000000000000, 0.000000000000000000, 0.000000000000000000 ) ) ;
#98133=VERTEX_POINT ( 'NONE', #75624 ) ;
#98148=DIRECTION ( 'NONE',  ( 0.000000000000000000, -1.000000000000000000, 0.000000000000000000 ) ) ;
#98176=EDGE_CURVE ( 'NONE', #92586, #34646, #21465, .T. ) ;
#98203=ORIENTED_EDGE ( 'NONE', *, *, #81227, .T. ) ;
#98205=EDGE_CURVE ( 'NONE', #17856, #73615, #53486, .T. ) ;
#98255=CARTESIAN_POINT ( 'NONE',  ( 105.5720000000000312, 0.000000000000000000, 0.000000000000000000 ) ) ;
#98289=EDGE_LOOP ( 'NONE', ( #91096, #51738, #13876, #66401, #1982 ) ) ;
#98378=ORIENTED_EDGE ( 'NONE', *, *, #85655, .F. ) ;
#98401=FACE_OUTER_BOUND ( 'NONE', #86851, .T. ) ;
#98439=CIRCLE ( 'NONE', #95069, 5.000000000000000888 ) ;
#98448=CARTESIAN_POINT ( 'NONE',  ( 6.400000000000000355, -4.618802153516994302, 8.000000000000000000 ) ) ;
#98467=ORIENTED_EDGE ( 'NONE', *, *, #46957, .T. ) ;
#98472=CIRCLE ( 'NONE', #50203, 5.000000000000011546 ) ;
#98494=FACE_OUTER_BOUND ( 'NONE', #85869, .T. ) ;
#98530=EDGE_CURVE ( 'NONE', #36517, #75948, #95508, .T. ) ;
#98587=FACE_OUTER_BOUND ( 'NONE', #81340, .T. ) ;
#98641=ORIENTED_EDGE ( 'NONE', *, *, #71551, .F. ) ;
#98694=CARTESIAN_POINT ( 'NONE',  ( 92.82022815836235452, 1.016364837396684119E-14, 0.000000000000000000 ) ) ;
#98700=AXIS2_PLACEMENT_3D ( 'NONE', #66857, #41507, #98148 ) ;
#98709=B_SPLINE_CURVE_WITH_KNOTS ( 'NONE', 3,
 ( #105837, #31981, #41117, #90733, #33571, #607 ),
 .UNSPECIFIED., .F., .F.,
 ( 4, 2, 4 ),
 ( 2.380731631042988191E-07, 0.002336973833157631863, 0.004673709593152160051 ),
 .UNSPECIFIED. ) ;
#98747=LINE ( 'NONE', #42654, #8397 ) ;
#98749=CARTESIAN_POINT ( 'NONE',  ( 0.3173508448886524502, 5.375634714784618851, -6.689127551062007626 ) ) ;
#98762=CARTESIAN_POINT ( 'NONE',  ( 5.799999999999999822, -9.237604307034013473, 7.924929828396943928E-16 ) ) ;
#98806=ORIENTED_EDGE ( 'NONE', *, *, #90378, .T. ) ;
#98807=CARTESIAN_POINT ( 'NONE',  ( 93.97977184163765685, 6.123233995736568081E-16, -5.000000000000011546 ) ) ;
#98847=CARTESIAN_POINT ( 'NONE',  ( 82.70911704725124025, -5.000000000000000000, 0.000000000000000000 ) ) ;
#98863=CONICAL_SURFACE ( 'NONE', #93739, 4.171999999999999709, 0.7853981633974603804 ) ;
#98871=ORIENTED_EDGE ( 'NONE', *, *, #89092, .T. ) ;
#98887=FACE_OUTER_BOUND ( 'NONE', #3526, .T. ) ;
#98908=ORIENTED_EDGE ( 'NONE', *, *, #101267, .T. ) ;
#98915=DIRECTION ( 'NONE',  ( 0.000000000000000000, 1.000000000000000000, 0.000000000000000000 ) ) ;
#98923=DIRECTION ( 'NONE',  ( 0.000000000000000000, -1.000000000000000000, 0.000000000000000000 ) ) ;
#98924=ORIENTED_EDGE ( 'NONE', *, *, #8535, .F. ) ;
#99076=CIRCLE ( 'NONE', #61157, 5.000000000000010658 ) ;
#99147=EDGE_CURVE ( 'NONE', #32237, #58039, #33702, .T. ) ;
#99175=DIRECTION ( 'NONE',  ( 0.000000000000000000, -1.000000000000000000, 0.000000000000000000 ) ) ;
#99222=CARTESIAN_POINT ( 'NONE',  ( 80.97977184163765685, 1.030564683017419500E-14, 0.000000000000000000 ) ) ;
#99224=LINE ( 'NONE', #9153, #66990 ) ;
#99248=EDGE_LOOP ( 'NONE', ( #51774, #63650, #81496, #97328, #44331, #37237 ) ) ;
#99252=DIRECTION ( 'NONE',  ( -1.000000000000000000, -0.000000000000000000, -0.000000000000000000 ) ) ;
#99274=AXIS2_PLACEMENT_3D ( 'NONE', #76583, #100864, #35647 ) ;
#99275=DIRECTION ( 'NONE',  ( 0.000000000000000000, -1.000000000000000000, 0.000000000000000000 ) ) ;
#99312=DIRECTION ( 'NONE',  ( 0.000000000000000000, 0.000000000000000000, 1.000000000000000000 ) ) ;
#99318=LINE ( 'NONE', #25492, #49085 ) ;
#99365=CIRCLE ( 'NONE', #87398, 5.000000000000010658 ) ;
#99382=CARTESIAN_POINT ( 'NONE',  ( 0.000000000000000000, 0.000000000000000000, 0.000000000000000000 ) ) ;
#99388=AXIS2_PLACEMENT_3D ( 'NONE', #88974, #40414, #82472 ) ;
#99401=CARTESIAN_POINT ( 'NONE',  ( 105.5720000000000312, 0.000000000000000000, 0.000000000000000000 ) ) ;
#99419=DIRECTION ( 'NONE',  ( 0.000000000000000000, 0.000000000000000000, -1.000000000000000000 ) ) ;
#99460=DIRECTION ( 'NONE',  ( 0.5735764363510557073, -0.8191520442889850262, 1.003171929053516612E-16 ) ) ;
#99475=ORIENTED_EDGE ( 'NONE', *, *, #5169, .F. ) ;
#99476=VECTOR ( 'NONE', #99460, 1000.000000000000000 ) ;
#99513=ORIENTED_EDGE ( 'NONE', *, *, #7664, .F. ) ;
#99558=VERTEX_POINT ( 'NONE', #105751 ) ;
#99598=VECTOR ( 'NONE', #29457, 1000.000000000000000 ) ;
#99629=CARTESIAN_POINT ( 'NONE',  ( 87.62222222222222001, -4.171999999999998820, 5.616230220889773285E-16 ) ) ;
#99745=CIRCLE ( 'NONE', #97967, 4.172000000000009479 ) ;
#99777=EDGE_CURVE ( 'NONE', #22089, #13365, #33773, .T. ) ;
#99798=AXIS2_PLACEMENT_3D ( 'NONE', #17552, #59601, #67685 ) ;
#99877=CARTESIAN_POINT ( 'NONE',  ( 102.9313392694734688, 1.016364837396684119E-14, 0.000000000000000000 ) ) ;
#99909=ADVANCED_FACE ( 'NONE', ( #2021 ), #17698, .T. ) ;
#99942=AXIS2_PLACEMENT_3D ( 'NONE', #16844, #15767, #48121 ) ;
#99968=VERTEX_POINT ( 'NONE', #14261 ) ;
#99971=FACE_OUTER_BOUND ( 'NONE', #70959, .T. ) ;
#99986=ADVANCED_FACE ( 'NONE', ( #96285 ), #100875, .T. ) ;
#99990=CARTESIAN_POINT ( 'NONE',  ( 0.000000000000000000, 3.004629197474323585E-15, 8.000000000000000000 ) ) ;
#100043=( LENGTH_UNIT ( ) NAMED_UNIT ( * ) SI_UNIT ( .MILLI., .METRE. ) );
#100071=DIRECTION ( 'NONE',  ( 0.000000000000000000, 0.000000000000000000, 1.000000000000000000 ) ) ;
#100097=ORIENTED_EDGE ( 'NONE', *, *, #60812, .T. ) ;
#100099=CONICAL_SURFACE ( 'NONE', #7085, 4.172000000000009479, 0.9599310885968813656 ) ;
#100178=AXIS2_PLACEMENT_3D ( 'NONE', #23647, #88893, #22056 ) ;
#100184=EDGE_CURVE ( 'NONE', #20613, #41052, #64777, .T. ) ;
#100200=ORIENTED_EDGE ( 'NONE', *, *, #78304, .F. ) ;
#100248=DIRECTION ( 'NONE',  ( -1.000000000000000000, -1.224606353822377258E-16, -0.000000000000000000 ) ) ;
#100255=AXIS2_PLACEMENT_3D ( 'NONE', #1731, #74033, #83712 ) ;
#100258=DIRECTION ( 'NONE',  ( -0.000000000000000000, 0.8660254037844388186, 0.4999999999999996114 ) ) ;
#100277=DIRECTION ( 'NONE',  ( 0.000000000000000000, -1.000000000000000000, 0.000000000000000000 ) ) ;
#100379=EDGE_CURVE ( 'NONE', #6367, #104741, #44156, .T. ) ;
#100388=B_SPLINE_CURVE_WITH_KNOTS ( 'NONE', 3,
 ( #58028, #1372, #34338, #81758, #57488, #16516, #49402, #82311 ),
 .UNSPECIFIED., .F., .F.,
 ( 4, 2, 2, 4 ),
 ( 0.004673709593152165255, 0.005837709341827652942, 0.007001709090503139762, 0.009329708587854115137 ),
 .UNSPECIFIED. ) ;
#100425=CARTESIAN_POINT ( 'NONE',  ( 85.31310517497098544, 1.030564683017419500E-14, 0.000000000000000000 ) ) ;
#100436=EDGE_CURVE ( 'NONE', #16299, #22473, #59635, .T. ) ;
#100459=EDGE_LOOP ( 'NONE', ( #98924, #40609, #97594, #100200, #52780, #103821 ) ) ;
#100481=DIRECTION ( 'NONE',  ( 0.000000000000000000, -1.000000000000000000, 0.000000000000000000 ) ) ;
#100493=ORIENTED_EDGE ( 'NONE', *, *, #25364, .F. ) ;
#100510=CIRCLE ( 'NONE', #35103, 5.000000000000011546 ) ;
#100534=AXIS2_PLACEMENT_3D ( 'NONE', #30358, #102095, #61124 ) ;
#100559=DIRECTION ( 'NONE',  ( 0.000000000000000000, 1.000000000000000000, 0.000000000000000000 ) ) ;
#100568=DIRECTION ( 'NONE',  ( 0.000000000000000000, -1.000000000000000000, 0.000000000000000000 ) ) ;
#100618=CONICAL_SURFACE ( 'NONE', #73037, 5.000000000000010658, 0.9599310885968697082 ) ;
#100620=LINE ( 'NONE', #26256, #34383 ) ;
#100651=CARTESIAN_POINT ( 'NONE',  ( 91.09088295274877112, 1.030564683017419500E-14, 0.000000000000000000 ) ) ;
#100656=EDGE_LOOP ( 'NONE', ( #36607, #6561, #98203, #7663, #94498 ) ) ;
#100683=FACE_OUTER_BOUND ( 'NONE', #72887, .T. ) ;
#100704=DIRECTION ( 'NONE',  ( -1.000000000000000000, -0.000000000000000000, -0.000000000000000000 ) ) ;
#100721=DIRECTION ( 'NONE',  ( 0.5735764363510554853, 0.8191520442889852482, 0.000000000000000000 ) ) ;
#100766=DIRECTION ( 'NONE',  ( 0.5735764363510554853, 0.8191520442889852482, 0.000000000000000000 ) ) ;
#100864=DIRECTION ( 'NONE',  ( -1.000000000000000000, -1.224606353822377258E-16, -0.000000000000000000 ) ) ;
#100872=ORIENTED_EDGE ( 'NONE', *, *, #68947, .F. ) ;
#100875=CONICAL_SURFACE ( 'NONE', #7864, 4.172000000000009479, 0.9599310885968813656 ) ;
#100880=VERTEX_POINT ( 'NONE', #25889 ) ;
#100882=CARTESIAN_POINT ( 'NONE',  ( 83.86866073052654258, -2.002967142162725287E-29, 5.000000000000011546 ) ) ;
#100961=CARTESIAN_POINT ( 'NONE',  ( 102.6464385083043283, 1.030564683017419500E-14, 0.000000000000000000 ) ) ;
#100963=CARTESIAN_POINT ( 'NONE',  ( 5.799999999999999822, 0.000000000000000000, 0.000000000000000000 ) ) ;
#100970=PRESENTATION_STYLE_ASSIGNMENT (( #68079 ) ) ;
#100977=EDGE_CURVE ( 'NONE', #15530, #17856, #23543, .T. ) ;
#100981=CARTESIAN_POINT ( 'NONE',  ( 81.84444444444444855, 4.172000000000019249, 5.109226446042768454E-16 ) ) ;
#101024=ORIENTED_EDGE ( 'NONE', *, *, #68209, .T. ) ;
#101098=ORIENTED_EDGE ( 'NONE', *, *, #27054, .F. ) ;
#101120=VECTOR ( 'NONE', #70850, 1000.000000000000114 ) ;
#101128=ADVANCED_FACE ( 'NONE', ( #85563 ), #25395, .T. ) ;
#101163=AXIS2_PLACEMENT_3D ( 'NONE', #94104, #4036, #61219 ) ;
#101203=CARTESIAN_POINT ( 'NONE',  ( 82.70911704725124025, 1.016364837396684119E-14, 0.000000000000000000 ) ) ;
#101237=CARTESIAN_POINT ( 'NONE',  ( 104.3757837139179117, 1.016364837396684119E-14, 0.000000000000000000 ) ) ;
#101241=VERTEX_POINT ( 'NONE', #55934 ) ;
#101267=EDGE_CURVE ( 'NONE', #93631, #42388, #87820, .T. ) ;
#101271=FACE_OUTER_BOUND ( 'NONE', #32644, .T. ) ;
#101297=VECTOR ( 'NONE', #8641, 1000.000000000000000 ) ;
#101302=B_SPLINE_CURVE_WITH_KNOTS ( 'NONE', 3,
 ( #13885, #55405, #46802, #79695, #5804, #38727 ),
 .UNSPECIFIED., .F., .F.,
 ( 4, 2, 4 ),
 ( 0.02753256083616405225, 0.02987018135583073206, 0.03220780187549741186 ),
 .UNSPECIFIED. ) ;
#101328=DIRECTION ( 'NONE',  ( -1.000000000000000000, -1.224606353822377258E-16, -0.000000000000000000 ) ) ;
#101334=CARTESIAN_POINT ( 'NONE',  ( 6.400000000000000355, -4.618802153517009401, -8.000000000000001776 ) ) ;
#101368=CARTESIAN_POINT ( 'NONE',  ( 99.75754961941544252, 1.030564683017419500E-14, 0.000000000000000000 ) ) ;
#101409=ORIENTED_EDGE ( 'NONE', *, *, #4552, .F. ) ;
#101411=CARTESIAN_POINT ( 'NONE',  ( 80.97977184163765685, -5.000000000000000888, 6.123233995736779101E-16 ) ) ;
#101454=DIRECTION ( 'NONE',  ( 0.000000000000000000, 0.000000000000000000, -1.000000000000000000 ) ) ;
#101490=DIRECTION ( 'NONE',  ( -1.000000000000000000, -1.224606353822377258E-16, -0.000000000000000000 ) ) ;
#101514=ADVANCED_FACE ( 'NONE', ( #32666 ), #49446, .T. ) ;
#101525=ORIENTED_EDGE ( 'NONE', *, *, #60812, .F. ) ;
#101534=AXIS2_PLACEMENT_3D ( 'NONE', #83859, #66616, #59070 ) ;
#101568=DIRECTION ( 'NONE',  ( 0.000000000000000000, -1.000000000000000000, 0.000000000000000000 ) ) ;
#101620=DIRECTION ( 'NONE',  ( 0.000000000000000000, -1.000000000000000000, 0.000000000000000000 ) ) ;
#101627=ORIENTED_EDGE ( 'NONE', *, *, #86606, .T. ) ;
#101645=CARTESIAN_POINT ( 'NONE',  ( 101.4868948250290259, 5.000000000000023093, 6.123233995736781074E-16 ) ) ;
#101646=EDGE_CURVE ( 'NONE', #65096, #25050, #87350, .T. ) ;
#101686=CIRCLE ( 'NONE', #13820, 5.000000000000010658 ) ;
#101711=ORIENTED_EDGE ( 'NONE', *, *, #87628, .F. ) ;
#101734=EDGE_CURVE ( 'NONE', #82760, #92683, #96196, .T. ) ;
#101758=CARTESIAN_POINT ( 'NONE',  ( 5.799999999999999822, -9.237604307034013473, 7.924929828396943928E-16 ) ) ;
#101766=AXIS2_PLACEMENT_3D ( 'NONE', #44540, #86610, #77430 ) ;
#101774=VERTEX_POINT ( 'NONE', #12593 ) ;
#101816=ORIENTED_EDGE ( 'NONE', *, *, #33785, .T. ) ;
#101822=CARTESIAN_POINT ( 'NONE',  ( 101.2019940638598854, 1.030564683017419500E-14, 0.000000000000000000 ) ) ;
#101837=PRODUCT ( 'hex bolt gradeab_iso_ISO 4014 - M10 x 100 x 26-S', 'hex bolt gradeab_iso_ISO 4014 - M10 x 100 x 26-S', '', ( #48172 ) ) ;
#101847=DIRECTION ( 'NONE',  ( 0.000000000000000000, -0.5000000000000008882, 0.8660254037844381525 ) ) ;
#101876=ORIENTED_EDGE ( 'NONE', *, *, #17436, .F. ) ;
#101881=VERTEX_POINT ( 'NONE', #53075 ) ;
#101882=CARTESIAN_POINT ( 'NONE',  ( 0.4964154566687890013, 4.996589667937374912, 7.345652830558757174 ) ) ;
#101891=VERTEX_POINT ( 'NONE', #41131 ) ;
#101917=ORIENTED_EDGE ( 'NONE', *, *, #103398, .F. ) ;
#101941=CIRCLE ( 'NONE', #22753, 5.000000000000011546 ) ;
#101982=CARTESIAN_POINT ( 'NONE',  ( 104.0908829527487711, 1.030564683017419500E-14, 0.000000000000000000 ) ) ;
#101996=CARTESIAN_POINT ( 'NONE',  ( 85.31310517497098544, -2.002967142162725287E-29, 5.000000000000011546 ) ) ;
#101997=DIRECTION ( 'NONE',  ( -1.000000000000000000, -0.000000000000000000, -0.000000000000000000 ) ) ;
#102006=VERTEX_POINT ( 'NONE', #621 ) ;
#102009=FACE_OUTER_BOUND ( 'NONE', #83294, .T. ) ;
#102042=ORIENTED_EDGE ( 'NONE', *, *, #55610, .T. ) ;
#102054=ORIENTED_EDGE ( 'NONE', *, *, #32843, .F. ) ;
#102072=DIRECTION ( 'NONE',  ( -1.000000000000000000, -1.224606353822377258E-16, -0.000000000000000000 ) ) ;
#102095=DIRECTION ( 'NONE',  ( -1.000000000000000000, -0.000000000000000000, -0.000000000000000000 ) ) ;
#102101=DIRECTION ( 'NONE',  ( 0.000000000000000000, 0.000000000000000000, 1.000000000000000000 ) ) ;
#102121=DIRECTION ( 'NONE',  ( 0.000000000000000000, -1.000000000000000000, 0.000000000000000000 ) ) ;
#102191=ADVANCED_FACE ( 'NONE', ( #62321 ), #77958, .T. ) ;
#102233=ORIENTED_EDGE ( 'NONE', *, *, #54405, .F. ) ;
#102295=ORIENTED_EDGE ( 'NONE', *, *, #63165, .F. ) ;
#102307=ORIENTED_EDGE ( 'NONE', *, *, #59267, .T. ) ;
#102339=VERTEX_POINT ( 'NONE', #100882 ) ;
#102376=VERTEX_POINT ( 'NONE', #37279 ) ;
#102412=CIRCLE ( 'NONE', #9378, 5.000000000000010658 ) ;
#102416=EDGE_CURVE ( 'NONE', #54959, #16922, #82523, .T. ) ;
#102450=ORIENTED_EDGE ( 'NONE', *, *, #102460, .T. ) ;
#102460=EDGE_CURVE ( 'NONE', #45219, #34210, #79571, .T. ) ;
#102505=ORIENTED_EDGE ( 'NONE', *, *, #31850, .T. ) ;
#102573=DIRECTION ( 'NONE',  ( -1.000000000000000000, -0.000000000000000000, -0.000000000000000000 ) ) ;
#102598=DIRECTION ( 'NONE',  ( 0.000000000000000000, -1.000000000000000000, 0.000000000000000000 ) ) ;
#102604=CARTESIAN_POINT ( 'NONE',  ( 0.7145311798163234140, -9.237604307034013473, 6.198474679904167468E-16 ) ) ;
#102648=CARTESIAN_POINT ( 'NONE',  ( 0.000000000000000000, 6.123233995736767268E-16, -5.000000000000000888 ) ) ;
#102684=VERTEX_POINT ( 'NONE', #12575 ) ;
#102686=EDGE_CURVE ( 'NONE', #101241, #89169, #12050, .T. ) ;
#102692=CIRCLE ( 'NONE', #56135, 5.000000000000011546 ) ;
#102716=CIRCLE ( 'NONE', #23523, 0.4000000000000001887 ) ;
#102722=CARTESIAN_POINT ( 'NONE',  ( 96.28888888888889142, 1.023464760207051730E-14, 0.000000000000000000 ) ) ;
#102725=AXIS2_PLACEMENT_3D ( 'NONE', #9798, #42714, #51320 ) ;
#102731=EDGE_CURVE ( 'NONE', #64937, #71316, #20746, .T. ) ;
#102752=EDGE_CURVE ( 'NONE', #34646, #79234, #106685, .T. ) ;
#102785=ORIENTED_EDGE ( 'NONE', *, *, #93560, .T. ) ;
#102796=ORIENTED_EDGE ( 'NONE', *, *, #1218, .T. ) ;
#102863=VECTOR ( 'NONE', #105666, 1000.000000000000000 ) ;
#102876=ORIENTED_EDGE ( 'NONE', *, *, #105684, .T. ) ;
#102885=CARTESIAN_POINT ( 'NONE',  ( 99.75754961941544252, 1.030564683017419500E-14, 0.000000000000000000 ) ) ;
#102895=CARTESIAN_POINT ( 'NONE',  ( 5.799999999999999822, 8.000000000000000000, 0.000000000000000000 ) ) ;
#102932=ADVANCED_FACE ( 'NONE', ( #28025 ), #12841, .T. ) ;
#103017=LINE ( 'NONE', #62047, #90852 ) ;
#103032=DIRECTION ( 'NONE',  ( -1.000000000000000000, -0.000000000000000000, -0.000000000000000000 ) ) ;
#103094=CIRCLE ( 'NONE', #37681, 5.000000000000011546 ) ;
#103102=ORIENTED_EDGE ( 'NONE', *, *, #29002, .F. ) ;
#103107=ORIENTED_EDGE ( 'NONE', *, *, #45550, .F. ) ;
#103119=AXIS2_PLACEMENT_3D ( 'NONE', #10802, #68000, #99275 ) ;
#103125=ADVANCED_FACE ( 'NONE', ( #48920 ), #96539, .T. ) ;
#103155=CIRCLE ( 'NONE', #85930, 5.000000000000010658 ) ;
#103171=ORIENTED_EDGE ( 'NONE', *, *, #86113, .T. ) ;
#103250=DIRECTION ( 'NONE',  ( -0.5735764363510461594, 0.8191520442889916875, 1.003171929053524870E-16 ) ) ;
#103282=DIRECTION ( 'NONE',  ( -1.000000000000000000, -1.224606353822377258E-16, -0.000000000000000000 ) ) ;
#103283=ORIENTED_EDGE ( 'NONE', *, *, #11649, .F. ) ;
#103344=CARTESIAN_POINT ( 'NONE',  ( 89.64643850830432825, 1.030564683017419500E-14, 0.000000000000000000 ) ) ;
#103356=AXIS2_PLACEMENT_3D ( 'NONE', #96550, #40960, #73849 ) ;
#103390=DIRECTION ( 'NONE',  ( 0.000000000000000000, -1.000000000000000000, 0.000000000000000000 ) ) ;
#103398=EDGE_CURVE ( 'NONE', #86608, #102376, #43520, .T. ) ;
#103410=DIRECTION ( 'NONE',  ( 0.000000000000000000, 1.000000000000000000, 0.000000000000000000 ) ) ;
#103413=ORIENTED_EDGE ( 'NONE', *, *, #33, .F. ) ;
#103445=DIRECTION ( 'NONE',  ( 0.000000000000000000, 1.000000000000000000, 0.000000000000000000 ) ) ;
#103451=EDGE_CURVE ( 'NONE', #36922, #67654, #75966, .T. ) ;
#103452=ORIENTED_EDGE ( 'NONE', *, *, #3134, .T. ) ;
#103463=CARTESIAN_POINT ( 'NONE',  ( 5.799999999999999822, 8.000000000000000000, 0.000000000000000000 ) ) ;
#103560=DIRECTION ( 'NONE',  ( 0.000000000000000000, -1.000000000000000000, 0.000000000000000000 ) ) ;
#103622=DIRECTION ( 'NONE',  ( -1.000000000000000000, -0.000000000000000000, -0.000000000000000000 ) ) ;
#103627=ORIENTED_EDGE ( 'NONE', *, *, #94417, .T. ) ;
#103645=LINE ( 'NONE', #22227, #67035 ) ;
#103647=ORIENTED_EDGE ( 'NONE', *, *, #5285, .F. ) ;
#103659=CARTESIAN_POINT ( 'NONE',  ( 0.08224679563971286356, -7.710515798486365036, -2.644994884459105577 ) ) ;
#103698=CARTESIAN_POINT ( 'NONE',  ( 5.799999999999999822, 4.618802153517003184, -8.000000000000000000 ) ) ;
#103699=CARTESIAN_POINT ( 'NONE',  ( 104.0908829527487711, 5.000000000000020428, 0.000000000000000000 ) ) ;
#103777=ORIENTED_EDGE ( 'NONE', *, *, #55416, .T. ) ;
#103792=DIRECTION ( 'NONE',  ( -1.000000000000000000, -0.000000000000000000, -0.000000000000000000 ) ) ;
#103821=ORIENTED_EDGE ( 'NONE', *, *, #46663, .F. ) ;
#103827=CARTESIAN_POINT ( 'NONE',  ( 82.42421628608209971, 1.030564683017419500E-14, 0.000000000000000000 ) ) ;
#103850=DIRECTION ( 'NONE',  ( -1.000000000000000000, -1.224606353822377258E-16, -0.000000000000000000 ) ) ;
#103891=AXIS2_PLACEMENT_3D ( 'NONE', #27398, #43004, #51611 ) ;
#103908=CARTESIAN_POINT ( 'NONE',  ( 92.53532739719321398, 1.030564683017419500E-14, 0.000000000000000000 ) ) ;
#103910=FACE_OUTER_BOUND ( 'NONE', #37406, .T. ) ;
#103920=DIRECTION ( 'NONE',  ( 0.000000000000000000, -1.000000000000000000, 0.000000000000000000 ) ) ;
#103929=AXIS2_PLACEMENT_3D ( 'NONE', #50487, #83399, #9497 ) ;
#104012=CIRCLE ( 'NONE', #45445, 5.000000000000010658 ) ;
#104083=VECTOR ( 'NONE', #56412, 1000.000000000000000 ) ;
#104126=ORIENTED_EDGE ( 'NONE', *, *, #77519, .T. ) ;
#104169=ORIENTED_EDGE ( 'NONE', *, *, #45581, .T. ) ;
#104209=VERTEX_POINT ( 'NONE', #28603 ) ;
#104225=DIRECTION ( 'NONE',  ( 0.000000000000000000, 0.000000000000000000, -1.000000000000000000 ) ) ;
#104297=CARTESIAN_POINT ( 'NONE',  ( 101.4868948250290259, 1.016364837396684119E-14, 0.000000000000000000 ) ) ;
#104325=ORIENTED_EDGE ( 'NONE', *, *, #88444, .F. ) ;
#104328=DIRECTION ( 'NONE',  ( 0.000000000000000000, -1.000000000000000000, 0.000000000000000000 ) ) ;
#104339=ORIENTED_EDGE ( 'NONE', *, *, #64505, .T. ) ;
#104385=DIRECTION ( 'NONE',  ( 0.000000000000000000, -1.000000000000000000, 0.000000000000000000 ) ) ;
#104401=EDGE_CURVE ( 'NONE', #27178, #57410, #24428, .T. ) ;
#104406=ORIENTED_EDGE ( 'NONE', *, *, #67, .T. ) ;
#104465=EDGE_CURVE ( 'NONE', #13469, #92048, #33039, .T. ) ;
#104467=ORIENTED_EDGE ( 'NONE', *, *, #15197, .F. ) ;
#104505=EDGE_LOOP ( 'NONE', ( #41910, #67230, #76457, #52045, #35949, #49717 ) ) ;
#104572=FACE_OUTER_BOUND ( 'NONE', #33175, .T. ) ;
#104685=EDGE_CURVE ( 'NONE', #7953, #85648, #18112, .T. ) ;
#104733=AXIS2_PLACEMENT_3D ( 'NONE', #90570, #16681, #49572 ) ;
#104741=VERTEX_POINT ( 'NONE', #86041 ) ;
#104789=ADVANCED_FACE ( 'NONE', ( #61223 ), #94107, .T. ) ;
#104801=ADVANCED_FACE ( 'NONE', ( #20810 ), #88229, .T. ) ;
#104814=CARTESIAN_POINT ( 'NONE',  ( -8.012931681025682785E-15, -7.321656987762868773, 3.318518101603009196 ) ) ;
#104859=DIRECTION ( 'NONE',  ( -1.000000000000000000, -1.224606353822377258E-16, -0.000000000000000000 ) ) ;
#104931=ORIENTED_EDGE ( 'NONE', *, *, #44547, .F. ) ;
#104939=FACE_OUTER_BOUND ( 'NONE', #70468, .T. ) ;
#104955=ADVANCED_FACE ( 'NONE', ( #17452 ), #91337, .T. ) ;
#104972=CARTESIAN_POINT ( 'NONE',  ( 99.17777777777777715, 1.023464760207051730E-14, 0.000000000000000000 ) ) ;
#105014=DIRECTION ( 'NONE',  ( -1.000000000000000000, -0.000000000000000000, -0.000000000000000000 ) ) ;
#105060=CARTESIAN_POINT ( 'NONE',  ( 103.5111111111111057, 4.172000000000019249, 5.109226446042768454E-16 ) ) ;
#105076=EDGE_CURVE ( 'NONE', #102006, #64162, #70764, .T. ) ;
#105088=CARTESIAN_POINT ( 'NONE',  ( 0.000000000000000000, 9.797174393178825657E-16, -8.000000000000000000 ) ) ;
#105111=EDGE_CURVE ( 'NONE', #62320, #74466, #12713, .T. ) ;
#105117=DIRECTION ( 'NONE',  ( 0.000000000000000000, -1.000000000000000000, 0.000000000000000000 ) ) ;
#105119=EDGE_LOOP ( 'NONE', ( #3712, #21718, #7967, #2317, #23435 ) ) ;
#105138=EDGE_CURVE ( 'NONE', #62320, #37220, #89750, .T. ) ;
#105152=ORIENTED_EDGE ( 'NONE', *, *, #7935, .T. ) ;
#105156=CARTESIAN_POINT ( 'NONE',  ( 0.7145311798163270778, 9.237604307034018802, 3.185620757954082679E-16 ) ) ;
#105165=CARTESIAN_POINT ( 'NONE',  ( 95.42421628608209971, 1.030564683017419500E-14, 0.000000000000000000 ) ) ;
#105209=AXIS2_PLACEMENT_3D ( 'NONE', #13395, #20512, #30151 ) ;
#105268=CARTESIAN_POINT ( 'NONE',  ( 81.26467260280679739, 6.123233995736582872E-16, -5.000000000000011546 ) ) ;
#105278=VERTEX_POINT ( 'NONE', #39472 ) ;
#105316=CARTESIAN_POINT ( 'NONE',  ( 79.82022815836235452, -2.002967142162725287E-29, 5.000000000000011546 ) ) ;
#105319=PLANE ( 'NONE',  #11804 ) ;
#105378=CARTESIAN_POINT ( 'NONE',  ( 0.3194001229792609586, 3.115132258397516729, -7.999999999999998224 ) ) ;
#105412=CARTESIAN_POINT ( 'NONE',  ( 89.93133926947346879, -5.000000000000000000, 0.000000000000000000 ) ) ;
#105421=AXIS2_PLACEMENT_3D ( 'NONE', #92607, #19838, #76417 ) ;
#105462=AXIS2_PLACEMENT_3D ( 'NONE', #60572, #93462, #91852 ) ;
#105563=CONICAL_SURFACE ( 'NONE', #5628, 5.000000000000010658, 0.9599310885968697082 ) ;
#105571=ORIENTED_EDGE ( 'NONE', *, *, #86311, .T. ) ;
#105574=CIRCLE ( 'NONE', #24606, 5.000000000000010658 ) ;
#105582=PRODUCT_DEFINITION ( 'UNKNOWN', '', #47376, #76901 ) ;
#105596=ADVANCED_FACE ( 'NONE', ( #81750 ), #81226, .T. ) ;
#105641=ORIENTED_EDGE ( 'NONE', *, *, #14814, .F. ) ;
#105643=DIRECTION ( 'NONE',  ( -1.000000000000000000, -1.224606353822377258E-16, -0.000000000000000000 ) ) ;
#105666=DIRECTION ( 'NONE',  ( 0.5735764363510554853, 0.8191520442889852482, 0.000000000000000000 ) ) ;
#105684=EDGE_CURVE ( 'NONE', #10713, #1566, #24634, .T. ) ;
#105716=ORIENTED_EDGE ( 'NONE', *, *, #11199, .T. ) ;
#105739=EDGE_CURVE ( 'NONE', #17510, #28693, #94125, .T. ) ;
#105751=CARTESIAN_POINT ( 'NONE',  ( 6.400000000000000355, 0.000000000000000000, -5.400000000000001243 ) ) ;
#105755=DIRECTION ( 'NONE',  ( -1.000000000000000000, -0.000000000000000000, -0.000000000000000000 ) ) ;
#105791=CARTESIAN_POINT ( 'NONE',  ( 0.4969600502617480542, 4.995646404165275278, -7.347286611336972584 ) ) ;
#105837=CARTESIAN_POINT ( 'NONE',  ( 0.7145311798161605443, -4.618802153517258979, -8.000000000000001776 ) ) ;
#105860=LINE ( 'NONE', #97762, #72941 ) ;
#105871=EDGE_CURVE ( 'NONE', #20011, #66540, #66531, .T. ) ;
#105937=DIRECTION ( 'NONE',  ( 0.000000000000000000, 0.000000000000000000, 1.000000000000000000 ) ) ;
#105941=ORIENTED_EDGE ( 'NONE', *, *, #98530, .F. ) ;
#105965=ORIENTED_EDGE ( 'NONE', *, *, #28617, .F. ) ;
#105973=VERTEX_POINT ( 'NONE', #105268 ) ;
#105982=ORIENTED_EDGE ( 'NONE', *, *, #86457, .T. ) ;
#105990=AXIS2_PLACEMENT_3D ( 'NONE', #52623, #85553, #95235 ) ;
#105997=AXIS2_PLACEMENT_3D ( 'NONE', #34722, #76725, #35791 ) ;
#106005=AXIS2_PLACEMENT_3D ( 'NONE', #84264, #27669, #43275 ) ;
#106008=EDGE_CURVE ( 'NONE', #45973, #9203, #82250, .T. ) ;
#106022=CARTESIAN_POINT ( 'NONE',  ( 81.84444444444444855, -4.171999999999998820, 5.616230220889773285E-16 ) ) ;
#106033=CARTESIAN_POINT ( 'NONE',  ( 0.000000000000000000, 0.000000000000000000, 0.000000000000000000 ) ) ;
#106037=EDGE_LOOP ( 'NONE', ( #19386, #38448, #30081, #34865, #41267 ) ) ;
#106055=DIRECTION ( 'NONE',  ( -1.000000000000000000, -1.224606353822377258E-16, -0.000000000000000000 ) ) ;
#106083=DIRECTION ( 'NONE',  ( 1.000000000000000000, 1.224606353822377258E-16, 0.000000000000000000 ) ) ;
#106123=VECTOR ( 'NONE', #37058, 1000.000000000000000 ) ;
#106137=VECTOR ( 'NONE', #16494, 1000.000000000000000 ) ;
#106150=AXIS2_PLACEMENT_3D ( 'NONE', #9854, #42766, #60573 ) ;
#106155=CONICAL_SURFACE ( 'NONE', #102725, 8.000000000000000000, 1.047197551196600296 ) ;
#106195=LINE ( 'NONE', #16139, #14051 ) ;
#106198=EDGE_CURVE ( 'NONE', #77127, #231, #29651, .T. ) ;
#106211=ORIENTED_EDGE ( 'NONE', *, *, #100436, .F. ) ;
#106227=VECTOR ( 'NONE', #7353, 1000.000000000000000 ) ;
#106249=CIRCLE ( 'NONE', #28792, 8.000000000000000000 ) ;
#106252=CARTESIAN_POINT ( 'NONE',  ( 106.4000000000000057, 0.000000000000000000, 0.000000000000000000 ) ) ;
#106259=EDGE_CURVE ( 'NONE', #45933, #99558, #238, .T. ) ;
#106403=EDGE_CURVE ( 'NONE', #45933, #76580, #98439, .T. ) ;
#106488=ORIENTED_EDGE ( 'NONE', *, *, #100977, .T. ) ;
#106518=CIRCLE ( 'NONE', #79045, 4.172000000000009479 ) ;
#106523=ADVANCED_FACE ( 'NONE', ( #22665, #56033 ), #88964, .T. ) ;
#106658=DIRECTION ( 'NONE',  ( -1.000000000000000000, -1.224606353822377258E-16, -0.000000000000000000 ) ) ;
#106677=COLOUR_RGB ( '', 0.66274510, 0.83137255, 0.94901961) ;
#106683=DIRECTION ( 'NONE',  ( -1.000000000000000000, -1.224606353822377258E-16, -0.000000000000000000 ) ) ;
#106685=CIRCLE ( 'NONE', #87769, 8.000000000000000000 ) ;
#106693=EDGE_LOOP ( 'NONE', ( #46642, #27334, #75865, #49272, #102054, #79035 ) ) ;
#106694=AXIS2_PLACEMENT_3D ( 'NONE', #60202, #91486, #18135 ) ;
#106711=ORIENTED_EDGE ( 'NONE', *, *, #53240, .F. ) ;
#106717=EDGE_CURVE ( 'NONE', #21366, #17909, #7267, .T. ) ;
#106741=CARTESIAN_POINT ( 'NONE',  ( 95.42421628608209971, 1.030564683017419500E-14, 0.000000000000000000 ) ) ;
#106763=DIRECTION ( 'NONE',  ( 1.000000000000000000, 1.224606353822377258E-16, 0.000000000000000000 ) ) ;
#106766=FACE_OUTER_BOUND ( 'NONE', #55004, .T. ) ;
ENDSEC;
END-ISO-10303-21;
